ISO-10303-21;
HEADER;
/* Generated by software containing ST-Developer
 * from STEP Tools, Inc. (www.steptools.com) 
 */

FILE_DESCRIPTION(
/* description */ (''),
/* implementation_level */ '2;1');

FILE_NAME(
/* name */ 'Screw_02.step',
/* time_stamp */ '2026-10-04T22:56:18-07:00',
/* author */ (''),
/* organization */ (''),
/* preprocessor_version */ 'ST-DEVELOPER v20.2',
/* originating_system */ 'Autodesk Translation Framework v15.15.0.0',
/* authorisation */ '');

FILE_SCHEMA (('AUTOMOTIVE_DESIGN { 1 0 10303 214 3 1 1 }'));
ENDSEC;

DATA;
#10=MECHANICAL_DESIGN_GEOMETRIC_PRESENTATION_REPRESENTATION('',(#197),#14544);
#50=CONICAL_SURFACE('',#2110,3.70051543670999,0.906750163968186);
#53=B_SPLINE_SURFACE_WITH_KNOTS('',3,3,((#13719,#13720,#13721,#13722,#13723,
#13724,#13725,#13726,#13727,#13728,#13729,#13730,#13731,#13732,#13733,#13734,
#13735,#13736,#13737,#13738,#13739,#13740,#13741,#13742,#13743,#13744,#13745,
#13746,#13747,#13748,#13749,#13750,#13751,#13752,#13753,#13754,#13755,#13756,
#13757,#13758,#13759,#13760,#13761,#13762,#13763,#13764,#13765,#13766,#13767,
#13768,#13769,#13770),(#13771,#13772,#13773,#13774,#13775,#13776,#13777,
#13778,#13779,#13780,#13781,#13782,#13783,#13784,#13785,#13786,#13787,#13788,
#13789,#13790,#13791,#13792,#13793,#13794,#13795,#13796,#13797,#13798,#13799,
#13800,#13801,#13802,#13803,#13804,#13805,#13806,#13807,#13808,#13809,#13810,
#13811,#13812,#13813,#13814,#13815,#13816,#13817,#13818,#13819,#13820,#13821,
#13822),(#13823,#13824,#13825,#13826,#13827,#13828,#13829,#13830,#13831,
#13832,#13833,#13834,#13835,#13836,#13837,#13838,#13839,#13840,#13841,#13842,
#13843,#13844,#13845,#13846,#13847,#13848,#13849,#13850,#13851,#13852,#13853,
#13854,#13855,#13856,#13857,#13858,#13859,#13860,#13861,#13862,#13863,#13864,
#13865,#13866,#13867,#13868,#13869,#13870,#13871,#13872,#13873,#13874),
(#13875,#13876,#13877,#13878,#13879,#13880,#13881,#13882,#13883,#13884,
#13885,#13886,#13887,#13888,#13889,#13890,#13891,#13892,#13893,#13894,#13895,
#13896,#13897,#13898,#13899,#13900,#13901,#13902,#13903,#13904,#13905,#13906,
#13907,#13908,#13909,#13910,#13911,#13912,#13913,#13914,#13915,#13916,#13917,
#13918,#13919,#13920,#13921,#13922,#13923,#13924,#13925,#13926)),
 .UNSPECIFIED.,.F.,.F.,.F.,(4,4),(4,1,1,1,1,1,1,1,1,1,1,1,1,1,1,1,1,1,1,
1,1,1,1,1,1,1,1,1,1,1,1,1,1,1,1,1,1,1,1,1,1,1,1,1,1,1,1,1,1,4),(-0.000425975868175074,
0.0530000950082445),(8.30815772716284,9.30770753701498,10.3072573468671,
11.3068071567193,12.3063569665714,13.3059067764236,14.3054565862757,15.3050063961278,
16.30455620598,17.3041060158321,18.3036558256843,19.3032056355364,20.3027554453886,
21.3023052552407,22.3018550650929,23.301404874945,24.3009546847971,25.3005044946493,
26.3000543045014,27.2996041143536,28.2991539242057,29.2987037340579,30.29825354391,
31.2978033537621,32.2973531636143,33.2969029734664,34.2964527833186,35.2960025931707,
36.2955524030229,37.295102212875,38.2946520227271,39.2942018325793,40.2937516424314,
41.2933014522836,42.2928512621357,43.2924010719879,44.29195088184,45.2915006916922,
46.2910505015443,47.2906003113964,48.2901501212486,49.2896999311007,50.2892497409529,
51.288799550805,52.2883493606572,53.2878991705093,54.2874489803615,55.2869987902136,
56.2865486000657,57.2865243857861),.UNSPECIFIED.);
#54=B_SPLINE_SURFACE_WITH_KNOTS('',3,3,((#14187,#14188,#14189,#14190,#14191,
#14192,#14193,#14194,#14195,#14196,#14197,#14198,#14199,#14200,#14201,#14202,
#14203,#14204,#14205,#14206,#14207,#14208,#14209,#14210,#14211,#14212,#14213,
#14214,#14215,#14216,#14217,#14218,#14219,#14220,#14221,#14222,#14223,#14224,
#14225,#14226,#14227,#14228,#14229,#14230,#14231,#14232,#14233,#14234,#14235,
#14236,#14237,#14238),(#14239,#14240,#14241,#14242,#14243,#14244,#14245,
#14246,#14247,#14248,#14249,#14250,#14251,#14252,#14253,#14254,#14255,#14256,
#14257,#14258,#14259,#14260,#14261,#14262,#14263,#14264,#14265,#14266,#14267,
#14268,#14269,#14270,#14271,#14272,#14273,#14274,#14275,#14276,#14277,#14278,
#14279,#14280,#14281,#14282,#14283,#14284,#14285,#14286,#14287,#14288,#14289,
#14290),(#14291,#14292,#14293,#14294,#14295,#14296,#14297,#14298,#14299,
#14300,#14301,#14302,#14303,#14304,#14305,#14306,#14307,#14308,#14309,#14310,
#14311,#14312,#14313,#14314,#14315,#14316,#14317,#14318,#14319,#14320,#14321,
#14322,#14323,#14324,#14325,#14326,#14327,#14328,#14329,#14330,#14331,#14332,
#14333,#14334,#14335,#14336,#14337,#14338,#14339,#14340,#14341,#14342),
(#14343,#14344,#14345,#14346,#14347,#14348,#14349,#14350,#14351,#14352,
#14353,#14354,#14355,#14356,#14357,#14358,#14359,#14360,#14361,#14362,#14363,
#14364,#14365,#14366,#14367,#14368,#14369,#14370,#14371,#14372,#14373,#14374,
#14375,#14376,#14377,#14378,#14379,#14380,#14381,#14382,#14383,#14384,#14385,
#14386,#14387,#14388,#14389,#14390,#14391,#14392,#14393,#14394)),
 .UNSPECIFIED.,.F.,.F.,.F.,(4,4),(4,1,1,1,1,1,1,1,1,1,1,1,1,1,1,1,1,1,1,
1,1,1,1,1,1,1,1,1,1,1,1,1,1,1,1,1,1,1,1,1,1,1,1,1,1,1,1,1,1,4),(-0.000359185103406873,
0.0530514251731689),(11.6159672492052,12.6159430071938,13.615492817046,
14.6150426268981,15.6145924367503,16.6141422466024,17.6136920564545,18.6132418663067,
19.6127916761588,20.612341486011,21.6118912958631,22.6114411057153,23.6109909155674,
24.6105407254196,25.6100905352717,26.6096403451238,27.609190154976,28.6087399648281,
29.6082897746803,30.6078395845324,31.6073893943846,32.6069392042367,33.6064890140888,
34.606038823941,35.6055886337931,36.6051384436453,37.6046882534974,38.6042380633496,
39.6037878732017,40.6033376830538,41.602887492906,42.6024373027581,43.6019871126103,
44.6015369224624,45.6010867323146,46.6006365421667,47.6001863520188,48.599736161871,
49.5992859717231,50.5988357815753,51.5983855914274,52.5979354012796,53.5974852111317,
54.5970350209839,55.596584830836,56.5961346406881,57.5956844505403,58.5952342603924,
59.5947840702446,60.5943338800967),.UNSPECIFIED.);
#122=B_SPLINE_CURVE_WITH_KNOTS('',3,(#8676,#8677,#8678,#8679,#8680,#8681,
#8682,#8683),.UNSPECIFIED.,.F.,.F.,(4,1,1,1,1,4),(10.3751771421666,11.3068071567193,
12.3063569665714,13.3059067764236,14.3054565862757,15.1257192387471),
 .UNSPECIFIED.);
#123=B_SPLINE_CURVE_WITH_KNOTS('',3,(#8686,#8687,#8688,#8689,#8690,#8691,
#8692,#8693,#8694,#8695,#8696,#8697,#8698,#8699,#8700,#8701,#8702,#8703,
#8704,#8705,#8706,#8707,#8708,#8709,#8710,#8711,#8712,#8713,#8714,#8715,
#8716,#8717,#8718,#8719,#8720,#8721,#8722,#8723,#8724,#8725,#8726,#8727,
#8728,#8729,#8730,#8731,#8732,#8733,#8734,#8735,#8736,#8737,#8738,#8739,
#8740,#8741,#8742,#8743,#8744,#8745,#8746,#8747,#8748,#8749,#8750,#8751,
#8752,#8753,#8754,#8755,#8756,#8757,#8758,#8759,#8760,#8761,#8762,#8763,
#8764,#8765,#8766,#8767,#8768,#8769,#8770,#8771,#8772,#8773,#8774,#8775,
#8776,#8777,#8778,#8779),.UNSPECIFIED.,.F.,.F.,(4,2,2,2,2,2,2,2,2,2,2,2,
2,2,2,2,2,2,2,2,2,2,2,2,2,2,2,2,2,2,2,2,2,2,2,2,2,2,2,2,2,2,2,2,2,2,4),
(-2.07535699417274,-2.07062624526911,-2.06390397808145,-2.03913496638295,
-2.01054723885914,-1.99466355694519,-1.98597044106963,-1.97810011824729,
-1.96742913432041,-1.93617993541108,-1.90152147750812,-1.89003277159946,
-1.8815263154361,-1.87695834489268,-1.8729734601704,-1.86687528387374,-1.84488951098834,
-1.79878739549274,-1.7862206749192,-1.77883081238585,-1.77203218474349,
-1.76280246808816,-1.73953077312565,-1.70020061595449,-1.68839386433749,
-1.67985016566027,-1.6754535499156,-1.67147820244209,-1.66552760282937,
-1.647152261186,-1.60862847305887,-1.59400947809981,-1.58211143388748,-1.57457733824053,
-1.56734072385867,-1.55670381365091,-1.51422192860002,-1.4878998886173,
-1.48032481757243,-1.47592214047974,-1.47211852010191,-1.46536351188341,
-1.42636243278102,-1.39463510154257,-1.38348036493685,-1.37610595103745,
-1.37340468443901),.UNSPECIFIED.);
#124=B_SPLINE_CURVE_WITH_KNOTS('',3,(#8785,#8786,#8787,#8788,#8789,#8790,
#8791,#8792,#8793,#8794,#8795,#8796,#8797,#8798,#8799,#8800,#8801,#8802,
#8803,#8804,#8805,#8806,#8807,#8808,#8809,#8810,#8811,#8812,#8813,#8814,
#8815,#8816,#8817,#8818,#8819,#8820,#8821,#8822,#8823,#8824,#8825,#8826,
#8827,#8828,#8829,#8830,#8831,#8832,#8833,#8834,#8835,#8836,#8837,#8838,
#8839,#8840,#8841,#8842,#8843,#8844,#8845,#8846,#8847,#8848,#8849,#8850,
#8851,#8852,#8853,#8854,#8855,#8856,#8857,#8858,#8859,#8860,#8861,#8862,
#8863,#8864,#8865,#8866,#8867,#8868,#8869,#8870,#8871,#8872,#8873,#8874,
#8875,#8876,#8877,#8878,#8879,#8880,#8881,#8882,#8883,#8884,#8885,#8886,
#8887,#8888,#8889,#8890,#8891,#8892,#8893,#8894,#8895,#8896,#8897,#8898,
#8899,#8900,#8901,#8902,#8903,#8904,#8905,#8906,#8907,#8908,#8909,#8910,
#8911,#8912,#8913,#8914,#8915,#8916,#8917,#8918,#8919,#8920,#8921,#8922,
#8923,#8924,#8925,#8926,#8927,#8928,#8929,#8930,#8931,#8932,#8933,#8934,
#8935,#8936,#8937,#8938,#8939,#8940,#8941,#8942,#8943,#8944,#8945,#8946,
#8947,#8948,#8949,#8950,#8951,#8952,#8953,#8954,#8955,#8956),
 .UNSPECIFIED.,.F.,.F.,(4,3,3,3,3,3,3,3,3,3,3,3,3,3,3,3,3,3,3,3,3,3,3,3,
3,3,3,3,3,3,3,3,3,3,3,3,3,3,3,3,3,3,3,3,3,3,3,3,3,3,3,3,3,3,3,3,3,4),(15.7079632679489,
15.8140060705019,15.9200901242099,16.0263330305178,16.1326617635271,16.2392097967397,
16.30455620598,16.4094926907624,16.5142711739612,16.6189258395903,16.7235142950206,
16.8280721401984,16.9326349307205,17.0373085987797,17.1420432536121,17.2469612836429,
17.3041060158321,17.4090419624236,17.5138199393734,17.6184741490198,17.7230621798904,
17.8276196326623,17.9321820636969,18.0368554252288,18.1415898031092,18.2465076058582,
18.3036558256843,18.4085885657132,18.5133632718617,18.6180141312869,18.7225987646189,
18.8271527776088,18.931711731645,19.0363815833322,19.141112427443,19.2460266968149,
19.3032056355364,19.4081402098677,19.5129167767403,19.6175695269526,19.7221560686272,
19.8267120046426,19.9312728935312,20.0359446847347,20.1406774739337,20.2455936761873,
20.3027554453886,20.4076898194264,20.5124661874783,20.6171187420747,20.7217050902322,
20.8262608351303,20.9308215356054,21.035493143851,21.1402257529102,21.2451417814176,
21.3023052552407,21.4102199499323),.UNSPECIFIED.);
#125=B_SPLINE_CURVE_WITH_KNOTS('',3,(#8957,#8958,#8959,#8960,#8961),
 .UNSPECIFIED.,.F.,.F.,(4,1,4),(15.1257192387471,15.3050063961278,15.7079567456947),
 .UNSPECIFIED.);
#126=B_SPLINE_CURVE_WITH_KNOTS('',3,(#8962,#8963,#8964,#8965,#8966,#8967,
#8968,#8969,#8970,#8971,#8972,#8973,#8974,#8975,#8976,#8977,#8978,#8979,
#8980,#8981,#8982,#8983,#8984,#8985,#8986,#8987,#8988,#8989,#8990,#8991,
#8992,#8993,#8994,#8995,#8996,#8997,#8998,#8999,#9000,#9001,#9002,#9003,
#9004,#9005,#9006,#9007,#9008,#9009,#9010,#9011,#9012,#9013,#9014,#9015,
#9016,#9017,#9018,#9019,#9020,#9021,#9022,#9023,#9024,#9025,#9026,#9027,
#9028,#9029,#9030,#9031,#9032,#9033,#9034,#9035,#9036,#9037,#9038,#9039,
#9040,#9041,#9042,#9043,#9044,#9045,#9046,#9047,#9048,#9049,#9050,#9051,
#9052,#9053,#9054,#9055,#9056,#9057,#9058,#9059,#9060,#9061,#9062,#9063,
#9064,#9065,#9066,#9067,#9068,#9069,#9070,#9071,#9072,#9073,#9074,#9075,
#9076,#9077,#9078,#9079,#9080,#9081,#9082,#9083,#9084,#9085,#9086,#9087,
#9088,#9089,#9090,#9091,#9092,#9093,#9094,#9095,#9096,#9097,#9098,#9099,
#9100,#9101,#9102,#9103,#9104,#9105,#9106,#9107,#9108,#9109,#9110,#9111,
#9112,#9113,#9114,#9115,#9116,#9117,#9118,#9119,#9120,#9121,#9122,#9123,
#9124,#9125),.UNSPECIFIED.,.F.,.F.,(4,2,2,2,2,2,2,2,2,2,2,2,2,2,2,2,2,2,
2,2,2,2,2,2,2,2,2,2,2,2,2,2,2,2,2,2,2,2,2,2,2,2,2,2,2,2,2,2,2,2,2,2,2,2,
2,2,2,2,2,2,2,2,2,2,2,2,2,2,2,2,2,2,2,2,2,2,2,2,2,2,2,4),(-1.37340468443901,
-1.36871743081555,-1.35748583702605,-1.3200010148775,-1.29672758652404,
-1.28744009490948,-1.28019430521612,-1.27590019966677,-1.2716085688058,
-1.26427445536536,-1.22518572267299,-1.19428746066202,-1.18328761720507,
-1.17599945296877,-1.16869369100309,-1.15759715127668,-1.1181943045483,
-1.09601897457847,-1.0869871962481,-1.07990084592359,-1.07566513746222,
-1.07134135369325,-1.06390168160929,-1.03810159496872,-0.992803412570896,
-0.982338601089973,-0.975177691561462,-0.96770063758569,-0.955857909323519,
-0.941268128320568,-0.902444827390983,-0.884869616820766,-0.878940686944186,
-0.874885335771914,-0.8701287887699,-0.860444431478508,-0.846440319909858,
-0.81679757628812,-0.811538025734025,-0.790068708525572,-0.780999903268975,
-0.773948618441998,-0.765995966563767,-0.751522254455603,-0.731996729298023,
-0.691751235073339,-0.682044394561865,-0.677285813277941,-0.673242944351546,
-0.667351658205613,-0.648687982702851,-0.598586700061476,-0.585406495261867,
-0.577693318198781,-0.570590040383836,-0.560886292698399,-0.531591748652482,
-0.490049087033579,-0.481436396826925,-0.476882546047545,-0.472770001759554,
-0.466425444949794,-0.439660929000518,-0.392740047594552,-0.382512461256994,
-0.375396513289168,-0.367869588254539,-0.355723130340433,-0.322764296660365,
-0.287567482415229,-0.280428805481126,-0.276165142153246,-0.271836165726112,
-0.264372895412004,-0.238768212099689,-0.193299058928824,-0.182872884802073,
-0.175726134313817,-0.168255059270011,-0.156406019240682,-0.141805592911803,
-0.116782820621066),.UNSPECIFIED.);
#127=B_SPLINE_CURVE_WITH_KNOTS('',3,(#9131,#9132,#9133,#9134,#9135,#9136,
#9137,#9138,#9139,#9140,#9141,#9142,#9143,#9144,#9145,#9146,#9147,#9148,
#9149,#9150,#9151,#9152,#9153,#9154,#9155,#9156,#9157,#9158,#9159,#9160,
#9161,#9162,#9163,#9164,#9165,#9166,#9167,#9168,#9169,#9170,#9171,#9172,
#9173,#9174,#9175,#9176,#9177,#9178,#9179,#9180,#9181,#9182,#9183,#9184,
#9185,#9186,#9187,#9188,#9189,#9190,#9191,#9192,#9193,#9194,#9195,#9196,
#9197,#9198,#9199,#9200,#9201,#9202,#9203,#9204,#9205,#9206,#9207,#9208,
#9209,#9210,#9211,#9212,#9213,#9214,#9215,#9216,#9217,#9218,#9219,#9220,
#9221,#9222,#9223,#9224,#9225,#9226,#9227,#9228,#9229,#9230,#9231,#9232,
#9233,#9234,#9235,#9236,#9237,#9238,#9239,#9240,#9241,#9242,#9243,#9244,
#9245,#9246,#9247,#9248,#9249,#9250,#9251,#9252,#9253,#9254,#9255,#9256,
#9257,#9258,#9259,#9260,#9261,#9262,#9263,#9264,#9265,#9266,#9267,#9268,
#9269,#9270,#9271,#9272,#9273,#9274,#9275,#9276,#9277,#9278,#9279,#9280),
 .UNSPECIFIED.,.F.,.F.,(4,2,2,2,2,2,2,2,2,2,2,2,2,2,2,2,2,2,2,2,2,2,2,2,
2,2,2,2,2,2,2,2,2,2,2,2,2,2,2,2,2,2,2,2,2,2,2,2,2,2,2,2,2,2,2,2,2,2,2,2,
2,2,2,2,2,2,2,2,2,2,2,2,2,2,4),(-1.14061870450622,-1.13958195964596,-1.12266879087202,
-1.08281934178168,-1.06959889951782,-1.06471429770308,-1.06068012672009,
-1.05587064594565,-1.04587632392007,-0.999418617025877,-0.976433036897593,
-0.967166228933324,-0.960092877789842,-0.952248888383839,-0.938376963922012,
-0.920052937498073,-0.894060657937701,-0.871556239654625,-0.865322258102495,
-0.861267461095725,-0.856682550344552,-0.847919948238388,-0.801100630640885,
-0.799115970822433,-0.776456064607275,-0.767226345807944,-0.76015819165588,
-0.752296729049045,-0.738324922715054,-0.719803447177033,-0.693815912555669,
-0.67165232509663,-0.665434233695802,-0.661382280499621,-0.656791660709034,
-0.64799739350855,-0.606818368303741,-0.577680011860102,-0.567920265960079,
-0.560804794226708,-0.553104033972044,-0.540012435378701,-0.516652027872025,
-0.473266797217643,-0.466300249493322,-0.462071551381904,-0.457702709275398,
-0.450041696240669,-0.440005173513315,-0.412835238526543,-0.380872948511376,
-0.369743491624624,-0.362402893987223,-0.35506506155264,-0.343951299162992,
-0.312385485717975,-0.272863502890842,-0.266179132741583,-0.26241555881735,
-0.258115242971251,-0.250793298578873,-0.226411012152923,-0.17878218694598,
-0.168659285477799,-0.161560276461644,-0.154003631587863,-0.14169344121923,
-0.11377328835674,-0.0754140544872524,-0.0673951691566298,-0.0629547708213861,
-0.0587770332817225,-0.0520752430550884,-0.0212767115436388,-0.000594353055929244),
 .UNSPECIFIED.);
#128=B_SPLINE_CURVE_WITH_KNOTS('',3,(#9281,#9282,#9283,#9284,#9285,#9286,
#9287,#9288,#9289,#9290,#9291,#9292,#9293,#9294,#9295,#9296,#9297,#9298,
#9299),.UNSPECIFIED.,.F.,.F.,(4,3,3,3,3,3,4),(21.4102199499323,21.5145277033485,
21.6187228794953,21.722854083458,21.8269466273695,21.9310741676971,21.9911485751285),
 .UNSPECIFIED.);
#129=B_SPLINE_CURVE_WITH_KNOTS('',3,(#9301,#9302,#9303,#9304,#9305,#9306,
#9307,#9308,#9309,#9310,#9311,#9312,#9313,#9314,#9315,#9316,#9317,#9318),
 .UNSPECIFIED.,.F.,.F.,(4,2,2,2,2,2,2,2,4),(-0.116782820621066,-0.102980098125634,
-0.085284604519627,-0.0793273984135347,-0.0752749720407285,-0.0705497398843767,
-0.06102445685247,-0.0473538417127571,-0.00061658398721623),
 .UNSPECIFIED.);
#130=B_SPLINE_CURVE_WITH_KNOTS('',3,(#9319,#9320,#9321,#9322,#9323,#9324,
#9325,#9326,#9327,#9328,#9329,#9330,#9331,#9332,#9333,#9334,#9335,#9336,
#9337,#9338,#9339,#9340,#9341,#9342,#9343,#9344,#9345,#9346,#9347,#9348,
#9349,#9350,#9351,#9352,#9353,#9354,#9355,#9356,#9357,#9358,#9359,#9360,
#9361,#9362,#9363,#9364,#9365,#9366,#9367,#9368,#9369,#9370,#9371,#9372,
#9373,#9374,#9375,#9376,#9377,#9378,#9379,#9380,#9381,#9382,#9383,#9384,
#9385,#9386,#9387,#9388,#9389,#9390,#9391,#9392,#9393,#9394,#9395,#9396,
#9397,#9398,#9399,#9400,#9401,#9402,#9403,#9404,#9405,#9406,#9407,#9408,
#9409,#9410,#9411,#9412,#9413,#9414,#9415,#9416,#9417,#9418,#9419,#9420,
#9421,#9422,#9423,#9424,#9425,#9426,#9427,#9428,#9429,#9430,#9431,#9432,
#9433,#9434,#9435,#9436,#9437,#9438,#9439,#9440,#9441,#9442,#9443,#9444,
#9445,#9446,#9447,#9448,#9449,#9450,#9451,#9452,#9453,#9454,#9455,#9456,
#9457,#9458,#9459,#9460,#9461,#9462,#9463,#9464,#9465,#9466,#9467,#9468,
#9469,#9470,#9471,#9472,#9473,#9474),.UNSPECIFIED.,.F.,.F.,(4,2,2,2,2,2,
2,2,2,2,2,2,2,2,2,2,2,2,2,2,2,2,2,2,2,2,2,2,2,2,2,2,2,2,2,2,2,2,2,2,2,2,
2,2,2,2,2,2,2,2,2,2,2,2,2,2,2,2,2,2,2,2,2,2,2,2,2,2,2,2,2,2,2,2,2,2,2,4),
(-2.51378437080705,-2.50403412993197,-2.49569275978735,-2.4890492244808,
-2.48247746651656,-2.47156832709352,-2.43112912652391,-2.40958993904581,
-2.40069266360761,-2.39367754444654,-2.38944008648743,-2.3850849117104,
-2.37748874337329,-2.33868487780727,-2.31048225053466,-2.29818897115585,
-2.29063663288652,-2.28353790617523,-2.27340912602132,-2.22578723704126,
-2.20137359621892,-2.19404819352388,-2.18974775666784,-2.18598580437682,
-2.17930772677495,-2.13976604713605,-2.10823733424573,-2.09712971628745,
-2.08979408129866,-2.08245438588889,-2.07132424549092,-2.03256101584112,
-2.01019268342857,-2.00111140656932,-1.99398988861816,-1.98973091019721,
-1.98593957491622,-1.97909176364722,-1.94107284853398,-1.90860126763712,
-1.89737409170347,-1.89001717454648,-1.88269853975448,-1.87168596483596,
-1.84317218534402,-1.81858185768069,-1.80513781418202,-1.79572151108212,
-1.79101608653026,-1.78695823582036,-1.78096166148747,-1.76211273249074,
-1.72427362390954,-1.70982229066988,-1.69805894240342,-1.69060420516893,
-1.68344794478296,-1.67296076088694,-1.62790910643968,-1.60882407495956,
-1.59698695384212,-1.59187884999028,-1.587881968817,-1.58259968637489,-1.57049888342963,
-1.52613809762451,-1.51084393113901,-1.49859846821437,-1.49105467975322,
-1.48395094353315,-1.47379181203992,-1.42636992345633,-1.40184009580425,
-1.39450071182093,-1.39019731016868,-1.38591207155117,-1.37866220630911,
-1.37342554502812),.UNSPECIFIED.);
#131=B_SPLINE_CURVE_WITH_KNOTS('',3,(#9479,#9480,#9481,#9482,#9483,#9484,
#9485,#9486,#9487,#9488,#9489,#9490,#9491,#9492,#9493,#9494,#9495,#9496,
#9497,#9498,#9499,#9500,#9501,#9502,#9503,#9504,#9505,#9506,#9507,#9508,
#9509,#9510,#9511,#9512,#9513,#9514,#9515,#9516,#9517,#9518,#9519,#9520,
#9521,#9522,#9523,#9524,#9525,#9526,#9527,#9528,#9529,#9530,#9531,#9532,
#9533,#9534,#9535,#9536,#9537,#9538,#9539,#9540,#9541,#9542,#9543,#9544,
#9545,#9546,#9547,#9548,#9549,#9550,#9551,#9552,#9553,#9554,#9555,#9556,
#9557,#9558,#9559,#9560,#9561,#9562,#9563,#9564,#9565,#9566,#9567,#9568,
#9569,#9570,#9571,#9572,#9573,#9574,#9575,#9576,#9577,#9578,#9579,#9580,
#9581,#9582,#9583,#9584,#9585,#9586,#9587,#9588,#9589,#9590,#9591,#9592,
#9593,#9594,#9595,#9596,#9597,#9598,#9599,#9600,#9601,#9602,#9603,#9604,
#9605,#9606,#9607,#9608,#9609,#9610,#9611,#9612,#9613,#9614,#9615,#9616,
#9617,#9618,#9619,#9620,#9621,#9622,#9623,#9624,#9625,#9626,#9627,#9628,
#9629,#9630,#9631,#9632,#9633,#9634,#9635,#9636,#9637,#9638,#9639,#9640),
 .UNSPECIFIED.,.F.,.F.,(4,2,2,2,2,2,2,2,2,2,2,2,2,2,2,2,2,2,2,2,2,2,2,2,
2,2,2,2,2,2,2,2,2,2,2,2,2,2,2,2,2,2,2,2,2,2,2,2,2,2,2,2,2,2,2,2,2,2,2,2,
2,2,2,2,2,2,2,2,2,2,2,2,2,2,2,2,2,2,2,2,4),(-2.39712982154602,-2.37982822062964,
-2.36865519395186,-2.36130697773033,-2.35397711103529,-2.34290705949758,
-2.30322269035014,-2.27203351873412,-2.26519392855631,-2.26099006907781,
-2.25658860397391,-2.24876473218744,-2.21021735720178,-2.18219173395406,
-2.16988518348984,-2.16232945507946,-2.15523034487358,-2.14670714630564,
-2.12298763570221,-2.07728526027882,-2.06741562350919,-2.06262840655135,
-2.05859008504526,-2.0527460756908,-2.03595372179219,-1.99628036112784,
-1.98156521764677,-1.96964904440506,-1.96216489337884,-1.95502446924087,
-1.94464244695748,-1.89880747281565,-1.87263665982996,-1.86560192359237,
-1.86135942682898,-1.85700648900914,-1.84942584938645,-1.81961990294089,
-1.79172799479035,-1.77912062417306,-1.76845651929048,-1.76119687894259,
-1.75463962397716,-1.74383518181111,-1.70132948089653,-1.67273853853663,
-1.66571201038827,-1.66147104391196,-1.6571159371628,-1.6495250466247,-1.62096258023062,
-1.58187612035999,-1.56990812464652,-1.56241413754037,-1.55527909917317,
-1.54493220248383,-1.49883577875733,-1.47356474731669,-1.46613856692982,
-1.46181676485615,-1.45754638164616,-1.45037367011324,-1.41575255653518,
-1.38212339666726,-1.3700711994623,-1.36256139372232,-1.35543508155993,
-1.34514442048775,-1.29863746327514,-1.27216652507063,-1.26552237131373,
-1.26135498595559,-1.25689625480186,-1.24878711935642,-1.23792668529515,
-1.20577170339601,-1.17728442476895,-1.16754158552402,-1.16042715070981,
-1.1527171437714,-1.14061870450622),.UNSPECIFIED.);
#132=B_SPLINE_CURVE_WITH_KNOTS('',3,(#9641,#9642,#9643,#9644,#9645,#9646,
#9647,#9648,#9649,#9650,#9651,#9652,#9653,#9654,#9655,#9656,#9657,#9658,
#9659,#9660,#9661,#9662,#9663,#9664,#9665,#9666,#9667,#9668,#9669,#9670,
#9671,#9672,#9673,#9674,#9675,#9676,#9677,#9678,#9679,#9680,#9681,#9682,
#9683,#9684,#9685,#9686,#9687,#9688,#9689,#9690,#9691,#9692,#9693,#9694,
#9695,#9696,#9697,#9698,#9699,#9700,#9701,#9702,#9703,#9704,#9705,#9706,
#9707,#9708,#9709,#9710,#9711,#9712,#9713,#9714,#9715,#9716,#9717,#9718,
#9719,#9720,#9721,#9722,#9723,#9724,#9725,#9726,#9727,#9728,#9729,#9730,
#9731,#9732,#9733,#9734,#9735,#9736,#9737,#9738,#9739,#9740,#9741,#9742,
#9743,#9744,#9745,#9746,#9747,#9748,#9749,#9750,#9751,#9752,#9753,#9754,
#9755,#9756,#9757,#9758,#9759,#9760,#9761,#9762,#9763,#9764,#9765,#9766,
#9767,#9768,#9769,#9770,#9771,#9772,#9773,#9774,#9775,#9776,#9777,#9778,
#9779,#9780,#9781,#9782,#9783,#9784,#9785,#9786,#9787,#9788,#9789,#9790,
#9791,#9792,#9793,#9794,#9795,#9796,#9797,#9798),.UNSPECIFIED.,.F.,.F.,
(4,2,2,2,2,2,2,2,2,2,2,2,2,2,2,2,2,2,2,2,2,2,2,2,2,2,2,2,2,2,2,2,2,2,2,
2,2,2,2,2,2,2,2,2,2,2,2,2,2,2,2,2,2,2,2,2,2,2,2,2,2,2,2,2,2,2,2,2,2,2,2,
2,2,2,2,2,2,2,4),(-1.37342554502812,-1.33696888519612,-1.31599588280204,
-1.30083372389245,-1.29276344707354,-1.28573464590891,-1.27671691634361,
-1.25701206626934,-1.22203976080302,-1.19977452572423,-1.1935519713523,
-1.18949971434911,-1.18491216460396,-1.17613234532156,-1.13518072828273,
-1.1057937615912,-1.09602774370631,-1.08891214603407,-1.08121550618681,
-1.06814289170902,-1.04441797874472,-1.00150686267968,-0.994457653340163,
-0.990212921266357,-0.985865078057203,-0.978306536753042,-0.951838422854677,
-0.907830865572262,-0.897213297876052,-0.890035291338718,-0.882611335137387,
-0.87101663977932,-0.856853444677602,-0.820884985122024,-0.799863535275151,
-0.793695479516006,-0.789651979329424,-0.785042309942625,-0.776144499491377,
-0.763758746982642,-0.718618715741055,-0.701985338797066,-0.693670919387845,
-0.686730787430037,-0.678081381148968,-0.659236756575006,-0.6288700647275,
-0.602489099950622,-0.595034534733468,-0.590708088271243,-0.586445484469463,
-0.579305810914881,-0.570193882432757,-0.547679508863399,-0.50920321758957,
-0.498061865773953,-0.490720365046891,-0.483386956059274,-0.472291126056974,
-0.440856639292396,-0.401114053743307,-0.394454688556459,-0.390695988214397,
-0.386390841739503,-0.379042034747994,-0.354426112834819,-0.307214774795675,
-0.29703259743498,-0.289925694224372,-0.282389439735313,-0.270182987341686,
-0.23694231788426,-0.202182775892267,-0.195016484547438,-0.190748523634948,
-0.186427790448431,-0.179001931413061,-0.153718969852119,-0.116908344231473),
 .UNSPECIFIED.);
#133=B_SPLINE_CURVE_WITH_KNOTS('',3,(#9804,#9805,#9806,#9807,#9808,#9809,
#9810,#9811,#9812,#9813,#9814,#9815,#9816,#9817,#9818,#9819,#9820,#9821,
#9822,#9823,#9824,#9825,#9826,#9827,#9828,#9829,#9830,#9831,#9832,#9833,
#9834,#9835,#9836,#9837,#9838,#9839,#9840,#9841,#9842,#9843,#9844,#9845,
#9846,#9847,#9848,#9849,#9850,#9851,#9852,#9853,#9854,#9855,#9856,#9857,
#9858,#9859,#9860,#9861,#9862,#9863,#9864,#9865,#9866,#9867,#9868,#9869,
#9870,#9871,#9872,#9873,#9874,#9875,#9876,#9877,#9878,#9879,#9880,#9881,
#9882,#9883,#9884,#9885,#9886,#9887,#9888,#9889,#9890,#9891,#9892,#9893,
#9894,#9895,#9896,#9897,#9898,#9899,#9900,#9901,#9902,#9903,#9904,#9905,
#9906,#9907,#9908,#9909,#9910,#9911,#9912,#9913,#9914,#9915,#9916,#9917,
#9918,#9919,#9920,#9921,#9922,#9923,#9924,#9925,#9926,#9927,#9928,#9929,
#9930,#9931,#9932,#9933,#9934,#9935,#9936,#9937,#9938,#9939,#9940,#9941,
#9942,#9943,#9944,#9945,#9946,#9947,#9948,#9949,#9950,#9951),
 .UNSPECIFIED.,.F.,.F.,(4,2,2,2,2,2,2,2,2,2,2,2,2,2,2,2,2,2,2,2,2,2,2,2,
2,2,2,2,2,2,2,2,2,2,2,2,2,2,2,2,2,2,2,2,2,2,2,2,2,2,2,2,2,2,2,2,2,2,2,2,
2,2,2,2,2,2,2,2,2,2,2,2,2,4),(-1.14097344694939,-1.13646400189371,-1.1272692673211,
-1.1043715879283,-1.06651269588549,-1.05534360370122,-1.04799598085995,
-1.04066523591785,-1.02959087664762,-0.998328570863161,-0.958311683721402,
-0.951683248647658,-0.947929237353639,-0.943614324414954,-0.936220341227765,
-0.911220910509429,-0.864704478268882,-0.854424034243729,-0.847300413186092,
-0.839789699374971,-0.827727506389926,-0.789091707982635,-0.760268461203665,
-0.752654206773099,-0.748294784768412,-0.744058328519856,-0.737053065241778,
-0.728174494290414,-0.706717110443944,-0.666442340431915,-0.655422435981745,
-0.648101226052769,-0.640743153429538,-0.629517000033496,-0.597067149632733,
-0.558970652836188,-0.552126791864149,-0.548335482489455,-0.544073736764986,
-0.536942388819262,-0.527845649679413,-0.505404300443613,-0.466810230385369,
-0.455673460605494,-0.448331200953813,-0.440994047856292,-0.429886085925357,
-0.398368874800689,-0.358761651094981,-0.352086110115651,-0.348323877618132,
-0.344020907956559,-0.336686766343578,-0.312203528815908,-0.264752030232991,
-0.25460260043251,-0.247499144062276,-0.239949846260566,-0.227681159287737,
-0.212344962657144,-0.167646029963723,-0.155815887049593,-0.150575733395198,
-0.146579338644274,-0.141429728618438,-0.129319280740467,-0.109510257460682,
-0.0659694565309138,-0.0553200026572353,-0.0481352911225703,-0.0407159436544367,
-0.0331545468549584,-0.0213394885155918,-0.000593737719980223),
 .UNSPECIFIED.);
#134=B_SPLINE_CURVE_WITH_KNOTS('',3,(#9952,#9953,#9954,#9955,#9956,#9957,
#9958,#9959,#9960,#9961,#9962,#9963,#9964,#9965,#9966,#9967),
 .UNSPECIFIED.,.F.,.F.,(4,2,2,2,2,2,2,4),(-2.51321608836282,-2.47261480947244,
-2.46539989016161,-2.46112157445569,-2.4573432595597,-2.45057262653564,
-2.41186419033852,-2.39712982154602),.UNSPECIFIED.);
#135=B_SPLINE_CURVE_WITH_KNOTS('',3,(#9969,#9970,#9971,#9972,#9973,#9974,
#9975,#9976,#9977,#9978,#9979,#9980,#9981,#9982,#9983,#9984,#9985,#9986),
 .UNSPECIFIED.,.F.,.F.,(4,2,2,2,2,2,2,2,4),(-0.116908344231473,-0.107697949475263,
-0.0973491581199381,-0.0902159090932756,-0.0827264498688542,-0.0707726724833073,
-0.031819298716922,-0.00902562018967192,-0.000594336423203717),
 .UNSPECIFIED.);
#136=B_SPLINE_CURVE_WITH_KNOTS('',3,(#9987,#9988,#9989,#9990,#9991,#9992,
#9993,#9994,#9995,#9996,#9997,#9998,#9999,#10000,#10001,#10002,#10003,#10004,
#10005,#10006,#10007,#10008,#10009,#10010,#10011,#10012,#10013,#10014,#10015,
#10016,#10017,#10018,#10019,#10020,#10021,#10022,#10023,#10024,#10025,#10026,
#10027,#10028,#10029,#10030,#10031,#10032,#10033,#10034,#10035,#10036,#10037,
#10038,#10039,#10040,#10041,#10042,#10043,#10044,#10045,#10046,#10047,#10048,
#10049,#10050,#10051,#10052,#10053,#10054,#10055,#10056,#10057,#10058,#10059,
#10060,#10061,#10062,#10063,#10064,#10065,#10066,#10067,#10068,#10069,#10070,
#10071,#10072,#10073,#10074,#10075,#10076,#10077,#10078,#10079,#10080,#10081,
#10082,#10083,#10084,#10085,#10086,#10087,#10088,#10089,#10090,#10091,#10092,
#10093,#10094,#10095,#10096,#10097,#10098,#10099,#10100,#10101,#10102,#10103,
#10104,#10105,#10106,#10107,#10108,#10109,#10110,#10111,#10112,#10113,#10114,
#10115,#10116,#10117,#10118,#10119,#10120,#10121,#10122,#10123,#10124,#10125,
#10126,#10127,#10128,#10129,#10130,#10131,#10132,#10133,#10134,#10135,#10136,
#10137,#10138,#10139,#10140,#10141,#10142),.UNSPECIFIED.,.F.,.F.,(4,2,2,
2,2,2,2,2,2,2,2,2,2,2,2,2,2,2,2,2,2,2,2,2,2,2,2,2,2,2,2,2,2,2,2,2,2,2,2,
2,2,2,2,2,2,2,2,2,2,2,2,2,2,2,2,2,2,2,2,2,2,2,2,2,2,2,2,2,2,2,2,2,2,2,2,
2,2,4),(-2.5139771603986,-2.50974231440594,-2.50550766132944,-2.50154507535624,
-2.4957462142949,-2.47922982302599,-2.46210389994978,-2.4378966219083,-2.41752514377281,
-2.40866940415638,-2.40165396777123,-2.39347579910472,-2.37816882780702,
-2.33145804647038,-2.31893107799337,-2.30996346440651,-2.30534090013258,
-2.30130241623188,-2.29516578641853,-2.27612107492151,-2.2386601327274,
-2.22426612998011,-2.21253617441478,-2.20508777725738,-2.19792771607934,
-2.18741623335324,-2.14255199934756,-2.12338213763505,-2.1115128093502,
-2.10639998108809,-2.10240348350174,-2.09712692763231,-2.08506222428278,
-2.04066251390605,-2.02536444500856,-2.01311691278679,-2.00557293655083,
-1.99846970636383,-1.98831251685999,-1.94088154276745,-1.91635867308484,
-1.9090202716227,-1.90471717167386,-1.90095686331538,-1.89428889175171,
-1.85465251314199,-1.82317896996235,-1.81207813779998,-1.80474346917739,
-1.79740212821455,-1.78626414060057,-1.7476352919286,-1.72518328287483,
-1.71608359358885,-1.70895139795921,-1.70469012944518,-1.70090018578456,
-1.69406109583143,-1.65595905273851,-1.62353671474701,-1.61231531633278,
-1.60495913940849,-1.59763900645014,-1.58661967163277,-1.55799067849915,
-1.51927059611237,-1.51035098109844,-1.50573702499238,-1.50169468115358,
-1.49553567122442,-1.4746620051643,-1.43859743071974,-1.42442109879224,
-1.41281752020196,-1.40539154504965,-1.39821395422413,-1.38760175305837,
-1.37383024056511),.UNSPECIFIED.);
#137=B_SPLINE_CURVE_WITH_KNOTS('',3,(#10147,#10148,#10149,#10150,#10151,
#10152,#10153,#10154,#10155,#10156,#10157,#10158,#10159,#10160,#10161,#10162,
#10163,#10164,#10165,#10166,#10167,#10168,#10169,#10170,#10171,#10172,#10173,
#10174,#10175,#10176,#10177,#10178,#10179,#10180,#10181,#10182,#10183,#10184,
#10185,#10186,#10187,#10188,#10189,#10190,#10191,#10192,#10193,#10194,#10195,
#10196,#10197,#10198,#10199,#10200,#10201,#10202,#10203,#10204,#10205,#10206,
#10207,#10208,#10209,#10210,#10211,#10212,#10213,#10214,#10215,#10216,#10217,
#10218,#10219,#10220,#10221,#10222,#10223,#10224,#10225,#10226,#10227,#10228,
#10229,#10230,#10231,#10232,#10233,#10234,#10235,#10236,#10237,#10238,#10239,
#10240,#10241,#10242,#10243,#10244,#10245,#10246,#10247,#10248,#10249,#10250,
#10251,#10252,#10253,#10254,#10255,#10256,#10257,#10258,#10259,#10260,#10261,
#10262,#10263,#10264,#10265,#10266,#10267,#10268,#10269,#10270,#10271,#10272,
#10273,#10274,#10275,#10276,#10277,#10278,#10279,#10280,#10281,#10282,#10283,
#10284,#10285,#10286,#10287,#10288,#10289,#10290,#10291,#10292,#10293,#10294,
#10295,#10296,#10297,#10298,#10299,#10300,#10301,#10302,#10303,#10304,#10305,
#10306,#10307,#10308,#10309,#10310,#10311,#10312,#10313,#10314,#10315,#10316),
 .UNSPECIFIED.,.F.,.F.,(4,2,2,2,2,2,2,2,2,2,2,2,2,2,2,2,2,2,2,2,2,2,2,2,
2,2,2,2,2,2,2,2,2,2,2,2,2,2,2,2,2,2,2,2,2,2,2,2,2,2,2,2,2,2,2,2,2,2,2,2,
2,2,2,2,2,2,2,2,2,2,2,2,2,2,2,2,2,2,2,2,2,2,2,2,4),(-2.39716550844473,-2.38235738603314,
-2.35842144763977,-2.35115384039938,-2.34686562342799,-2.34309596376143,
-2.33637218037512,-2.29726343256587,-2.26548629893112,-2.25434752545061,
-2.24700638275891,-2.23967212728965,-2.22857211700272,-2.1893637225085,
-2.16728042196396,-2.15826235349736,-2.15117742777478,-2.14692578197953,
-2.14258647615187,-2.13506865455545,-2.1072780138158,-2.07799254417099,
-2.0595097647271,-2.05091277446615,-2.04390797212759,-2.03551737455716,
-2.01840446400436,-1.97387414855571,-1.96154105035962,-1.95267052327612,
-1.94806600128552,-1.94402035125614,-1.93783907130222,-1.91655293707972,
-1.88084868021968,-1.86673290115953,-1.85516521884818,-1.84774611346243,
-1.84056401947354,-1.8299232640557,-1.78607780077785,-1.75949692691008,
-1.75192595740346,-1.74757557620068,-1.74333243335886,-1.73629206997448,
-1.70005579598112,-1.66790033187141,-1.65580608857251,-1.6482898184602,
-1.64117000733272,-1.6309117220091,-1.58420419681792,-1.55928860303882,
-1.55190419999156,-1.54759141965172,-1.54383639354996,-1.53720131043032,
-1.49728191798483,-1.46599148056203,-1.45491417802411,-1.44758305789801,
-1.44023613280808,-1.42907052557603,-1.39104762333584,-1.3682266188749,
-1.35904734943522,-1.35186941780441,-1.3475986186538,-1.34327910839688,
-1.33586165488846,-1.31086987103338,-1.28838349155678,-1.27076716258182,
-1.25726023587208,-1.24948334515615,-1.2423928378255,-1.23281805248766,
-1.20541977550243,-1.18421102044453,-1.15964926327666,-1.15224172666494,
-1.14792424228513,-1.14365142107152,-1.14097344694939),.UNSPECIFIED.);
#138=B_SPLINE_CURVE_WITH_KNOTS('',3,(#10317,#10318,#10319,#10320,#10321,
#10322,#10323,#10324,#10325,#10326,#10327,#10328,#10329,#10330,#10331,#10332,
#10333,#10334,#10335,#10336,#10337,#10338,#10339,#10340,#10341,#10342,#10343,
#10344,#10345,#10346,#10347,#10348,#10349,#10350,#10351,#10352,#10353,#10354,
#10355,#10356,#10357,#10358,#10359,#10360,#10361,#10362,#10363,#10364,#10365,
#10366,#10367,#10368,#10369,#10370,#10371,#10372,#10373,#10374,#10375,#10376,
#10377,#10378,#10379,#10380,#10381,#10382,#10383,#10384,#10385,#10386,#10387,
#10388,#10389,#10390,#10391,#10392,#10393,#10394,#10395,#10396,#10397,#10398,
#10399,#10400,#10401,#10402,#10403,#10404,#10405,#10406,#10407,#10408,#10409,
#10410,#10411,#10412,#10413,#10414,#10415,#10416,#10417,#10418,#10419,#10420,
#10421,#10422,#10423,#10424,#10425,#10426,#10427,#10428,#10429,#10430,#10431,
#10432,#10433,#10434,#10435,#10436,#10437,#10438,#10439,#10440,#10441,#10442,
#10443,#10444,#10445,#10446,#10447,#10448,#10449,#10450,#10451,#10452,#10453,
#10454,#10455,#10456,#10457,#10458,#10459,#10460,#10461,#10462,#10463,#10464,
#10465,#10466,#10467,#10468,#10469,#10470),.UNSPECIFIED.,.F.,.F.,(4,2,2,
2,2,2,2,2,2,2,2,2,2,2,2,2,2,2,2,2,2,2,2,2,2,2,2,2,2,2,2,2,2,2,2,2,2,2,2,
2,2,2,2,2,2,2,2,2,2,2,2,2,2,2,2,2,2,2,2,2,2,2,2,2,2,2,2,2,2,2,2,2,2,2,2,
2,4),(-1.37383024056511,-1.34349731540928,-1.31705490309835,-1.30949832522974,
-1.30515066541329,-1.30090502287577,-1.29385286769016,-1.25770689987854,
-1.22362942230147,-1.21245255606101,-1.20510365224169,-1.19777464244973,
-1.18670939150684,-1.15552063823869,-1.1153573229877,-1.10874342925435,
-1.10499193043474,-1.1006734934197,-1.0932619850194,-1.0681130421046,-1.02183621388935,
-1.01151920481442,-1.00438987030478,-0.996889617840733,-0.984883613661946,
-0.950076256323802,-0.916575705536087,-0.909357259131994,-0.905078194646556,
-0.900767563171138,-0.89339419901032,-0.868574597606939,-0.821713846778265,
-0.811479042593566,-0.804362906709166,-0.796840019979762,-0.784710873386791,
-0.75052981776179,-0.716604504437372,-0.709406180853282,-0.705131254463527,
-0.700816455480394,-0.693422243709192,-0.668421793835061,-0.621885837497626,
-0.611605740278395,-0.604482552356341,-0.596972639663292,-0.584913027143422,
-0.552379595811848,-0.5164487560532,-0.509371911653121,-0.505121479831962,
-0.500779692074401,-0.493252029552087,-0.467068232997983,-0.422580701263669,
-0.412023526501566,-0.40485525773917,-0.397416579128286,-0.385743377964248,
-0.371446062606456,-0.334640239415005,-0.331167944570213,-0.314092075074438,
-0.308223006489398,-0.304182164814755,-0.299410325417555,-0.289625381471665,
-0.275402922450765,-0.226794148326838,-0.214175233539595,-0.206562449046453,
-0.199412490105201,-0.189412365137428,-0.153042973105517,-0.117060520499069),
 .UNSPECIFIED.);
#139=B_SPLINE_CURVE_WITH_KNOTS('',3,(#10476,#10477,#10478,#10479,#10480,
#10481,#10482,#10483,#10484,#10485,#10486,#10487,#10488,#10489,#10490,#10491,
#10492,#10493,#10494,#10495,#10496,#10497,#10498,#10499,#10500,#10501,#10502,
#10503,#10504,#10505,#10506,#10507,#10508,#10509,#10510,#10511,#10512,#10513,
#10514,#10515,#10516,#10517,#10518,#10519,#10520,#10521,#10522,#10523,#10524,
#10525,#10526,#10527,#10528,#10529,#10530,#10531,#10532,#10533,#10534,#10535,
#10536,#10537,#10538,#10539,#10540,#10541,#10542,#10543,#10544,#10545,#10546,
#10547,#10548,#10549,#10550,#10551,#10552,#10553,#10554,#10555,#10556,#10557,
#10558,#10559,#10560,#10561,#10562,#10563,#10564,#10565,#10566,#10567,#10568,
#10569,#10570,#10571,#10572,#10573,#10574,#10575,#10576,#10577,#10578,#10579,
#10580,#10581,#10582,#10583,#10584,#10585,#10586,#10587,#10588,#10589,#10590,
#10591,#10592,#10593,#10594,#10595,#10596,#10597,#10598,#10599,#10600,#10601,
#10602,#10603,#10604,#10605,#10606,#10607,#10608,#10609,#10610,#10611,#10612,
#10613,#10614,#10615,#10616,#10617,#10618,#10619,#10620,#10621,#10622,#10623,
#10624,#10625),.UNSPECIFIED.,.F.,.F.,(4,2,2,2,2,2,2,2,2,2,2,2,2,2,2,2,2,
2,2,2,2,2,2,2,2,2,2,2,2,2,2,2,2,2,2,2,2,2,2,2,2,2,2,2,2,2,2,2,2,2,2,2,2,
2,2,2,2,2,2,2,2,2,2,2,2,2,2,2,2,2,2,2,2,2,4),(-1.14066834730415,-1.13528708228451,
-1.12825874370977,-1.11908952757347,-1.09679743353057,-1.09405211095703,
-1.05799686607207,-1.04142723336169,-1.03574582603282,-1.03173946765447,
-1.02688599334257,-1.0166347101821,-1.0013895134999,-0.949578516067516,
-0.939351418593466,-0.932227839927205,-0.924684865519697,-0.91248856322471,
-0.88103571118122,-0.84434028124934,-0.837351590564754,-0.833111747206177,
-0.82873653939268,-0.82105720118224,-0.810989956120682,-0.783660025081896,
-0.751928535848876,-0.740804028318319,-0.733461603689559,-0.726117783786739,
-0.714985993738198,-0.68330721460369,-0.643929042402749,-0.637224870169614,
-0.633457623199097,-0.629164660474318,-0.621871921607312,-0.597722363135909,
-0.549663362388753,-0.539605197993634,-0.532448911988693,-0.524860290457296,
-0.51236008205074,-0.482998575266667,-0.444104625300159,-0.437349581753881,
-0.433575455096387,-0.429294418534457,-0.422067567339357,-0.391068271416759,
-0.352049912296781,-0.340936279149132,-0.333597222338206,-0.326254155837573,
-0.315118121898445,-0.283383210420531,-0.244161853391143,-0.237444692321296,
-0.233674632362936,-0.229381206936217,-0.222094795011784,-0.198014624474899,
-0.149831759319823,-0.139788442362888,-0.132630526681158,-0.125029029589257,
-0.112478218150378,-0.0827830876071397,-0.0450813175921124,-0.0379343399491491,
-0.0336695761806261,-0.0293431468026109,-0.0247229939503656,-0.0162435752141435,
-0.000615599677778074),.UNSPECIFIED.);
#140=B_SPLINE_CURVE_WITH_KNOTS('',3,(#10626,#10627,#10628,#10629,#10630,
#10631,#10632,#10633,#10634,#10635,#10636,#10637,#10638,#10639),
 .UNSPECIFIED.,.F.,.F.,(4,2,2,2,2,2,4),(-2.51359551756059,-2.46820697681293,
-2.45559533539021,-2.44798484919415,-2.44083562026429,-2.43083389655103,
-2.39716550844473),.UNSPECIFIED.);
#141=B_SPLINE_CURVE_WITH_KNOTS('',3,(#10641,#10642,#10643,#10644,#10645,
#10646,#10647,#10648,#10649,#10650,#10651,#10652,#10653,#10654,#10655,#10656,
#10657,#10658,#10659,#10660,#10661,#10662),.UNSPECIFIED.,.F.,.F.,(4,2,2,
2,2,2,2,2,2,2,4),(-0.117060520499069,-0.116506876729,-0.109491812339823,
-0.105253945341782,-0.100898190861845,-0.0932999678296215,-0.0664641804689692,
-0.0235325687190956,-0.0128214917675811,-0.0060588672363243,-0.000775673896845518),
 .UNSPECIFIED.);
#142=B_SPLINE_CURVE_WITH_KNOTS('',3,(#10663,#10664,#10665,#10666,#10667,
#10668,#10669,#10670,#10671,#10672,#10673,#10674,#10675,#10676,#10677,#10678,
#10679,#10680,#10681,#10682,#10683,#10684,#10685,#10686,#10687,#10688,#10689,
#10690,#10691,#10692,#10693,#10694,#10695,#10696,#10697,#10698,#10699,#10700,
#10701,#10702,#10703,#10704,#10705,#10706,#10707,#10708,#10709,#10710,#10711,
#10712,#10713,#10714,#10715,#10716,#10717,#10718,#10719,#10720,#10721,#10722,
#10723,#10724,#10725,#10726,#10727,#10728,#10729,#10730,#10731,#10732,#10733,
#10734,#10735,#10736,#10737,#10738,#10739,#10740,#10741,#10742,#10743,#10744,
#10745,#10746,#10747,#10748,#10749,#10750,#10751,#10752,#10753,#10754,#10755,
#10756,#10757,#10758,#10759,#10760,#10761,#10762,#10763,#10764,#10765,#10766,
#10767,#10768,#10769,#10770,#10771,#10772,#10773,#10774,#10775,#10776,#10777,
#10778,#10779,#10780,#10781,#10782,#10783,#10784,#10785,#10786,#10787,#10788,
#10789,#10790,#10791,#10792,#10793,#10794,#10795,#10796,#10797,#10798,#10799,
#10800,#10801,#10802,#10803,#10804,#10805,#10806),.UNSPECIFIED.,.F.,.F.,
(4,2,2,2,2,2,2,2,2,2,2,2,2,2,2,2,2,2,2,2,2,2,2,2,2,2,2,2,2,2,2,2,2,2,2,
2,2,2,2,2,2,2,2,2,2,2,2,2,2,2,2,2,2,2,2,2,2,2,2,2,2,2,2,2,2,2,2,2,2,2,2,
4),(1.14091205305926,1.14098686325601,1.17506124787357,1.18225125030916,
1.1865219920022,1.19083569419543,1.19822744595321,1.22321132728064,1.26980756717636,
1.28008286646988,1.28720518188926,1.29471630830586,1.3067839074636,1.34126970256588,
1.37489612603386,1.38210092847233,1.38637731973488,1.39069033933279,1.39807859739005,
1.42303310353215,1.4696683584786,1.47993497352466,1.48705464895511,1.49456566669604,
1.50663882495049,1.55441262806513,1.57671672803689,1.58293925919969,1.5869907888506,
1.5915763000801,1.60034992138208,1.6412109396252,1.67071307969318,1.68048126427172,
1.68759530647032,1.69528728204652,1.7083442745729,1.73218070338743,1.77488913957184,
1.7819634457011,1.78621221562835,1.79055226759289,1.79807644166995,1.8242397694806,
1.86877672233358,1.87932730827248,1.88649268517233,1.89392955546362,1.90560296526389,
1.91990111702837,1.95675405061808,1.97666366136682,1.9827628448936,1.98683495498047,
1.99149048806365,2.00063899654464,2.01353302438057,2.06503962186941,2.07735690524454,
2.08491173590531,2.09208562825065,2.10225501861761,2.13942737719031,2.17443185793313,
2.18157681844205,2.18583946049176,2.1901625562319,2.19760569236046,2.22305268192794,
2.26771687382351,2.27548794694238,2.28095113544787),.UNSPECIFIED.);
#143=B_SPLINE_CURVE_WITH_KNOTS('',3,(#10810,#10811,#10812,#10813,#10814,
#10815,#10816,#10817,#10818,#10819,#10820,#10821,#10822,#10823,#10824,#10825,
#10826,#10827,#10828,#10829,#10830,#10831,#10832,#10833,#10834,#10835,#10836,
#10837,#10838,#10839,#10840,#10841,#10842,#10843,#10844,#10845,#10846,#10847,
#10848,#10849,#10850,#10851,#10852,#10853,#10854,#10855,#10856,#10857,#10858,
#10859,#10860,#10861,#10862,#10863,#10864,#10865,#10866,#10867,#10868,#10869,
#10870,#10871,#10872,#10873),.UNSPECIFIED.,.F.,.F.,(4,3,3,3,3,3,3,3,3,3,
3,3,3,3,3,3,3,3,3,3,3,4),(-4.09157007060721,-3.99819923940857,-3.89835156497246,
-3.79864772858848,-3.69864794120947,-3.5991264524945,-3.4996392348841,-3.40015603967125,
-3.29977938714255,-3.20015661005484,-3.09940301980564,-2.99864942955643,
-2.89996225994261,-2.80141569488778,-2.70297985623509,-2.60460299513241,
-2.50625345286672,-2.40789960785008,-2.30944973523756,-2.2109455342352,
-2.11228415465847,-2.06679336762492),.UNSPECIFIED.);
#144=B_SPLINE_CURVE_WITH_KNOTS('',3,(#10877,#10878,#10879,#10880,#10881),
 .UNSPECIFIED.,.F.,.F.,(4,1,4),(0.,0.999549809852145,1.11662023360648),
 .UNSPECIFIED.);
#145=B_SPLINE_CURVE_WITH_KNOTS('',3,(#10883,#10884,#10885,#10886,#10887,
#10888,#10889,#10890,#10891,#10892,#10893,#10894,#10895,#10896,#10897,#10898,
#10899,#10900,#10901,#10902,#10903,#10904,#10905,#10906,#10907,#10908,#10909,
#10910,#10911,#10912,#10913,#10914,#10915,#10916,#10917,#10918,#10919,#10920,
#10921,#10922,#10923,#10924,#10925,#10926,#10927,#10928,#10929,#10930,#10931,
#10932,#10933,#10934,#10935,#10936,#10937,#10938,#10939,#10940,#10941,#10942,
#10943,#10944,#10945,#10946,#10947,#10948,#10949,#10950,#10951,#10952,#10953,
#10954,#10955,#10956,#10957,#10958,#10959,#10960,#10961,#10962,#10963,#10964,
#10965,#10966,#10967,#10968,#10969,#10970,#10971,#10972,#10973,#10974,#10975,
#10976,#10977,#10978,#10979,#10980,#10981,#10982,#10983,#10984,#10985,#10986,
#10987,#10988,#10989,#10990,#10991,#10992,#10993,#10994,#10995,#10996,#10997,
#10998,#10999,#11000,#11001,#11002,#11003,#11004,#11005,#11006,#11007,#11008,
#11009,#11010,#11011,#11012,#11013,#11014,#11015,#11016,#11017,#11018,#11019,
#11020,#11021,#11022,#11023,#11024,#11025,#11026,#11027,#11028,#11029,#11030,
#11031,#11032,#11033,#11034,#11035,#11036,#11037,#11038,#11039,#11040,#11041,
#11042,#11043,#11044,#11045,#11046,#11047,#11048,#11049,#11050,#11051,#11052,
#11053,#11054,#11055,#11056,#11057,#11058,#11059,#11060,#11061,#11062,#11063,
#11064,#11065,#11066,#11067,#11068,#11069,#11070,#11071,#11072),
 .UNSPECIFIED.,.F.,.F.,(4,3,3,3,3,3,3,3,3,3,3,3,3,3,3,3,3,3,3,3,3,3,3,3,
3,3,3,3,3,3,3,3,3,3,3,3,3,3,3,3,3,3,3,3,3,3,3,3,3,3,3,3,3,3,3,3,3,3,3,3,
3,3,3,4),(1.11662023360648,1.21415700903785,1.31227483537115,1.40958631975065,
1.50685024378918,1.60409914654667,1.70284926483607,1.8002232178696,1.89966141878694,
1.99909961970429,2.0988159569863,2.19838757899243,2.29842031031293,2.39780836260854,
2.49716197145402,2.59651155591453,2.697046024325,2.79653649081236,2.8975929601844,
2.99864942955643,3.09848076178733,3.19817176264502,3.29817519724046,3.39769245810353,
3.49717869068034,3.59666414129913,3.69704791582649,3.79668086896899,3.89744005418878,
3.99819923940857,4.09777814999803,4.19721232014855,4.29727941128758,4.39653099436606,
4.49574881322469,4.59496347522391,4.69565986873311,4.79501895395638,4.89638400160855,
4.99774904926072,5.09743314979569,5.19697375033416,5.2970143889315,5.39637464816663,
5.49570174804806,5.59502615055517,5.69559432769459,5.79506317005562,5.89618101458424,
5.99729885911286,6.09698793002092,6.19653388796859,6.29657323559314,6.3959397624514,
6.49527345959839,6.59460478137224,6.69516575327043,6.79464224294108,6.89574545595304,
6.99684866896501,7.1073445025526,7.21750034428983,7.32707552235099,7.39980554057894),
 .UNSPECIFIED.);
#146=B_SPLINE_CURVE_WITH_KNOTS('',3,(#11074,#11075,#11076,#11077,#11078,
#11079,#11080,#11081,#11082,#11083,#11084,#11085,#11086,#11087,#11088,#11089,
#11090,#11091,#11092,#11093,#11094,#11095,#11096,#11097,#11098,#11099,#11100,
#11101,#11102,#11103,#11104,#11105,#11106,#11107,#11108,#11109,#11110,#11111,
#11112,#11113,#11114,#11115,#11116,#11117,#11118,#11119,#11120,#11121,#11122,
#11123,#11124,#11125,#11126,#11127,#11128,#11129,#11130,#11131,#11132,#11133,
#11134,#11135,#11136,#11137,#11138,#11139,#11140,#11141,#11142,#11143,#11144,
#11145,#11146,#11147,#11148,#11149,#11150,#11151,#11152,#11153,#11154,#11155,
#11156,#11157,#11158,#11159,#11160,#11161,#11162,#11163,#11164,#11165,#11166,
#11167,#11168,#11169,#11170,#11171,#11172,#11173,#11174,#11175,#11176,#11177,
#11178,#11179,#11180,#11181,#11182,#11183,#11184,#11185,#11186,#11187,#11188,
#11189,#11190,#11191,#11192,#11193,#11194,#11195,#11196,#11197,#11198,#11199,
#11200,#11201,#11202,#11203,#11204,#11205,#11206,#11207,#11208,#11209,#11210,
#11211,#11212,#11213,#11214,#11215,#11216,#11217,#11218,#11219,#11220,#11221,
#11222,#11223,#11224,#11225,#11226,#11227,#11228,#11229,#11230,#11231,#11232,
#11233,#11234,#11235,#11236,#11237,#11238,#11239,#11240,#11241,#11242,#11243,
#11244,#11245,#11246,#11247,#11248,#11249,#11250,#11251,#11252,#11253,#11254,
#11255,#11256,#11257,#11258,#11259,#11260,#11261,#11262,#11263),
 .UNSPECIFIED.,.F.,.F.,(4,3,3,3,3,3,3,3,3,3,3,3,3,3,3,3,3,3,3,3,3,3,3,3,
3,3,3,3,3,3,3,3,3,3,3,3,3,3,3,3,3,3,3,3,3,3,3,3,3,3,3,3,3,3,3,3,3,3,3,3,
3,3,3,4),(7.39980554078607,7.50053108874774,7.60129313193771,7.7022021005082,
7.80318522932661,7.90438016308932,7.99639847881715,8.09607318258208,8.19560444098551,
8.29564742194599,8.39499854501913,8.49431660729804,8.59363208364627,8.69421113490202,
8.79367142016632,8.8948098544178,8.99594828866929,9.09562248122942,9.19515325722896,
9.29519636239052,9.39454707756092,9.49386476100677,9.59317988824142,9.69375944081142,
9.79321945438592,9.89435877645368,9.99549809852144,10.0951692453042,10.1946969174379,
10.2947407913049,10.3940882835689,10.4934027064381,10.5927145397381,10.693297881897,
10.7927545527067,10.8939012305401,10.9950479083736,11.0947207974823,11.1942502358541,
11.2942936711506,11.3936429749175,11.492959222287,11.5922728906363,11.6928540975337,
11.792312610642,11.8934551644338,11.9945977182257,12.0942704170841,12.1937996665268,
12.2938431492207,12.393192268754,12.4925083340807,12.5918218228387,12.6924032491485,
12.7918615906077,12.8930045593428,12.9941475280779,13.0933718526145,13.192459812771,
13.2914426505252,13.3903625391045,13.4892414456069,13.5881552424106,13.6829908479657),
 .UNSPECIFIED.);
#147=B_SPLINE_CURVE_WITH_KNOTS('',3,(#11265,#11266,#11267,#11268,#11269,
#11270,#11271,#11272,#11273,#11274,#11275,#11276,#11277,#11278,#11279,#11280,
#11281,#11282,#11283,#11284,#11285,#11286,#11287,#11288,#11289,#11290,#11291,
#11292,#11293,#11294,#11295,#11296,#11297,#11298,#11299,#11300,#11301,#11302,
#11303,#11304,#11305,#11306,#11307,#11308,#11309,#11310,#11311,#11312,#11313,
#11314,#11315,#11316,#11317,#11318,#11319,#11320,#11321,#11322,#11323,#11324,
#11325,#11326,#11327,#11328,#11329,#11330,#11331,#11332,#11333,#11334,#11335,
#11336,#11337,#11338,#11339,#11340,#11341,#11342,#11343,#11344,#11345,#11346,
#11347,#11348,#11349,#11350,#11351,#11352,#11353,#11354,#11355,#11356,#11357,
#11358,#11359,#11360,#11361,#11362,#11363,#11364,#11365,#11366,#11367,#11368,
#11369,#11370,#11371,#11372,#11373,#11374,#11375,#11376,#11377,#11378,#11379,
#11380,#11381,#11382,#11383,#11384,#11385,#11386,#11387,#11388,#11389,#11390,
#11391,#11392,#11393,#11394,#11395,#11396,#11397,#11398,#11399,#11400,#11401,
#11402,#11403,#11404,#11405,#11406,#11407,#11408,#11409,#11410,#11411,#11412,
#11413,#11414,#11415,#11416,#11417,#11418,#11419,#11420,#11421,#11422,#11423,
#11424,#11425,#11426,#11427,#11428,#11429,#11430,#11431,#11432,#11433,#11434,
#11435,#11436,#11437,#11438,#11439,#11440,#11441,#11442,#11443,#11444,#11445,
#11446,#11447,#11448,#11449,#11450,#11451,#11452,#11453,#11454),
 .UNSPECIFIED.,.F.,.F.,(4,3,3,3,3,3,3,3,3,3,3,3,3,3,3,3,3,3,3,3,3,3,3,3,
3,3,3,3,3,3,3,3,3,3,3,3,3,3,3,3,3,3,3,3,3,3,3,3,3,3,3,3,3,3,3,3,3,3,3,3,
3,3,3,4),(13.6829908483355,13.8012987037146,13.9211119521594,13.99369733793,
14.093369932917,14.1928990751328,14.292942584214,14.392291589093,14.4916075372192,
14.5909209063797,14.6915024667303,14.7909606838751,14.8921039158287,14.9932471477822,
15.0929197052539,15.1924488098593,15.2924923283312,15.3918412956528,15.4911572063268,
15.5904705381924,15.6910521430529,15.7905103236783,15.8916536406563,15.9927969576343,
16.0924694828721,16.1919985545393,16.2920420811577,16.3913910140619,16.4907068898376,
16.5900201863698,16.690601831649,16.7900599762254,16.8912033718559,16.9923467674864,
17.0920193189202,17.1915484171806,17.2915919372004,17.3909408974713,17.4902568008438,
17.5895701251662,17.6901517382093,17.7896099107689,17.8907532440537,17.9918965773386,
18.0915691226361,18.1910982147193,18.2911417362782,18.3904906903181,18.4898065874535,
18.5891199055412,18.6897015259535,18.7891596923486,18.8903030397697,18.9914463871907,
19.0907047944209,19.1898201075523,19.2888206743773,19.3877588790043,19.4866657728217,
19.5855723677555,19.6845767311066,19.7836300076881,19.8828580081811,19.9661761547613),
 .UNSPECIFIED.);
#148=B_SPLINE_CURVE_WITH_KNOTS('',3,(#11456,#11457,#11458,#11459,#11460,
#11461,#11462,#11463,#11464,#11465,#11466,#11467,#11468,#11469,#11470,#11471,
#11472,#11473,#11474,#11475,#11476,#11477,#11478,#11479,#11480,#11481,#11482,
#11483,#11484,#11485,#11486,#11487,#11488,#11489,#11490,#11491,#11492,#11493,
#11494,#11495,#11496,#11497,#11498,#11499,#11500,#11501,#11502,#11503,#11504,
#11505,#11506,#11507,#11508,#11509,#11510,#11511,#11512,#11513,#11514,#11515,
#11516,#11517,#11518,#11519,#11520,#11521,#11522,#11523,#11524,#11525,#11526,
#11527,#11528,#11529,#11530,#11531,#11532,#11533,#11534,#11535,#11536,#11537,
#11538,#11539,#11540,#11541,#11542,#11543,#11544,#11545,#11546,#11547,#11548,
#11549,#11550,#11551,#11552,#11553,#11554,#11555,#11556,#11557,#11558,#11559,
#11560,#11561,#11562,#11563,#11564,#11565,#11566,#11567,#11568,#11569,#11570,
#11571,#11572,#11573,#11574,#11575,#11576,#11577,#11578,#11579,#11580,#11581,
#11582,#11583,#11584,#11585,#11586,#11587,#11588,#11589,#11590,#11591,#11592,
#11593,#11594,#11595,#11596,#11597,#11598,#11599,#11600,#11601,#11602,#11603,
#11604,#11605,#11606,#11607,#11608,#11609,#11610,#11611,#11612,#11613,#11614,
#11615,#11616,#11617,#11618,#11619,#11620,#11621,#11622,#11623,#11624,#11625,
#11626,#11627,#11628,#11629,#11630,#11631,#11632,#11633,#11634,#11635,#11636,
#11637,#11638,#11639,#11640,#11641,#11642,#11643,#11644,#11645),
 .UNSPECIFIED.,.F.,.F.,(4,3,3,3,3,3,3,3,3,3,3,3,3,3,3,3,3,3,3,3,3,3,3,3,
3,3,3,3,3,3,3,3,3,3,3,3,3,3,3,3,3,3,3,3,3,3,3,3,3,3,3,3,3,3,3,3,3,3,3,3,
3,3,3,4),(19.9661761551452,19.9909961970429,20.0906687423831,20.1901978344841,
20.2902413560355,20.3895903100322,20.4889062071013,20.5882195250995,20.6888011455484,
20.7882593117979,20.8894026593464,20.990546006895,21.0902185513232,21.1897476425038,
21.2897911642842,21.3891401173469,21.4884560134792,21.5877693305389,21.688350952091,
21.7878091174074,21.8889524670773,21.9900958167472,22.0897683609266,22.189297451851,
22.2893409736946,22.3886899264848,22.4880058223391,22.5873191391156,22.6879007609866,
22.7873589260099,22.8885022763046,22.9896456265993,23.0893181710964,23.1888472623445,
23.2888907841079,23.3882397372341,23.4875556334283,23.5868689505481,23.6874505720239,
23.7869087373954,23.8880520869235,23.9891954364515,24.0888679808449,24.1883970719877,
24.2884405937772,24.3877895467945,24.4871054428787,24.5864187598876,24.6870003814916,
24.7864585467512,24.8876018965274,24.9887452463036,25.0884177908087,25.1879468820631,
25.2879904038247,25.387339356953,25.4866552531475,25.5859685702662,25.6865501917386,
25.7860083571051,25.8871517066304,25.9882950561557,26.1188282590924,26.2493614620292),
 .UNSPECIFIED.);
#149=B_SPLINE_CURVE_WITH_KNOTS('',3,(#11647,#11648,#11649,#11650,#11651,
#11652,#11653,#11654,#11655,#11656,#11657,#11658,#11659,#11660,#11661,#11662,
#11663,#11664,#11665,#11666,#11667,#11668,#11669,#11670,#11671,#11672,#11673,
#11674,#11675,#11676,#11677,#11678,#11679,#11680,#11681,#11682,#11683,#11684,
#11685,#11686,#11687,#11688,#11689,#11690,#11691,#11692,#11693,#11694,#11695,
#11696,#11697,#11698,#11699,#11700,#11701,#11702,#11703,#11704,#11705,#11706,
#11707,#11708,#11709,#11710,#11711,#11712,#11713,#11714,#11715,#11716,#11717,
#11718,#11719,#11720,#11721,#11722,#11723,#11724,#11725,#11726,#11727,#11728,
#11729,#11730,#11731,#11732,#11733,#11734,#11735,#11736,#11737,#11738,#11739,
#11740,#11741,#11742,#11743,#11744,#11745,#11746,#11747,#11748,#11749,#11750,
#11751,#11752,#11753,#11754,#11755,#11756,#11757,#11758,#11759,#11760,#11761,
#11762,#11763,#11764,#11765,#11766,#11767,#11768,#11769,#11770,#11771,#11772,
#11773,#11774,#11775,#11776,#11777,#11778,#11779,#11780,#11781,#11782,#11783,
#11784,#11785,#11786,#11787,#11788,#11789,#11790,#11791,#11792,#11793,#11794,
#11795,#11796,#11797,#11798,#11799,#11800,#11801,#11802,#11803,#11804,#11805,
#11806,#11807,#11808,#11809,#11810,#11811,#11812,#11813,#11814,#11815,#11816,
#11817,#11818,#11819,#11820,#11821,#11822,#11823,#11824,#11825,#11826,#11827,
#11828,#11829,#11830,#11831,#11832,#11833,#11834,#11835,#11836,#11837,#11838,
#11839),.UNSPECIFIED.,.F.,.F.,(4,3,3,3,3,3,3,3,3,3,3,3,3,3,3,3,3,3,3,3,
3,3,3,3,3,3,3,3,3,3,3,3,3,3,3,3,3,3,3,3,3,3,3,3,3,3,3,3,3,3,3,3,3,3,3,3,
3,3,3,3,3,3,3,3,4),(26.2493614623248,26.3477156658028,26.4460142361312,
26.5442888935363,26.6425713247428,26.7409564245699,26.8393988921363,26.9380064119851,
26.9878448660079,27.0875174104623,27.1870465016636,27.2870900234381,27.3864389765076,
27.4857548726413,27.5850681896973,27.685649811238,27.7851079765379,27.8862513261989,
27.98739467586,28.0870672212339,28.1865963133616,28.2866398349054,28.3859887889108,
28.4853046859821,28.5846180039758,28.6851996244099,28.7846577906385,28.8858011381754,
28.9869444857122,29.0866170277615,29.1861461165615,29.2861896389368,29.3855385896319,
29.4848544834064,29.5841677981215,29.6847494224822,29.7842075855098,29.885350940537,
29.9864942955643,30.0861668411268,30.1856959334179,30.2857394549178,30.3850884090259,
30.4844043061771,30.583717624228,30.6842992445252,30.7837574107548,30.8849007580856,
30.9860441054165,31.085716657025,31.1852457554226,31.2852892754034,31.3846382357193,
31.4839541391023,31.5832674634001,31.6838490763672,31.7833072488177,31.8844505820432,
31.9855939152686,32.0884337774174,32.1910932256562,32.2935519798997,32.3958915779211,
32.4981122183601,32.5325467695044),.UNSPECIFIED.);
#150=B_SPLINE_CURVE_WITH_KNOTS('',3,(#11841,#11842,#11843,#11844,#11845,
#11846,#11847,#11848,#11849,#11850,#11851,#11852,#11853,#11854,#11855,#11856,
#11857,#11858,#11859,#11860,#11861,#11862,#11863,#11864,#11865,#11866,#11867,
#11868,#11869,#11870,#11871,#11872,#11873,#11874,#11875,#11876,#11877,#11878,
#11879,#11880,#11881,#11882,#11883,#11884,#11885,#11886,#11887,#11888,#11889,
#11890,#11891,#11892,#11893,#11894,#11895,#11896,#11897,#11898,#11899,#11900,
#11901,#11902,#11903,#11904,#11905,#11906,#11907,#11908,#11909,#11910,#11911,
#11912,#11913,#11914,#11915,#11916,#11917,#11918,#11919,#11920,#11921,#11922,
#11923,#11924,#11925,#11926,#11927,#11928,#11929,#11930,#11931,#11932,#11933,
#11934,#11935,#11936,#11937,#11938,#11939,#11940,#11941,#11942,#11943,#11944,
#11945,#11946,#11947,#11948,#11949,#11950,#11951,#11952,#11953,#11954,#11955,
#11956,#11957,#11958,#11959,#11960,#11961,#11962,#11963,#11964,#11965,#11966,
#11967,#11968,#11969,#11970,#11971,#11972,#11973,#11974,#11975,#11976,#11977,
#11978,#11979,#11980,#11981,#11982,#11983,#11984,#11985,#11986,#11987,#11988,
#11989,#11990,#11991,#11992,#11993,#11994,#11995,#11996,#11997,#11998,#11999,
#12000,#12001,#12002,#12003,#12004,#12005,#12006,#12007,#12008,#12009,#12010,
#12011,#12012,#12013,#12014,#12015,#12016,#12017,#12018,#12019,#12020,#12021,
#12022,#12023,#12024,#12025,#12026,#12027,#12028,#12029,#12030,#12031,#12032,
#12033),.UNSPECIFIED.,.F.,.F.,(4,3,3,3,3,3,3,3,3,3,3,3,3,3,3,3,3,3,3,3,
3,3,3,3,3,3,3,3,3,3,3,3,3,3,3,3,3,3,3,3,3,3,3,3,3,3,3,3,3,3,3,3,3,3,3,3,
3,3,3,3,3,3,3,3,4),(32.5325467697432,32.6388708786208,32.7456097074644,
32.8525716002337,32.9598580208814,32.9851437251207,33.0848162851276,33.1843453917237,
33.2843889096299,33.383737877605,33.4830537884294,33.5823671199426,33.6829487237002,
33.7824069027416,33.8835502188572,33.9846935349729,34.0843661305128,34.1838952731631,
34.2839387821208,34.3832877871423,34.4826037353011,34.5819171043847,34.6824986644947,
34.7819568812939,34.8831001130595,34.984243344825,35.0839157121467,35.1834446260861,
35.28348819216,35.3828369689343,35.4821526895209,35.5814658320094,35.6820476626763,
35.781505657582,35.8826494061296,35.9837931546772,36.0834658770091,36.1829951448861,
36.2830386223415,36.382387747926,36.4817038146451,36.5810173001397,36.6815987162371,
36.7810570430293,36.8822000037793,36.9833429645293,37.0830158504659,37.1825452863463,
37.2825887223507,37.3819380253,37.4812542724812,37.5805679412715,37.681149149549,
37.7806076646393,37.8817502195104,37.9828927743815,38.0810757587581,38.1790933410021,
38.277018137445,38.3748823697557,38.4727181782476,38.5706033625315,38.6685154729089,
38.7665475575039,38.8157320763496),.UNSPECIFIED.);
#151=B_SPLINE_CURVE_WITH_KNOTS('',3,(#12035,#12036,#12037,#12038,#12039,
#12040,#12041,#12042,#12043,#12044,#12045,#12046,#12047,#12048,#12049,#12050,
#12051,#12052,#12053,#12054,#12055,#12056,#12057,#12058,#12059,#12060,#12061,
#12062,#12063,#12064,#12065,#12066,#12067,#12068,#12069,#12070,#12071,#12072,
#12073,#12074,#12075,#12076,#12077,#12078,#12079,#12080,#12081,#12082,#12083,
#12084,#12085,#12086,#12087,#12088,#12089,#12090,#12091,#12092,#12093,#12094,
#12095,#12096,#12097,#12098,#12099,#12100,#12101,#12102,#12103,#12104,#12105,
#12106,#12107,#12108,#12109,#12110,#12111,#12112,#12113,#12114,#12115,#12116,
#12117,#12118,#12119,#12120,#12121,#12122,#12123,#12124,#12125,#12126,#12127,
#12128,#12129,#12130,#12131,#12132,#12133,#12134,#12135,#12136,#12137,#12138,
#12139,#12140,#12141,#12142,#12143,#12144,#12145,#12146,#12147,#12148,#12149,
#12150,#12151,#12152,#12153,#12154,#12155,#12156,#12157,#12158,#12159,#12160,
#12161,#12162,#12163,#12164,#12165,#12166,#12167,#12168,#12169,#12170,#12171,
#12172,#12173,#12174,#12175,#12176,#12177,#12178,#12179,#12180,#12181,#12182,
#12183,#12184,#12185,#12186,#12187,#12188,#12189,#12190,#12191,#12192,#12193,
#12194,#12195,#12196,#12197,#12198,#12199,#12200,#12201,#12202,#12203,#12204,
#12205,#12206,#12207,#12208,#12209,#12210,#12211,#12212,#12213,#12214,#12215,
#12216,#12217,#12218,#12219,#12220,#12221,#12222,#12223,#12224),
 .UNSPECIFIED.,.F.,.F.,(4,3,3,3,3,3,3,3,3,3,3,3,3,3,3,3,3,3,3,3,3,3,3,3,
3,3,3,3,3,3,3,3,3,3,3,3,3,3,3,3,3,3,3,3,3,3,3,3,3,3,3,3,3,3,3,3,3,3,3,3,
3,3,3,4),(38.815732076684,38.9740421812337,38.9824425842336,39.0821169883579,
39.1816479305039,39.2816909884516,39.3810417581606,39.4803594541538,39.5796745519763,
39.6802540125036,39.779713893883,39.8808531439844,39.9819923940857,40.0816670057345,
40.1811981917972,40.2812411933147,40.3805922926417,40.4799103494576,40.5792258386122,
40.6798049299436,40.7792652727665,40.8804037383522,40.9815422039379,41.0812025067406,
41.1807193316412,41.2807659169098,41.3801026326589,41.479406329145,41.5787075003759,
41.6793036287294,41.7787499036571,41.8799209587235,41.98109201379,42.0807829495895,
42.1803303720206,42.2803693034733,42.3797363109771,42.4790701185659,42.5784011808555,
42.6789613415522,42.7784366657676,42.8795392447049,42.9806418236422,43.0803246126712,
43.1798641832779,43.279905114555,43.379265035741,43.4785920579057,43.5779166428325,
43.678485390498,43.7779550524245,43.8790733429594,43.9801916334943,44.0797657624161,
44.1791961764749,44.2792643348338,44.3785146836635,44.4777322163513,44.5769475395425,
44.6776460154935,44.7770080855589,44.8783747644527,44.9797414433465,45.0989173838636),
 .UNSPECIFIED.);
#152=B_SPLINE_CURVE_WITH_KNOTS('',3,(#12226,#12227,#12228,#12229,#12230,
#12231,#12232,#12233,#12234,#12235,#12236,#12237,#12238,#12239,#12240,#12241,
#12242,#12243,#12244,#12245,#12246,#12247,#12248,#12249,#12250,#12251,#12252,
#12253,#12254,#12255,#12256,#12257,#12258,#12259,#12260,#12261,#12262,#12263,
#12264,#12265,#12266,#12267,#12268,#12269,#12270,#12271,#12272,#12273,#12274,
#12275,#12276,#12277,#12278,#12279,#12280,#12281,#12282,#12283),
 .UNSPECIFIED.,.F.,.F.,(4,3,3,3,3,3,3,3,3,3,3,3,3,3,3,3,3,3,3,4),(45.0989173840903,
45.1972992220322,45.295544194221,45.39371339496,45.4918387659123,45.5899521922755,
45.6881513826732,45.7863907224215,45.8848024611066,45.9792912531986,46.0779782270971,
46.1765245999247,46.274960260773,46.3733369495747,46.4716863252168,46.5700400094697,
46.6684897839427,46.7669938897809,46.8656553144966,46.9113379312297),
 .UNSPECIFIED.);
#153=B_SPLINE_CURVE_WITH_KNOTS('',3,(#12287,#12288,#12289,#12290),
 .UNSPECIFIED.,.F.,.F.,(4,4),(-48.977940682755,-48.0738672208643),
 .UNSPECIFIED.);
#154=B_SPLINE_CURVE_WITH_KNOTS('',3,(#12292,#12293,#12294,#12295,#12296,
#12297,#12298,#12299,#12300,#12301,#12302),.UNSPECIFIED.,.F.,.F.,(4,1,1,
1,1,1,1,1,4),(-48.0738672208643,-47.9783908729029,-46.9788410630507,-45.9792912531986,
-44.9797414433464,-43.9801916334943,-42.9806418236422,-41.98109201379,-41.7906819136848),
 .UNSPECIFIED.);
#155=B_SPLINE_CURVE_WITH_KNOTS('',3,(#12304,#12305,#12306,#12307,#12308,
#12309,#12310,#12311,#12312,#12313,#12314,#12315,#12316,#12317,#12318,#12319,
#12320,#12321,#12322,#12323,#12324,#12325,#12326,#12327,#12328,#12329,#12330,
#12331,#12332,#12333,#12334,#12335,#12336,#12337,#12338,#12339,#12340,#12341,
#12342,#12343,#12344,#12345,#12346,#12347,#12348,#12349,#12350,#12351,#12352,
#12353,#12354,#12355,#12356,#12357,#12358,#12359,#12360,#12361,#12362,#12363,
#12364,#12365,#12366,#12367,#12368,#12369,#12370,#12371,#12372,#12373,#12374,
#12375,#12376,#12377,#12378,#12379,#12380,#12381,#12382,#12383,#12384,#12385,
#12386,#12387,#12388,#12389,#12390,#12391,#12392,#12393,#12394,#12395,#12396,
#12397,#12398,#12399,#12400,#12401,#12402,#12403,#12404,#12405,#12406,#12407,
#12408,#12409,#12410,#12411,#12412,#12413,#12414,#12415,#12416,#12417,#12418,
#12419,#12420,#12421,#12422,#12423,#12424,#12425,#12426,#12427,#12428,#12429,
#12430,#12431,#12432,#12433,#12434,#12435,#12436,#12437,#12438,#12439,#12440,
#12441,#12442,#12443,#12444,#12445,#12446,#12447,#12448,#12449,#12450,#12451,
#12452,#12453,#12454,#12455,#12456,#12457,#12458,#12459,#12460,#12461,#12462,
#12463,#12464,#12465,#12466,#12467,#12468,#12469,#12470,#12471,#12472,#12473,
#12474,#12475,#12476,#12477,#12478,#12479,#12480,#12481,#12482,#12483,#12484,
#12485,#12486,#12487,#12488,#12489,#12490,#12491,#12492,#12493,#12494,#12495,
#12496),.UNSPECIFIED.,.F.,.F.,(4,3,3,3,3,3,3,3,3,3,3,3,3,3,3,3,3,3,3,3,
3,3,3,3,3,3,3,3,3,3,3,3,3,3,3,3,3,3,3,3,3,3,3,3,3,3,3,3,3,3,3,3,3,3,3,3,
3,3,3,3,3,3,3,3,4),(-41.7906819136848,-41.6895394499664,-41.5916133636765,
-41.4937386771787,-41.3958832780933,-41.2980150835204,-41.2000434104553,
-41.1020090687524,-41.0038203197812,-40.9815422039379,-40.8818674958635,
-40.7823362331089,-40.682293253231,-40.5829421257369,-40.4836240590206,
-40.3843085782246,-40.2837295321899,-40.1842692424979,-40.0831308182918,
-39.9819923940857,-39.8823182004062,-39.7827874232564,-39.6827443183786,
-39.5833936019912,-39.484075917306,-39.3847607888111,-39.2841812376667,
-39.1847212227925,-39.083581903513,-38.9824425842336,-38.8827714393196,
-38.7832437690838,-38.683199894746,-38.5838524044374,-38.4845379835411,
-38.3852261522286,-38.2846428077668,-38.1851861389609,-38.0840394566712,
-37.9828927743814,-37.8832198845563,-37.7836904454607,-37.6836470103443,
-37.5842977058408,-37.4849814577319,-37.3856677886411,-37.2850865826131,
-37.1856280687656,-37.0844855166474,-36.9833429645293,-36.8836702655405,
-36.7841410159631,-36.6840975333024,-36.5847484136251,-36.4854323481509,
-36.3861188592427,-36.2855374331013,-36.1860790914856,-36.0849361230814,
-35.9837931546772,-35.8778143170505,-35.7721698676901,-35.666730815553,
-35.5615688752373,-35.5074966067537),.UNSPECIFIED.);
#156=B_SPLINE_CURVE_WITH_KNOTS('',3,(#12498,#12499,#12500,#12501,#12502,
#12503,#12504,#12505,#12506,#12507,#12508,#12509,#12510,#12511,#12512,#12513,
#12514,#12515,#12516,#12517,#12518,#12519,#12520,#12521,#12522,#12523,#12524,
#12525,#12526,#12527,#12528,#12529,#12530,#12531,#12532,#12533,#12534,#12535,
#12536,#12537,#12538,#12539,#12540,#12541,#12542,#12543,#12544,#12545,#12546,
#12547,#12548,#12549,#12550,#12551,#12552,#12553,#12554,#12555,#12556,#12557,
#12558,#12559,#12560,#12561,#12562,#12563,#12564,#12565,#12566,#12567,#12568,
#12569,#12570,#12571,#12572,#12573,#12574,#12575,#12576,#12577,#12578,#12579,
#12580,#12581,#12582,#12583,#12584,#12585,#12586,#12587,#12588,#12589,#12590,
#12591,#12592,#12593,#12594,#12595,#12596,#12597,#12598,#12599,#12600,#12601,
#12602,#12603,#12604,#12605,#12606,#12607,#12608,#12609,#12610,#12611,#12612,
#12613,#12614,#12615,#12616,#12617,#12618,#12619,#12620,#12621,#12622,#12623,
#12624,#12625,#12626,#12627,#12628,#12629,#12630,#12631,#12632,#12633,#12634,
#12635,#12636,#12637,#12638,#12639,#12640,#12641,#12642,#12643,#12644,#12645,
#12646,#12647,#12648,#12649,#12650,#12651,#12652,#12653,#12654,#12655,#12656,
#12657,#12658,#12659,#12660,#12661,#12662,#12663,#12664,#12665,#12666,#12667,
#12668,#12669,#12670,#12671,#12672,#12673,#12674,#12675,#12676,#12677,#12678,
#12679,#12680,#12681,#12682,#12683,#12684,#12685,#12686,#12687),
 .UNSPECIFIED.,.F.,.F.,(4,3,3,3,3,3,3,3,3,3,3,3,3,3,3,3,3,3,3,3,3,3,3,3,
3,3,3,3,3,3,3,3,3,3,3,3,3,3,3,3,3,3,3,3,3,3,3,3,3,3,3,3,3,3,3,3,3,3,3,3,
3,3,3,4),(-35.5074966065052,-35.4044188003066,-35.2993749364362,-35.195940502646,
-35.0900919237355,-34.984243344825,-34.8845707497232,-34.785041607391,-34.6849980983388,
-34.5856490933414,-34.4863331450963,-34.3870197758162,-34.2864382156054,
-34.1869799983413,-34.0858367666571,-33.9846935349729,-33.88502097749,-33.7854918728732,
-33.6854483544041,-33.5860993870697,-33.4867834763825,-33.3874701445034,
-33.2868885396577,-33.1874303590178,-33.0862870420692,-32.9851437251207,
-32.8854711999204,-32.7859421282914,-32.6858986016635,-32.5865496687987,
-32.4872337930628,-32.3879204965709,-32.2873388512453,-32.1878807067094,
-32.086737310989,-31.9855939152686,-31.8859213638172,-31.7863922655387,
-31.6863487455234,-31.5869997852342,-31.4876838818432,-31.3883705575024,
-31.2877889444809,-31.1883307719029,-31.0871874386596,-30.9860441054164,
-30.8863715601185,-30.786842468035,-30.6867989464762,-30.5874499924358,
-30.4881340952999,-30.3888207772115,-30.2882391567997,-30.1887809904039,
-30.0876376429841,-29.9864942955643,-29.8881025663735,-29.7898393529225,
-29.6916725189187,-29.5935700512061,-29.4954678707829,-29.3973701963672,
-29.2991861658934,-29.2243112993256),.UNSPECIFIED.);
#157=B_SPLINE_CURVE_WITH_KNOTS('',3,(#12689,#12690,#12691,#12692,#12693,
#12694,#12695,#12696,#12697,#12698,#12699,#12700,#12701,#12702,#12703,#12704,
#12705,#12706,#12707,#12708,#12709,#12710,#12711,#12712,#12713,#12714,#12715,
#12716,#12717,#12718,#12719,#12720,#12721,#12722,#12723,#12724,#12725,#12726,
#12727,#12728,#12729,#12730,#12731,#12732,#12733,#12734,#12735,#12736,#12737,
#12738,#12739,#12740,#12741,#12742,#12743,#12744,#12745,#12746,#12747,#12748,
#12749,#12750,#12751,#12752,#12753,#12754,#12755,#12756,#12757,#12758,#12759,
#12760,#12761,#12762,#12763,#12764,#12765,#12766,#12767,#12768,#12769,#12770,
#12771,#12772,#12773,#12774,#12775,#12776,#12777,#12778,#12779,#12780,#12781,
#12782,#12783,#12784,#12785,#12786,#12787,#12788,#12789,#12790,#12791,#12792,
#12793,#12794,#12795,#12796,#12797,#12798,#12799,#12800,#12801,#12802,#12803,
#12804,#12805,#12806,#12807,#12808,#12809,#12810,#12811,#12812,#12813,#12814,
#12815,#12816,#12817,#12818,#12819,#12820,#12821,#12822,#12823,#12824,#12825,
#12826,#12827,#12828,#12829,#12830,#12831,#12832,#12833,#12834,#12835,#12836,
#12837,#12838,#12839,#12840,#12841,#12842,#12843,#12844,#12845,#12846,#12847,
#12848,#12849,#12850,#12851,#12852,#12853,#12854,#12855,#12856,#12857,#12858,
#12859,#12860,#12861,#12862,#12863,#12864,#12865,#12866,#12867,#12868,#12869,
#12870,#12871,#12872,#12873,#12874,#12875,#12876,#12877,#12878),
 .UNSPECIFIED.,.F.,.F.,(4,3,3,3,3,3,3,3,3,3,3,3,3,3,3,3,3,3,3,3,3,3,3,3,
3,3,3,3,3,3,3,3,3,3,3,3,3,3,3,3,3,3,3,3,3,3,3,3,3,3,3,3,3,3,3,3,3,3,3,3,
3,3,3,4),(-29.2243112989953,-29.0922651704096,-28.9869444857122,-28.8872719403693,
-28.7877428482655,-28.6876993267148,-28.5883503727153,-28.4890344756434,
-28.3897211576422,-28.2891395371967,-28.1896813709443,-28.0885380234021,
-27.98739467586,-27.887722131432,-27.7881930402516,-27.6881495184711,-27.5888005654086,
-27.4894846692765,-27.3901713522169,-27.2895897306646,-27.1901315653484,
-27.0889882156781,-26.9878448660079,-26.888172321829,-26.7886432309051,
-26.6885997090615,-26.5892507562718,-26.4899348604181,-26.3906215436422,
-26.2900399217706,-26.1905817567479,-26.0894384064518,-25.9882950561557,
-25.8886225116583,-25.7890934204099,-25.6890498986466,-25.5897009455201,
-25.4903850493256,-25.3910717322055,-25.29049011073,-25.1910319453582,-25.0898885958309,
-24.9887452463036,-24.8890727019102,-24.7895436107676,-24.6895000889781,
-24.5901511359609,-24.4908352398768,-24.391521922868,-24.2909403012638,
-24.1914821360043,-24.0903387862279,-23.9891954364514,-23.889522891946,
-23.7899938006913,-23.6899502789298,-23.5906013258012,-23.4912854296062,
-23.3919721124873,-23.2913904910153,-23.1919323256484,-23.0907889761239,
-22.9896456265993,-22.941125992146),.UNSPECIFIED.);
#158=B_SPLINE_CURVE_WITH_KNOTS('',3,(#12880,#12881,#12882,#12883,#12884,
#12885,#12886,#12887,#12888,#12889,#12890,#12891,#12892,#12893,#12894,#12895,
#12896,#12897,#12898,#12899,#12900,#12901,#12902,#12903,#12904,#12905,#12906,
#12907,#12908,#12909,#12910,#12911,#12912,#12913,#12914,#12915,#12916,#12917,
#12918,#12919,#12920,#12921,#12922,#12923,#12924,#12925,#12926,#12927,#12928,
#12929,#12930,#12931,#12932,#12933,#12934,#12935,#12936,#12937,#12938,#12939,
#12940,#12941,#12942,#12943,#12944,#12945,#12946,#12947,#12948,#12949,#12950,
#12951,#12952,#12953,#12954,#12955,#12956,#12957,#12958,#12959,#12960,#12961,
#12962,#12963,#12964,#12965,#12966,#12967,#12968,#12969,#12970,#12971,#12972,
#12973,#12974,#12975,#12976,#12977,#12978,#12979,#12980,#12981,#12982,#12983,
#12984,#12985,#12986,#12987,#12988,#12989,#12990,#12991,#12992,#12993,#12994,
#12995,#12996,#12997,#12998,#12999,#13000,#13001,#13002,#13003,#13004,#13005,
#13006,#13007,#13008,#13009,#13010,#13011,#13012,#13013,#13014,#13015,#13016,
#13017,#13018,#13019,#13020,#13021,#13022,#13023,#13024,#13025,#13026,#13027,
#13028,#13029,#13030,#13031,#13032,#13033,#13034,#13035,#13036,#13037,#13038,
#13039,#13040,#13041,#13042,#13043,#13044,#13045,#13046,#13047,#13048,#13049,
#13050,#13051,#13052,#13053,#13054,#13055,#13056,#13057,#13058,#13059,#13060,
#13061,#13062,#13063,#13064,#13065,#13066,#13067,#13068,#13069),
 .UNSPECIFIED.,.F.,.F.,(4,3,3,3,3,3,3,3,3,3,3,3,3,3,3,3,3,3,3,3,3,3,3,3,
3,3,3,3,3,3,3,3,3,3,3,3,3,3,3,3,3,3,3,3,3,3,3,3,3,3,3,3,3,3,3,3,3,3,3,3,
3,3,3,4),(-22.9411259918217,-22.8422132186966,-22.7434395746755,-22.6447744362852,
-22.5461673015594,-22.4475867495727,-22.3490013949527,-22.2503151664381,
-22.1515747710859,-22.052665774763,-21.9900958167472,-21.8904232722928,
-21.7908941810916,-21.690850659317,-21.5915017062476,-21.4921858101138,
-21.3928724930579,-21.2922908715172,-21.1928327062173,-21.0916893565562,
-20.990546006895,-20.8908734615185,-20.7913443693884,-20.6913008478452,
-20.5919518938372,-20.4926359967633,-20.3933226787671,-20.292741058336,
-20.1932828921048,-20.0921395445738,-19.9909961970429,-19.891323654999,
-19.7917945662044,-19.6917510438277,-19.5924020931379,-19.4930861993685,
-19.3937728846584,-19.2931912602915,-19.193733097269,-19.0925897422298,
-18.9914463871907,-18.8917738416275,-18.7922447493354,-18.6922012278358,
-18.592852273727,-18.4935363765752,-18.3942230585238,-18.2936414382275,
-18.1941832719976,-18.0930399246681,-17.9918965773386,-17.8922240257118,
-17.7926949272958,-17.6926514073196,-17.5933024469851,-17.4939865435839,
-17.3946732192674,-17.2940916063222,-17.1946334338536,-17.09349010067,-16.9923467674864,
-16.8753468893682,-16.7595002690756,-16.6579406851814),.UNSPECIFIED.);
#159=B_SPLINE_CURVE_WITH_KNOTS('',3,(#13071,#13072,#13073,#13074,#13075,
#13076,#13077,#13078,#13079,#13080,#13081,#13082,#13083,#13084,#13085,#13086,
#13087,#13088,#13089,#13090,#13091,#13092,#13093,#13094,#13095,#13096,#13097,
#13098,#13099,#13100,#13101,#13102,#13103,#13104,#13105,#13106,#13107,#13108,
#13109,#13110,#13111,#13112,#13113,#13114,#13115,#13116,#13117,#13118,#13119,
#13120,#13121,#13122,#13123,#13124,#13125,#13126,#13127,#13128,#13129,#13130,
#13131,#13132,#13133,#13134,#13135,#13136,#13137,#13138,#13139,#13140,#13141,
#13142,#13143,#13144,#13145,#13146,#13147,#13148,#13149,#13150,#13151,#13152,
#13153,#13154,#13155,#13156,#13157,#13158,#13159,#13160,#13161,#13162,#13163,
#13164,#13165,#13166,#13167,#13168,#13169,#13170,#13171,#13172,#13173,#13174,
#13175,#13176,#13177,#13178,#13179,#13180,#13181,#13182,#13183,#13184,#13185,
#13186,#13187,#13188,#13189,#13190,#13191,#13192,#13193,#13194,#13195,#13196,
#13197,#13198,#13199,#13200,#13201,#13202,#13203,#13204,#13205,#13206,#13207,
#13208,#13209,#13210,#13211,#13212,#13213,#13214,#13215,#13216,#13217,#13218,
#13219,#13220,#13221,#13222,#13223,#13224,#13225,#13226,#13227,#13228,#13229,
#13230,#13231,#13232,#13233,#13234,#13235,#13236,#13237,#13238,#13239,#13240,
#13241,#13242,#13243,#13244,#13245,#13246,#13247,#13248,#13249,#13250,#13251,
#13252,#13253,#13254,#13255,#13256,#13257,#13258,#13259,#13260,#13261,#13262,
#13263),.UNSPECIFIED.,.F.,.F.,(4,3,3,3,3,3,3,3,3,3,3,3,3,3,3,3,3,3,3,3,
3,3,3,3,3,3,3,3,3,3,3,3,3,3,3,3,3,3,3,3,3,3,3,3,3,3,3,3,3,3,3,3,3,3,3,3,
3,3,3,3,3,3,3,3,4),(-16.6579406849664,-16.5586673411425,-16.4594098080319,
-16.3601376655488,-16.2607507488239,-16.1613029056952,-16.061674030148,
-15.9927969576343,-15.8931243976124,-15.7935952910013,-15.6935517730989,
-15.5942028051098,-15.4948868942719,-15.3955735627455,-15.2949919590046,
-15.1955337799511,-15.0943904638666,-14.9932471477821,-14.8935745521242,
-14.7940454093551,-14.694001900427,-14.5946528952861,-14.495336947008,-14.3960235778053,
-14.2954420178365,-14.1959838009197,-14.0948405694249,-13.99369733793,-13.894024970901,
-13.7944960572543,-13.6944524911072,-13.595103714624,-13.495787994327,-13.3964748521264,
-13.2958930211143,-13.1964350264896,-13.0952912772837,-12.9941475280779,
-12.8944748055864,-12.7949455375518,-12.694902060136,-12.5955529343998,
-12.4962368675317,-12.3969233818907,-12.2963419659745,-12.1968836390442,
-12.0957406786349,-11.9945977182257,-11.8949248315594,-11.7953953949446,
-11.6953519591232,-11.596002655434,-11.4966864075124,-11.3973727379825,
-11.2967915305803,-11.1973330147593,-11.0961904615665,-10.9950479083736,
-10.8944502270782,-10.7940032781318,-10.6891913030456,-10.5889704326472,
-10.4888063042122,-10.3886646483777,-10.3747553777868),.UNSPECIFIED.);
#160=B_SPLINE_CURVE_WITH_KNOTS('',3,(#13264,#13265,#13266,#13267,#13268,
#13269,#13270,#13271,#13272,#13273,#13274,#13275,#13276,#13277,#13278,#13279,
#13280,#13281,#13282,#13283,#13284,#13285,#13286,#13287,#13288,#13289,#13290,
#13291,#13292,#13293,#13294,#13295,#13296,#13297,#13298,#13299,#13300,#13301,
#13302,#13303,#13304,#13305,#13306,#13307,#13308,#13309,#13310,#13311,#13312,
#13313,#13314,#13315,#13316,#13317,#13318,#13319,#13320,#13321,#13322,#13323,
#13324,#13325,#13326,#13327,#13328,#13329,#13330,#13331,#13332,#13333,#13334,
#13335,#13336,#13337,#13338,#13339,#13340,#13341,#13342,#13343,#13344,#13345,
#13346,#13347,#13348,#13349,#13350,#13351,#13352,#13353,#13354,#13355,#13356,
#13357,#13358,#13359,#13360,#13361,#13362,#13363,#13364,#13365,#13366,#13367,
#13368,#13369,#13370,#13371,#13372,#13373,#13374,#13375,#13376,#13377,#13378,
#13379,#13380,#13381,#13382,#13383,#13384,#13385,#13386,#13387,#13388,#13389,
#13390,#13391,#13392,#13393,#13394,#13395,#13396,#13397,#13398,#13399,#13400,
#13401,#13402,#13403,#13404,#13405,#13406,#13407,#13408,#13409,#13410,#13411,
#13412,#13413,#13414,#13415,#13416,#13417,#13418,#13419,#13420,#13421,#13422,
#13423,#13424,#13425,#13426,#13427,#13428,#13429,#13430,#13431,#13432,#13433,
#13434,#13435,#13436,#13437,#13438,#13439,#13440,#13441,#13442,#13443,#13444,
#13445,#13446,#13447,#13448,#13449,#13450,#13451,#13452,#13453,#13454,#13455,
#13456),.UNSPECIFIED.,.F.,.F.,(4,3,3,3,3,3,3,3,3,3,3,3,3,3,3,3,3,3,3,3,
3,3,3,3,3,3,3,3,3,3,3,3,3,3,3,3,3,3,3,3,3,3,3,3,3,3,3,3,3,3,3,3,3,3,3,3,
3,3,3,3,3,3,3,3,4),(-10.3747553775598,-10.2633020300802,-10.1513665111728,
-10.0388261271735,-9.99549809852144,-9.8958236930791,-9.79629274962715,
-9.69624969200742,-9.59689892103024,-9.49758122378561,-9.39826612473022,
-9.29768666571498,-9.19822678315976,-9.09708753591453,-8.99594828866929,
-8.89627367265352,-8.79674248219455,-8.69669948177237,-8.5973483780097,
-8.49803031675303,-8.39871482315869,-8.29813573707331,-8.19867538985861,
-8.09753693433788,-7.99639847881715,-7.89673818865013,-7.79722137640207,
-7.69717478797244,-7.59783808482659,-7.49853440089793,-7.39923324216268,
-7.29863709886326,-7.19919083615364,-7.09801975255933,-6.99684866896501,
-6.89715772460678,-6.79761029368071,-6.69757136435973,-6.59820434857338,
-6.49887053279914,-6.3995394624311,-6.29897931160154,-6.19950397964904,
-6.09840141938095,-5.99729885911286,-5.897616043936,-5.79807644701137,-5.69803552229254,
-5.59867557456924,-5.49934852584398,-5.40002391436897,-5.29945519809191,
-5.19998550992019,-5.09886727959046,-4.99774904926072,-4.89936263245375,
-4.79838856225184,-4.70026016252175,-4.60219107760665,-4.50414935420518,
-4.4010045333635,-4.30286581258146,-4.20467026972117,-4.10633389245817,
-4.09157007083846),.UNSPECIFIED.);
#161=B_SPLINE_CURVE_WITH_KNOTS('',3,(#13459,#13460,#13461,#13462,#13463,
#13464,#13465,#13466,#13467,#13468,#13469,#13470,#13471,#13472,#13473,#13474,
#13475,#13476,#13477,#13478,#13479,#13480,#13481,#13482,#13483,#13484,#13485,
#13486,#13487,#13488,#13489,#13490,#13491,#13492,#13493,#13494,#13495,#13496,
#13497,#13498,#13499,#13500,#13501,#13502,#13503,#13504,#13505,#13506,#13507,
#13508,#13509,#13510,#13511,#13512,#13513,#13514,#13515,#13516,#13517,#13518,
#13519,#13520,#13521,#13522,#13523,#13524,#13525,#13526,#13527,#13528,#13529,
#13530,#13531,#13532,#13533,#13534,#13535,#13536,#13537,#13538,#13539,#13540,
#13541,#13542,#13543,#13544,#13545,#13546,#13547,#13548,#13549,#13550,#13551,
#13552,#13553,#13554,#13555,#13556,#13557,#13558,#13559,#13560,#13561,#13562,
#13563,#13564,#13565,#13566,#13567,#13568,#13569,#13570,#13571,#13572,#13573,
#13574,#13575,#13576,#13577,#13578,#13579,#13580,#13581,#13582,#13583,#13584,
#13585,#13586,#13587,#13588,#13589,#13590,#13591,#13592,#13593,#13594,#13595,
#13596,#13597,#13598,#13599,#13600),.UNSPECIFIED.,.F.,.F.,(4,2,2,2,2,2,
2,2,2,2,2,2,2,2,2,2,2,2,2,2,2,2,2,2,2,2,2,2,2,2,2,2,2,2,2,2,2,2,2,2,2,2,
2,2,2,2,2,2,2,2,2,2,2,2,2,2,2,2,2,2,2,2,2,2,2,2,2,2,2,2,4),(0.00344614780203521,
0.0284904809162007,0.0538827835859065,0.0686235091287068,0.0805907163808784,
0.088137184145726,0.0953647804091584,0.105948947249549,0.148809238680941,
0.174870676231912,0.182416612380744,0.186813258257199,0.191148233825763,
0.198518498889793,0.239540652573207,0.265824100780086,0.278138797633332,
0.285723990068682,0.292870302749267,0.303102561147615,0.350354141141507,
0.37701560068224,0.38337240950892,0.387492863749183,0.392033763200307,0.400628758995628,
0.442163465895457,0.46192026039917,0.476487946049621,0.484426655666293,
0.4914276555967,0.500373376773164,0.520704931735167,0.557385940501716,0.571367663036804,
0.581032891036802,0.585765491248748,0.589798436758793,0.595669021614399,
0.612777843676554,0.652219618644748,0.666914259898479,0.678822075434346,
0.686311010144705,0.693463387690597,0.70387939087316,0.749251031316509,
0.774776003909911,0.782234190550168,0.786568355294679,0.790321817980931,
0.796931037944707,0.837127218544441,0.868266394811345,0.879325378369257,
0.886654854005653,0.894008061095456,0.90519984640876,0.939888617553977,
0.975099823638863,0.982320866939109,0.986600426159565,0.99090689945427,
0.998270083153767,1.03736018233108,1.06825595227068,1.07927807583162,1.08659475677513,
1.09394298889186,1.10514182987474,1.14091205305926),.UNSPECIFIED.);
#162=B_SPLINE_CURVE_WITH_KNOTS('',3,(#13603,#13604,#13605,#13606,#13607,
#13608,#13609,#13610,#13611,#13612,#13613,#13614,#13615,#13616,#13617,#13618,
#13619,#13620,#13621,#13622,#13623,#13624,#13625,#13626,#13627,#13628,#13629,
#13630,#13631,#13632,#13633,#13634,#13635,#13636,#13637,#13638,#13639,#13640,
#13641,#13642,#13643,#13644,#13645,#13646,#13647,#13648,#13649,#13650,#13651,
#13652,#13653,#13654,#13655,#13656,#13657,#13658,#13659,#13660,#13661,#13662,
#13663,#13664,#13665,#13666,#13667,#13668,#13669,#13670,#13671,#13672,#13673,
#13674,#13675,#13676,#13677,#13678,#13679,#13680,#13681,#13682,#13683,#13684,
#13685,#13686,#13687,#13688,#13689,#13690,#13691,#13692,#13693,#13694,#13695,
#13696,#13697,#13698,#13699,#13700,#13701,#13702,#13703,#13704,#13705,#13706,
#13707,#13708,#13709,#13710,#13711,#13712,#13713,#13714,#13715,#13716,#13717,
#13718),.UNSPECIFIED.,.F.,.F.,(4,2,2,2,2,2,2,2,2,2,2,2,2,2,2,2,2,2,2,2,
2,2,2,2,2,2,2,2,2,2,2,2,2,2,2,2,2,2,2,2,2,2,2,2,2,2,2,2,2,2,2,2,2,2,2,2,
2,4),(-2.03242761728642,-2.02762265841596,-2.02074164543271,-1.99378590696461,
-1.96115676855459,-1.94888264165494,-1.94078466233113,-1.93352430127577,
-1.92153998007138,-1.87671871271659,-1.84476717116948,-1.83760222730833,
-1.83330543103495,-1.82911334753728,-1.82199209565321,-1.78922107582986,
-1.7632635939393,-1.75126440888435,-1.7410821508505,-1.73413278090626,-1.72703111694745,
-1.71602151042092,-1.67429397364971,-1.64188030443115,-1.63543654221534,
-1.63142051335166,-1.62706916372963,-1.61945826864553,-1.59000834494158,
-1.55174184931512,-1.53956017079099,-1.53197388661241,-1.5247696160083,
-1.51433383519624,-1.47029166509564,-1.444912902043,-1.43744218410541,-1.43306050649059,
-1.42871011071478,-1.42126320596611,-1.39601056521357,-1.37277625645214,
-1.35578375818058,-1.34259802423399,-1.33485159013306,-1.32769445744438,
-1.31787325536777,-1.28786256114238,-1.24733765389243,-1.23856726828699,
-1.23397102673795,-1.22992510616663,-1.22370955288778,-1.20129210256359,
-1.1753772154676,-1.15699378298739,-1.1431061302417,-1.14066834730415),
 .UNSPECIFIED.);
#163=B_SPLINE_CURVE_WITH_KNOTS('',3,(#13927,#13928,#13929,#13930,#13931,
#13932,#13933,#13934,#13935,#13936,#13937,#13938,#13939,#13940,#13941,#13942,
#13943,#13944,#13945,#13946,#13947,#13948,#13949,#13950,#13951,#13952,#13953,
#13954,#13955,#13956,#13957,#13958,#13959,#13960,#13961,#13962,#13963,#13964,
#13965,#13966,#13967,#13968,#13969,#13970,#13971,#13972,#13973,#13974,#13975,
#13976,#13977,#13978,#13979,#13980,#13981,#13982,#13983,#13984,#13985,#13986,
#13987,#13988,#13989,#13990,#13991,#13992,#13993,#13994,#13995,#13996,#13997,
#13998,#13999,#14000,#14001,#14002,#14003,#14004,#14005,#14006,#14007,#14008),
 .UNSPECIFIED.,.F.,.F.,(4,3,3,3,3,3,3,3,3,3,3,3,3,3,3,3,3,3,3,3,3,3,3,3,
3,3,3,4),(-0.461743572254199,-0.445279637544711,-0.419665409334653,-0.398766763381763,
-0.394162024454705,-0.368774962988829,-0.349177254342088,-0.339871226708548,
-0.335357168261631,-0.310607959532329,-0.286107327656323,-0.262350263015158,
-0.248443506470567,-0.244441072949281,-0.220948576203007,-0.211993293814896,
-0.187932245402815,-0.164529603299809,-0.160799747913903,-0.137491872951246,
-0.114210964158578,-0.0911177765171172,-0.0820653542879866,-0.0764306774118449,
-0.054031428691482,-0.0318872073099107,-0.0105083701393909,-7.00415783501338E-15),
 .UNSPECIFIED.);
#164=B_SPLINE_CURVE_WITH_KNOTS('',3,(#14009,#14010,#14011,#14012,#14013,
#14014,#14015,#14016,#14017,#14018,#14019,#14020,#14021,#14022,#14023,#14024,
#14025,#14026,#14027,#14028,#14029,#14030,#14031,#14032,#14033,#14034,#14035,
#14036,#14037,#14038,#14039,#14040,#14041,#14042,#14043,#14044,#14045,#14046,
#14047,#14048,#14049,#14050,#14051,#14052,#14053,#14054,#14055,#14056,#14057,
#14058,#14059,#14060,#14061,#14062,#14063,#14064,#14065,#14066,#14067,#14068,
#14069,#14070,#14071,#14072,#14073,#14074,#14075,#14076,#14077,#14078,#14079,
#14080,#14081,#14082,#14083,#14084,#14085,#14086,#14087,#14088,#14089,#14090,
#14091,#14092,#14093,#14094,#14095,#14096),.UNSPECIFIED.,.F.,.F.,(4,3,3,
3,3,3,3,3,3,3,3,3,3,3,3,3,3,3,3,3,3,3,3,3,3,3,3,3,3,4),(-0.46380305084373,
-0.450143378394066,-0.42834691099736,-0.416417514424194,-0.41061770490034,
-0.40583848098822,-0.383170125624015,-0.364752716270424,-0.357183720834536,
-0.352389301015471,-0.328937236053495,-0.305197499653431,-0.281594469780252,
-0.274956577509301,-0.271007211480475,-0.246578486425838,-0.235958639370917,
-0.212131827480764,-0.188305015590611,-0.184276201227976,-0.180478707993104,
-0.156057553901815,-0.131200496694823,-0.106091750867829,-0.0960021957213982,
-0.0910056989017407,-0.0652625445071726,-0.0394826186541935,-0.0142546737832877,
0.),.UNSPECIFIED.);
#165=B_SPLINE_CURVE_WITH_KNOTS('',3,(#14102,#14103,#14104,#14105,#14106,
#14107,#14108,#14109,#14110,#14111,#14112,#14113,#14114,#14115,#14116,#14117,
#14118,#14119,#14120,#14121,#14122,#14123,#14124,#14125,#14126,#14127,#14128,
#14129,#14130,#14131,#14132,#14133,#14134,#14135,#14136,#14137,#14138,#14139,
#14140,#14141,#14142,#14143,#14144,#14145,#14146,#14147,#14148,#14149,#14150,
#14151,#14152,#14153,#14154,#14155,#14156,#14157,#14158,#14159,#14160,#14161,
#14162,#14163,#14164,#14165,#14166,#14167,#14168,#14169,#14170,#14171,#14172,
#14173,#14174,#14175,#14176,#14177,#14178,#14179,#14180,#14181,#14182,#14183,
#14184,#14185,#14186),.UNSPECIFIED.,.F.,.F.,(4,3,3,3,3,3,3,3,3,3,3,3,3,
3,3,3,3,3,3,3,3,3,3,3,3,3,3,3,4),(-0.45699211118371,-0.445279637544697,
-0.419665409508243,-0.406685902277409,-0.398766768567209,-0.39416203748691,
-0.368775578482156,-0.349177265885345,-0.339871244646184,-0.335357179438787,
-0.31060797213875,-0.286107345244344,-0.262350291376267,-0.248443540782049,
-0.244441077482334,-0.220948588962521,-0.211993293814895,-0.187932247195927,
-0.164529607973285,-0.160799753252352,-0.137463400398657,-0.114082069442804,
-0.0911406010852215,-0.0820653229868862,-0.076430692769169,-0.0539748622314556,
-0.0318871978476813,-0.0105083424875331,0.),.UNSPECIFIED.);
#166=B_SPLINE_CURVE_WITH_KNOTS('',3,(#14396,#14397,#14398,#14399,#14400,
#14401,#14402,#14403,#14404,#14405,#14406,#14407,#14408,#14409,#14410,#14411,
#14412,#14413,#14414,#14415,#14416,#14417,#14418,#14419,#14420,#14421,#14422,
#14423,#14424,#14425,#14426,#14427,#14428,#14429,#14430,#14431,#14432,#14433,
#14434,#14435,#14436,#14437,#14438,#14439,#14440,#14441,#14442,#14443,#14444,
#14445,#14446,#14447,#14448,#14449,#14450,#14451,#14452,#14453,#14454,#14455,
#14456,#14457,#14458,#14459,#14460,#14461,#14462,#14463,#14464,#14465,#14466,
#14467,#14468,#14469,#14470,#14471,#14472,#14473,#14474,#14475,#14476,#14477,
#14478,#14479,#14480),.UNSPECIFIED.,.F.,.F.,(4,3,3,3,3,3,3,3,3,3,3,3,3,
3,3,3,3,3,3,3,3,3,3,3,3,3,3,3,4),(-0.46380305084373,-0.450143378394054,
-0.428264440755745,-0.410617883401312,-0.4058385271806,-0.383170177979863,
-0.364752761817912,-0.357183853622535,-0.352389339422303,-0.328937278005717,
-0.305197541696273,-0.281594511232344,-0.274956601237073,-0.27100723282273,
-0.246578506918939,-0.235958639370914,-0.21213183187221,-0.188305024373507,
-0.184276201248984,-0.180478707195112,-0.156127340170029,-0.131048754059854,
-0.105970167949679,-0.0960021891969689,-0.0910056975232237,-0.0652625456624386,
-0.0394826167527914,-0.0142546579228003,0.),.UNSPECIFIED.);
#167=B_SPLINE_CURVE_WITH_KNOTS('',3,(#14481,#14482,#14483,#14484),
 .UNSPECIFIED.,.F.,.F.,(4,4),(0.,0.0143039377755772),.UNSPECIFIED.);
#168=B_SPLINE_CURVE_WITH_KNOTS('',3,(#14485,#14486,#14487,#14488),
 .UNSPECIFIED.,.F.,.F.,(4,4),(0.,0.0481823570135641),.UNSPECIFIED.);
#173=TOROIDAL_SURFACE('',#2103,6.60753780880871,4.83650249899603);
#181=SHAPE_REPRESENTATION_RELATIONSHIP('SRR','None',#14583,#189);
#189=ADVANCED_BREP_SHAPE_REPRESENTATION('',(#205),#14543);
#197=STYLED_ITEM('',(#14627),#205);
#205=MANIFOLD_SOLID_BREP('Body1',#1833);
#251=LINE('',#8674,#307);
#252=LINE('',#8783,#308);
#253=LINE('',#9129,#309);
#254=LINE('',#9478,#310);
#255=LINE('',#9802,#311);
#256=LINE('',#10146,#312);
#257=LINE('',#10474,#313);
#258=LINE('',#14499,#314);
#259=LINE('',#14502,#315);
#260=LINE('',#14510,#316);
#261=LINE('',#14516,#317);
#307=VECTOR('',#2503,1.99475);
#308=VECTOR('',#2508,1.99475);
#309=VECTOR('',#2511,1.99475);
#310=VECTOR('',#2514,1.99475);
#311=VECTOR('',#2517,1.99475);
#312=VECTOR('',#2520,1.99475);
#313=VECTOR('',#2523,1.99475);
#314=VECTOR('',#2554,3.86373699625103);
#315=VECTOR('',#2557,3.70051543670999);
#316=VECTOR('',#2568,0.684464879973279);
#317=VECTOR('',#2577,1.77103530981268);
#358=CYLINDRICAL_SURFACE('',#2087,1.99475);
#359=CYLINDRICAL_SURFACE('',#2089,1.99475);
#360=CYLINDRICAL_SURFACE('',#2090,1.99475);
#361=CYLINDRICAL_SURFACE('',#2091,1.99475);
#362=CYLINDRICAL_SURFACE('',#2092,1.99475);
#363=CYLINDRICAL_SURFACE('',#2093,1.99475);
#364=CYLINDRICAL_SURFACE('',#2094,1.99475);
#365=CYLINDRICAL_SURFACE('',#2095,2.4505);
#366=CYLINDRICAL_SURFACE('',#2098,1.99475);
#367=CYLINDRICAL_SURFACE('',#2108,3.86373699625103);
#368=CYLINDRICAL_SURFACE('',#2114,0.684464879973279);
#369=CYLINDRICAL_SURFACE('',#2119,1.77103530981268);
#397=FACE_BOUND('',#629,.T.);
#398=FACE_BOUND('',#633,.T.);
#483=FACE_OUTER_BOUND('',#615,.T.);
#484=FACE_OUTER_BOUND('',#616,.T.);
#485=FACE_OUTER_BOUND('',#617,.T.);
#486=FACE_OUTER_BOUND('',#618,.T.);
#487=FACE_OUTER_BOUND('',#619,.T.);
#488=FACE_OUTER_BOUND('',#620,.T.);
#489=FACE_OUTER_BOUND('',#621,.T.);
#490=FACE_OUTER_BOUND('',#622,.T.);
#491=FACE_OUTER_BOUND('',#623,.T.);
#492=FACE_OUTER_BOUND('',#624,.T.);
#493=FACE_OUTER_BOUND('',#625,.T.);
#494=FACE_OUTER_BOUND('',#626,.T.);
#495=FACE_OUTER_BOUND('',#627,.T.);
#496=FACE_OUTER_BOUND('',#628,.T.);
#497=FACE_OUTER_BOUND('',#630,.T.);
#498=FACE_OUTER_BOUND('',#631,.T.);
#499=FACE_OUTER_BOUND('',#632,.T.);
#500=FACE_OUTER_BOUND('',#634,.T.);
#501=FACE_OUTER_BOUND('',#635,.T.);
#502=FACE_OUTER_BOUND('',#636,.T.);
#503=FACE_OUTER_BOUND('',#637,.T.);
#615=EDGE_LOOP('',(#1541,#1542,#1543,#1544));
#616=EDGE_LOOP('',(#1545,#1546,#1547,#1548,#1549));
#617=EDGE_LOOP('',(#1550,#1551,#1552,#1553,#1554,#1555));
#618=EDGE_LOOP('',(#1556,#1557,#1558,#1559));
#619=EDGE_LOOP('',(#1560,#1561,#1562,#1563,#1564,#1565));
#620=EDGE_LOOP('',(#1566,#1567,#1568,#1569));
#621=EDGE_LOOP('',(#1570,#1571,#1572,#1573,#1574,#1575));
#622=EDGE_LOOP('',(#1576,#1577,#1578,#1579,#1580,#1581,#1582,#1583,#1584,
#1585,#1586,#1587,#1588,#1589,#1590,#1591,#1592,#1593,#1594,#1595));
#623=EDGE_LOOP('',(#1596,#1597,#1598,#1599));
#624=EDGE_LOOP('',(#1600,#1601,#1602,#1603,#1604,#1605,#1606,#1607,#1608,
#1609,#1610,#1611,#1612,#1613,#1614,#1615,#1616,#1617,#1618,#1619,#1620,
#1621,#1622));
#625=EDGE_LOOP('',(#1623,#1624,#1625,#1626,#1627));
#626=EDGE_LOOP('',(#1628,#1629,#1630,#1631,#1632,#1633,#1634,#1635,#1636,
#1637,#1638,#1639,#1640,#1641,#1642,#1643,#1644,#1645,#1646,#1647,#1648,
#1649,#1650,#1651));
#627=EDGE_LOOP('',(#1652,#1653,#1654,#1655,#1656,#1657,#1658));
#628=EDGE_LOOP('',(#1659));
#629=EDGE_LOOP('',(#1660,#1661,#1662,#1663,#1664));
#630=EDGE_LOOP('',(#1665,#1666,#1667,#1668));
#631=EDGE_LOOP('',(#1669,#1670,#1671,#1672));
#632=EDGE_LOOP('',(#1673));
#633=EDGE_LOOP('',(#1674));
#634=EDGE_LOOP('',(#1675,#1676,#1677,#1678));
#635=EDGE_LOOP('',(#1679));
#636=EDGE_LOOP('',(#1680));
#637=EDGE_LOOP('',(#1681,#1682,#1683,#1684));
#711=CIRCLE('',#2088,1.99475);
#712=CIRCLE('',#2096,2.4505);
#713=CIRCLE('',#2097,2.4505);
#714=CIRCLE('',#2099,1.99475);
#715=CIRCLE('',#2101,2.4505);
#716=CIRCLE('',#2102,2.4505);
#717=CIRCLE('',#2104,4.83650249899603);
#718=CIRCLE('',#2105,1.77103530981268);
#719=CIRCLE('',#2107,3.86373699625103);
#720=CIRCLE('',#2109,3.86373699625103);
#721=CIRCLE('',#2111,3.53729387716894);
#722=CIRCLE('',#2113,0.684464879973279);
#723=CIRCLE('',#2115,0.684464879973279);
#724=CIRCLE('',#2118,1.77103530981268);
#859=VERTEX_POINT('',#8672);
#860=VERTEX_POINT('',#8673);
#861=VERTEX_POINT('',#8675);
#862=VERTEX_POINT('',#8684);
#863=VERTEX_POINT('',#8781);
#864=VERTEX_POINT('',#8782);
#865=VERTEX_POINT('',#8784);
#866=VERTEX_POINT('',#9127);
#867=VERTEX_POINT('',#9128);
#868=VERTEX_POINT('',#9130);
#869=VERTEX_POINT('',#9300);
#870=VERTEX_POINT('',#9476);
#871=VERTEX_POINT('',#9477);
#872=VERTEX_POINT('',#9800);
#873=VERTEX_POINT('',#9801);
#874=VERTEX_POINT('',#9803);
#875=VERTEX_POINT('',#9968);
#876=VERTEX_POINT('',#10144);
#877=VERTEX_POINT('',#10145);
#878=VERTEX_POINT('',#10472);
#879=VERTEX_POINT('',#10473);
#880=VERTEX_POINT('',#10475);
#881=VERTEX_POINT('',#10640);
#882=VERTEX_POINT('',#10808);
#883=VERTEX_POINT('',#10809);
#884=VERTEX_POINT('',#10874);
#885=VERTEX_POINT('',#10876);
#886=VERTEX_POINT('',#10882);
#887=VERTEX_POINT('',#11073);
#888=VERTEX_POINT('',#11264);
#889=VERTEX_POINT('',#11455);
#890=VERTEX_POINT('',#11646);
#891=VERTEX_POINT('',#11840);
#892=VERTEX_POINT('',#12034);
#893=VERTEX_POINT('',#12225);
#894=VERTEX_POINT('',#12284);
#895=VERTEX_POINT('',#12286);
#896=VERTEX_POINT('',#12291);
#897=VERTEX_POINT('',#12303);
#898=VERTEX_POINT('',#12497);
#899=VERTEX_POINT('',#12688);
#900=VERTEX_POINT('',#12879);
#901=VERTEX_POINT('',#13070);
#902=VERTEX_POINT('',#13458);
#903=VERTEX_POINT('',#13601);
#904=VERTEX_POINT('',#14098);
#905=VERTEX_POINT('',#14100);
#906=VERTEX_POINT('',#14395);
#907=VERTEX_POINT('',#14490);
#908=VERTEX_POINT('',#14494);
#909=VERTEX_POINT('',#14497);
#910=VERTEX_POINT('',#14501);
#911=VERTEX_POINT('',#14505);
#912=VERTEX_POINT('',#14508);
#913=VERTEX_POINT('',#14513);
#1099=EDGE_CURVE('',#859,#860,#251,.T.);
#1100=EDGE_CURVE('',#861,#859,#122,.T.);
#1101=EDGE_CURVE('',#862,#861,#711,.T.);
#1102=EDGE_CURVE('',#862,#860,#123,.T.);
#1103=EDGE_CURVE('',#863,#864,#252,.T.);
#1104=EDGE_CURVE('',#865,#863,#124,.T.);
#1105=EDGE_CURVE('',#859,#865,#125,.T.);
#1106=EDGE_CURVE('',#860,#864,#126,.T.);
#1107=EDGE_CURVE('',#866,#867,#253,.T.);
#1108=EDGE_CURVE('',#868,#866,#127,.F.);
#1109=EDGE_CURVE('',#863,#868,#128,.T.);
#1110=EDGE_CURVE('',#864,#869,#129,.T.);
#1111=EDGE_CURVE('',#869,#867,#130,.T.);
#1112=EDGE_CURVE('',#870,#871,#254,.T.);
#1113=EDGE_CURVE('',#866,#870,#131,.F.);
#1114=EDGE_CURVE('',#867,#871,#132,.T.);
#1115=EDGE_CURVE('',#872,#873,#255,.T.);
#1116=EDGE_CURVE('',#874,#872,#133,.F.);
#1117=EDGE_CURVE('',#870,#874,#134,.F.);
#1118=EDGE_CURVE('',#871,#875,#135,.T.);
#1119=EDGE_CURVE('',#875,#873,#136,.T.);
#1120=EDGE_CURVE('',#876,#877,#256,.T.);
#1121=EDGE_CURVE('',#872,#876,#137,.F.);
#1122=EDGE_CURVE('',#873,#877,#138,.T.);
#1123=EDGE_CURVE('',#878,#879,#257,.T.);
#1124=EDGE_CURVE('',#880,#878,#139,.F.);
#1125=EDGE_CURVE('',#876,#880,#140,.F.);
#1126=EDGE_CURVE('',#877,#881,#141,.T.);
#1127=EDGE_CURVE('',#881,#879,#142,.F.);
#1128=EDGE_CURVE('',#882,#883,#143,.T.);
#1129=EDGE_CURVE('',#883,#884,#712,.T.);
#1130=EDGE_CURVE('',#884,#885,#144,.T.);
#1131=EDGE_CURVE('',#885,#886,#145,.T.);
#1132=EDGE_CURVE('',#886,#887,#146,.T.);
#1133=EDGE_CURVE('',#887,#888,#147,.T.);
#1134=EDGE_CURVE('',#888,#889,#148,.T.);
#1135=EDGE_CURVE('',#889,#890,#149,.T.);
#1136=EDGE_CURVE('',#890,#891,#150,.T.);
#1137=EDGE_CURVE('',#891,#892,#151,.T.);
#1138=EDGE_CURVE('',#892,#893,#152,.T.);
#1139=EDGE_CURVE('',#894,#893,#713,.T.);
#1140=EDGE_CURVE('',#894,#895,#153,.T.);
#1141=EDGE_CURVE('',#895,#896,#154,.T.);
#1142=EDGE_CURVE('',#896,#897,#155,.T.);
#1143=EDGE_CURVE('',#897,#898,#156,.T.);
#1144=EDGE_CURVE('',#898,#899,#157,.T.);
#1145=EDGE_CURVE('',#899,#900,#158,.T.);
#1146=EDGE_CURVE('',#900,#901,#159,.T.);
#1147=EDGE_CURVE('',#901,#882,#160,.T.);
#1148=EDGE_CURVE('',#879,#902,#161,.F.);
#1149=EDGE_CURVE('',#903,#902,#714,.T.);
#1150=EDGE_CURVE('',#878,#903,#162,.F.);
#1151=EDGE_CURVE('',#893,#903,#163,.T.);
#1152=EDGE_CURVE('',#861,#884,#164,.T.);
#1153=EDGE_CURVE('',#884,#904,#715,.T.);
#1154=EDGE_CURVE('',#904,#905,#716,.T.);
#1155=EDGE_CURVE('',#905,#862,#165,.T.);
#1156=EDGE_CURVE('',#906,#894,#166,.T.);
#1157=EDGE_CURVE('',#902,#906,#167,.T.);
#1158=EDGE_CURVE('',#905,#883,#168,.T.);
#1159=EDGE_CURVE('',#904,#907,#717,.T.);
#1160=EDGE_CURVE('',#907,#907,#718,.T.);
#1161=EDGE_CURVE('',#908,#908,#719,.T.);
#1162=EDGE_CURVE('',#909,#909,#720,.T.);
#1163=EDGE_CURVE('',#909,#908,#258,.T.);
#1164=EDGE_CURVE('',#909,#910,#259,.T.);
#1165=EDGE_CURVE('',#910,#910,#721,.T.);
#1166=EDGE_CURVE('',#911,#911,#722,.T.);
#1167=EDGE_CURVE('',#912,#912,#723,.T.);
#1168=EDGE_CURVE('',#912,#911,#260,.T.);
#1169=EDGE_CURVE('',#913,#913,#724,.T.);
#1170=EDGE_CURVE('',#907,#913,#261,.T.);
#1541=ORIENTED_EDGE('',*,*,#1099,.F.);
#1542=ORIENTED_EDGE('',*,*,#1100,.F.);
#1543=ORIENTED_EDGE('',*,*,#1101,.F.);
#1544=ORIENTED_EDGE('',*,*,#1102,.T.);
#1545=ORIENTED_EDGE('',*,*,#1103,.F.);
#1546=ORIENTED_EDGE('',*,*,#1104,.F.);
#1547=ORIENTED_EDGE('',*,*,#1105,.F.);
#1548=ORIENTED_EDGE('',*,*,#1099,.T.);
#1549=ORIENTED_EDGE('',*,*,#1106,.T.);
#1550=ORIENTED_EDGE('',*,*,#1107,.F.);
#1551=ORIENTED_EDGE('',*,*,#1108,.F.);
#1552=ORIENTED_EDGE('',*,*,#1109,.F.);
#1553=ORIENTED_EDGE('',*,*,#1103,.T.);
#1554=ORIENTED_EDGE('',*,*,#1110,.T.);
#1555=ORIENTED_EDGE('',*,*,#1111,.T.);
#1556=ORIENTED_EDGE('',*,*,#1112,.F.);
#1557=ORIENTED_EDGE('',*,*,#1113,.F.);
#1558=ORIENTED_EDGE('',*,*,#1107,.T.);
#1559=ORIENTED_EDGE('',*,*,#1114,.T.);
#1560=ORIENTED_EDGE('',*,*,#1115,.F.);
#1561=ORIENTED_EDGE('',*,*,#1116,.F.);
#1562=ORIENTED_EDGE('',*,*,#1117,.F.);
#1563=ORIENTED_EDGE('',*,*,#1112,.T.);
#1564=ORIENTED_EDGE('',*,*,#1118,.T.);
#1565=ORIENTED_EDGE('',*,*,#1119,.T.);
#1566=ORIENTED_EDGE('',*,*,#1120,.F.);
#1567=ORIENTED_EDGE('',*,*,#1121,.F.);
#1568=ORIENTED_EDGE('',*,*,#1115,.T.);
#1569=ORIENTED_EDGE('',*,*,#1122,.T.);
#1570=ORIENTED_EDGE('',*,*,#1123,.F.);
#1571=ORIENTED_EDGE('',*,*,#1124,.F.);
#1572=ORIENTED_EDGE('',*,*,#1125,.F.);
#1573=ORIENTED_EDGE('',*,*,#1120,.T.);
#1574=ORIENTED_EDGE('',*,*,#1126,.T.);
#1575=ORIENTED_EDGE('',*,*,#1127,.T.);
#1576=ORIENTED_EDGE('',*,*,#1128,.T.);
#1577=ORIENTED_EDGE('',*,*,#1129,.T.);
#1578=ORIENTED_EDGE('',*,*,#1130,.T.);
#1579=ORIENTED_EDGE('',*,*,#1131,.T.);
#1580=ORIENTED_EDGE('',*,*,#1132,.T.);
#1581=ORIENTED_EDGE('',*,*,#1133,.T.);
#1582=ORIENTED_EDGE('',*,*,#1134,.T.);
#1583=ORIENTED_EDGE('',*,*,#1135,.T.);
#1584=ORIENTED_EDGE('',*,*,#1136,.T.);
#1585=ORIENTED_EDGE('',*,*,#1137,.T.);
#1586=ORIENTED_EDGE('',*,*,#1138,.T.);
#1587=ORIENTED_EDGE('',*,*,#1139,.F.);
#1588=ORIENTED_EDGE('',*,*,#1140,.T.);
#1589=ORIENTED_EDGE('',*,*,#1141,.T.);
#1590=ORIENTED_EDGE('',*,*,#1142,.T.);
#1591=ORIENTED_EDGE('',*,*,#1143,.T.);
#1592=ORIENTED_EDGE('',*,*,#1144,.T.);
#1593=ORIENTED_EDGE('',*,*,#1145,.T.);
#1594=ORIENTED_EDGE('',*,*,#1146,.T.);
#1595=ORIENTED_EDGE('',*,*,#1147,.T.);
#1596=ORIENTED_EDGE('',*,*,#1123,.T.);
#1597=ORIENTED_EDGE('',*,*,#1148,.T.);
#1598=ORIENTED_EDGE('',*,*,#1149,.F.);
#1599=ORIENTED_EDGE('',*,*,#1150,.F.);
#1600=ORIENTED_EDGE('',*,*,#1151,.F.);
#1601=ORIENTED_EDGE('',*,*,#1138,.F.);
#1602=ORIENTED_EDGE('',*,*,#1137,.F.);
#1603=ORIENTED_EDGE('',*,*,#1136,.F.);
#1604=ORIENTED_EDGE('',*,*,#1135,.F.);
#1605=ORIENTED_EDGE('',*,*,#1134,.F.);
#1606=ORIENTED_EDGE('',*,*,#1133,.F.);
#1607=ORIENTED_EDGE('',*,*,#1132,.F.);
#1608=ORIENTED_EDGE('',*,*,#1131,.F.);
#1609=ORIENTED_EDGE('',*,*,#1130,.F.);
#1610=ORIENTED_EDGE('',*,*,#1152,.F.);
#1611=ORIENTED_EDGE('',*,*,#1100,.T.);
#1612=ORIENTED_EDGE('',*,*,#1105,.T.);
#1613=ORIENTED_EDGE('',*,*,#1104,.T.);
#1614=ORIENTED_EDGE('',*,*,#1109,.T.);
#1615=ORIENTED_EDGE('',*,*,#1108,.T.);
#1616=ORIENTED_EDGE('',*,*,#1113,.T.);
#1617=ORIENTED_EDGE('',*,*,#1117,.T.);
#1618=ORIENTED_EDGE('',*,*,#1116,.T.);
#1619=ORIENTED_EDGE('',*,*,#1121,.T.);
#1620=ORIENTED_EDGE('',*,*,#1125,.T.);
#1621=ORIENTED_EDGE('',*,*,#1124,.T.);
#1622=ORIENTED_EDGE('',*,*,#1150,.T.);
#1623=ORIENTED_EDGE('',*,*,#1153,.T.);
#1624=ORIENTED_EDGE('',*,*,#1154,.T.);
#1625=ORIENTED_EDGE('',*,*,#1155,.T.);
#1626=ORIENTED_EDGE('',*,*,#1101,.T.);
#1627=ORIENTED_EDGE('',*,*,#1152,.T.);
#1628=ORIENTED_EDGE('',*,*,#1156,.F.);
#1629=ORIENTED_EDGE('',*,*,#1157,.F.);
#1630=ORIENTED_EDGE('',*,*,#1148,.F.);
#1631=ORIENTED_EDGE('',*,*,#1127,.F.);
#1632=ORIENTED_EDGE('',*,*,#1126,.F.);
#1633=ORIENTED_EDGE('',*,*,#1122,.F.);
#1634=ORIENTED_EDGE('',*,*,#1119,.F.);
#1635=ORIENTED_EDGE('',*,*,#1118,.F.);
#1636=ORIENTED_EDGE('',*,*,#1114,.F.);
#1637=ORIENTED_EDGE('',*,*,#1111,.F.);
#1638=ORIENTED_EDGE('',*,*,#1110,.F.);
#1639=ORIENTED_EDGE('',*,*,#1106,.F.);
#1640=ORIENTED_EDGE('',*,*,#1102,.F.);
#1641=ORIENTED_EDGE('',*,*,#1155,.F.);
#1642=ORIENTED_EDGE('',*,*,#1158,.T.);
#1643=ORIENTED_EDGE('',*,*,#1128,.F.);
#1644=ORIENTED_EDGE('',*,*,#1147,.F.);
#1645=ORIENTED_EDGE('',*,*,#1146,.F.);
#1646=ORIENTED_EDGE('',*,*,#1145,.F.);
#1647=ORIENTED_EDGE('',*,*,#1144,.F.);
#1648=ORIENTED_EDGE('',*,*,#1143,.F.);
#1649=ORIENTED_EDGE('',*,*,#1142,.F.);
#1650=ORIENTED_EDGE('',*,*,#1141,.F.);
#1651=ORIENTED_EDGE('',*,*,#1140,.F.);
#1652=ORIENTED_EDGE('',*,*,#1158,.F.);
#1653=ORIENTED_EDGE('',*,*,#1154,.F.);
#1654=ORIENTED_EDGE('',*,*,#1159,.T.);
#1655=ORIENTED_EDGE('',*,*,#1160,.T.);
#1656=ORIENTED_EDGE('',*,*,#1159,.F.);
#1657=ORIENTED_EDGE('',*,*,#1153,.F.);
#1658=ORIENTED_EDGE('',*,*,#1129,.F.);
#1659=ORIENTED_EDGE('',*,*,#1161,.F.);
#1660=ORIENTED_EDGE('',*,*,#1139,.T.);
#1661=ORIENTED_EDGE('',*,*,#1151,.T.);
#1662=ORIENTED_EDGE('',*,*,#1149,.T.);
#1663=ORIENTED_EDGE('',*,*,#1157,.T.);
#1664=ORIENTED_EDGE('',*,*,#1156,.T.);
#1665=ORIENTED_EDGE('',*,*,#1162,.F.);
#1666=ORIENTED_EDGE('',*,*,#1163,.T.);
#1667=ORIENTED_EDGE('',*,*,#1161,.T.);
#1668=ORIENTED_EDGE('',*,*,#1163,.F.);
#1669=ORIENTED_EDGE('',*,*,#1162,.T.);
#1670=ORIENTED_EDGE('',*,*,#1164,.T.);
#1671=ORIENTED_EDGE('',*,*,#1165,.F.);
#1672=ORIENTED_EDGE('',*,*,#1164,.F.);
#1673=ORIENTED_EDGE('',*,*,#1165,.T.);
#1674=ORIENTED_EDGE('',*,*,#1166,.F.);
#1675=ORIENTED_EDGE('',*,*,#1167,.F.);
#1676=ORIENTED_EDGE('',*,*,#1168,.T.);
#1677=ORIENTED_EDGE('',*,*,#1166,.T.);
#1678=ORIENTED_EDGE('',*,*,#1168,.F.);
#1679=ORIENTED_EDGE('',*,*,#1167,.T.);
#1680=ORIENTED_EDGE('',*,*,#1169,.F.);
#1681=ORIENTED_EDGE('',*,*,#1160,.F.);
#1682=ORIENTED_EDGE('',*,*,#1170,.T.);
#1683=ORIENTED_EDGE('',*,*,#1169,.T.);
#1684=ORIENTED_EDGE('',*,*,#1170,.F.);
#1716=PLANE('',#2100);
#1717=PLANE('',#2106);
#1718=PLANE('',#2112);
#1719=PLANE('',#2116);
#1720=PLANE('',#2117);
#1805=ADVANCED_FACE('',(#483),#358,.T.);
#1806=ADVANCED_FACE('',(#484),#359,.T.);
#1807=ADVANCED_FACE('',(#485),#360,.T.);
#1808=ADVANCED_FACE('',(#486),#361,.T.);
#1809=ADVANCED_FACE('',(#487),#362,.T.);
#1810=ADVANCED_FACE('',(#488),#363,.T.);
#1811=ADVANCED_FACE('',(#489),#364,.T.);
#1812=ADVANCED_FACE('',(#490),#365,.T.);
#1813=ADVANCED_FACE('',(#491),#366,.T.);
#1814=ADVANCED_FACE('',(#492),#53,.F.);
#1815=ADVANCED_FACE('',(#493),#1716,.T.);
#1816=ADVANCED_FACE('',(#494),#54,.F.);
#1817=ADVANCED_FACE('',(#495),#173,.F.);
#1818=ADVANCED_FACE('',(#496,#397),#1717,.T.);
#1819=ADVANCED_FACE('',(#497),#367,.T.);
#1820=ADVANCED_FACE('',(#498),#50,.T.);
#1821=ADVANCED_FACE('',(#499,#398),#1718,.T.);
#1822=ADVANCED_FACE('',(#500),#368,.F.);
#1823=ADVANCED_FACE('',(#501),#1719,.T.);
#1824=ADVANCED_FACE('',(#502),#1720,.T.);
#1825=ADVANCED_FACE('',(#503),#369,.T.);
#1833=CLOSED_SHELL('',(#1805,#1806,#1807,#1808,#1809,#1810,#1811,#1812,
#1813,#1814,#1815,#1816,#1817,#1818,#1819,#1820,#1821,#1822,#1823,#1824,
#1825));
#2086=AXIS2_PLACEMENT_3D('',#8670,#2499,#2500);
#2087=AXIS2_PLACEMENT_3D('',#8671,#2501,#2502);
#2088=AXIS2_PLACEMENT_3D('',#8685,#2504,#2505);
#2089=AXIS2_PLACEMENT_3D('',#8780,#2506,#2507);
#2090=AXIS2_PLACEMENT_3D('',#9126,#2509,#2510);
#2091=AXIS2_PLACEMENT_3D('',#9475,#2512,#2513);
#2092=AXIS2_PLACEMENT_3D('',#9799,#2515,#2516);
#2093=AXIS2_PLACEMENT_3D('',#10143,#2518,#2519);
#2094=AXIS2_PLACEMENT_3D('',#10471,#2521,#2522);
#2095=AXIS2_PLACEMENT_3D('',#10807,#2524,#2525);
#2096=AXIS2_PLACEMENT_3D('',#10875,#2526,#2527);
#2097=AXIS2_PLACEMENT_3D('',#12285,#2528,#2529);
#2098=AXIS2_PLACEMENT_3D('',#13457,#2530,#2531);
#2099=AXIS2_PLACEMENT_3D('',#13602,#2532,#2533);
#2100=AXIS2_PLACEMENT_3D('',#14097,#2534,#2535);
#2101=AXIS2_PLACEMENT_3D('',#14099,#2536,#2537);
#2102=AXIS2_PLACEMENT_3D('',#14101,#2538,#2539);
#2103=AXIS2_PLACEMENT_3D('',#14489,#2540,#2541);
#2104=AXIS2_PLACEMENT_3D('',#14491,#2542,#2543);
#2105=AXIS2_PLACEMENT_3D('',#14492,#2544,#2545);
#2106=AXIS2_PLACEMENT_3D('',#14493,#2546,#2547);
#2107=AXIS2_PLACEMENT_3D('',#14495,#2548,#2549);
#2108=AXIS2_PLACEMENT_3D('',#14496,#2550,#2551);
#2109=AXIS2_PLACEMENT_3D('',#14498,#2552,#2553);
#2110=AXIS2_PLACEMENT_3D('',#14500,#2555,#2556);
#2111=AXIS2_PLACEMENT_3D('',#14503,#2558,#2559);
#2112=AXIS2_PLACEMENT_3D('',#14504,#2560,#2561);
#2113=AXIS2_PLACEMENT_3D('',#14506,#2562,#2563);
#2114=AXIS2_PLACEMENT_3D('',#14507,#2564,#2565);
#2115=AXIS2_PLACEMENT_3D('',#14509,#2566,#2567);
#2116=AXIS2_PLACEMENT_3D('',#14511,#2569,#2570);
#2117=AXIS2_PLACEMENT_3D('',#14512,#2571,#2572);
#2118=AXIS2_PLACEMENT_3D('',#14514,#2573,#2574);
#2119=AXIS2_PLACEMENT_3D('',#14515,#2575,#2576);
#2499=DIRECTION('axis',(0.,0.,1.));
#2500=DIRECTION('refdir',(1.,0.,0.));
#2501=DIRECTION('center_axis',(0.,0.,1.));
#2502=DIRECTION('ref_axis',(0.983063241079179,0.183266647371803,0.));
#2503=DIRECTION('',(0.,0.,-1.));
#2504=DIRECTION('center_axis',(0.,0.,-1.));
#2505=DIRECTION('ref_axis',(1.,2.64874037426574E-14,0.));
#2506=DIRECTION('center_axis',(0.,0.,1.));
#2507=DIRECTION('ref_axis',(0.835702322852818,-0.549182690530578,0.));
#2508=DIRECTION('',(0.,0.,-1.));
#2509=DIRECTION('center_axis',(0.,0.,1.));
#2510=DIRECTION('ref_axis',(0.835702322852818,-0.549182690530578,0.));
#2511=DIRECTION('',(0.,0.,-1.));
#2512=DIRECTION('center_axis',(0.,0.,1.));
#2513=DIRECTION('ref_axis',(0.835702322852818,-0.549182690530578,0.));
#2514=DIRECTION('',(0.,0.,-1.));
#2515=DIRECTION('center_axis',(0.,0.,1.));
#2516=DIRECTION('ref_axis',(0.835702322852818,-0.549182690530578,0.));
#2517=DIRECTION('',(0.,0.,-1.));
#2518=DIRECTION('center_axis',(0.,0.,1.));
#2519=DIRECTION('ref_axis',(0.835702322852818,-0.549182690530578,0.));
#2520=DIRECTION('',(0.,0.,-1.));
#2521=DIRECTION('center_axis',(0.,0.,1.));
#2522=DIRECTION('ref_axis',(0.835702322852818,-0.549182690530578,0.));
#2523=DIRECTION('',(0.,0.,-1.));
#2524=DIRECTION('center_axis',(0.,0.,1.));
#2525=DIRECTION('ref_axis',(1.,0.,0.));
#2526=DIRECTION('center_axis',(0.,0.,1.));
#2527=DIRECTION('ref_axis',(1.,0.,0.));
#2528=DIRECTION('center_axis',(0.,0.,1.));
#2529=DIRECTION('ref_axis',(1.,0.,0.));
#2530=DIRECTION('center_axis',(0.,0.,1.));
#2531=DIRECTION('ref_axis',(0.637974576266918,-0.770057426454058,0.));
#2532=DIRECTION('center_axis',(0.,0.,1.));
#2533=DIRECTION('ref_axis',(1.,2.64874037426574E-14,0.));
#2534=DIRECTION('center_axis',(0.,0.,1.));
#2535=DIRECTION('ref_axis',(1.,0.,0.));
#2536=DIRECTION('center_axis',(0.,0.,1.));
#2537=DIRECTION('ref_axis',(1.,0.,0.));
#2538=DIRECTION('center_axis',(0.,0.,1.));
#2539=DIRECTION('ref_axis',(1.,0.,0.));
#2540=DIRECTION('center_axis',(0.,0.,1.));
#2541=DIRECTION('ref_axis',(1.,0.,0.));
#2542=DIRECTION('center_axis',(-1.22464679914735E-16,1.,0.));
#2543=DIRECTION('ref_axis',(-1.,-1.22464679914735E-16,0.));
#2544=DIRECTION('center_axis',(0.,0.,1.));
#2545=DIRECTION('ref_axis',(1.,0.,0.));
#2546=DIRECTION('center_axis',(0.,0.,-1.));
#2547=DIRECTION('ref_axis',(-1.,0.,0.));
#2548=DIRECTION('center_axis',(0.,0.,1.));
#2549=DIRECTION('ref_axis',(1.,0.,0.));
#2550=DIRECTION('center_axis',(0.,0.,1.));
#2551=DIRECTION('ref_axis',(1.,0.,0.));
#2552=DIRECTION('center_axis',(0.,0.,1.));
#2553=DIRECTION('ref_axis',(1.,0.,0.));
#2554=DIRECTION('',(0.,0.,-1.));
#2555=DIRECTION('center_axis',(0.,0.,-1.));
#2556=DIRECTION('ref_axis',(1.,0.,0.));
#2557=DIRECTION('',(0.78750500100757,-9.64415478796454E-17,0.616308261658131));
#2558=DIRECTION('center_axis',(0.,0.,1.));
#2559=DIRECTION('ref_axis',(1.,0.,0.));
#2560=DIRECTION('center_axis',(0.,0.,1.));
#2561=DIRECTION('ref_axis',(1.,0.,0.));
#2562=DIRECTION('center_axis',(0.,0.,1.));
#2563=DIRECTION('ref_axis',(1.,0.,0.));
#2564=DIRECTION('center_axis',(0.,0.,1.));
#2565=DIRECTION('ref_axis',(1.,0.,0.));
#2566=DIRECTION('center_axis',(0.,0.,1.));
#2567=DIRECTION('ref_axis',(1.,0.,0.));
#2568=DIRECTION('',(0.,0.,1.));
#2569=DIRECTION('center_axis',(0.,0.,1.));
#2570=DIRECTION('ref_axis',(1.,0.,0.));
#2571=DIRECTION('center_axis',(0.,0.,-1.));
#2572=DIRECTION('ref_axis',(-1.,0.,0.));
#2573=DIRECTION('center_axis',(0.,0.,1.));
#2574=DIRECTION('ref_axis',(1.,0.,0.));
#2575=DIRECTION('center_axis',(0.,0.,1.));
#2576=DIRECTION('ref_axis',(1.,0.,0.));
#2577=DIRECTION('',(0.,0.,-1.));
#8670=CARTESIAN_POINT('',(0.,0.,0.));
#8671=CARTESIAN_POINT('Origin',(0.,0.,89.2710285354474));
#8672=CARTESIAN_POINT('',(-1.66796412351461,1.09611534438488,91.3549851603904));
#8673=CARTESIAN_POINT('',(-1.66701720873947,1.09548217158769,91.1951011757363));
#8674=CARTESIAN_POINT('',(-1.66701720851066,1.09548217193587,89.2710285354474));
#8675=CARTESIAN_POINT('',(-1.16224713396736,-1.62528722506882,90.7501273547608));
#8676=CARTESIAN_POINT('Ctrl Pts',(-1.16224713396736,-1.62528722506882,90.7501273547608));
#8677=CARTESIAN_POINT('Ctrl Pts',(-0.658524710503023,-1.98155496728916,
90.7896669606139));
#8678=CARTESIAN_POINT('Ctrl Pts',(0.758122744768261,-2.20830555489497,90.8716287779614));
#8679=CARTESIAN_POINT('Ctrl Pts',(2.27985988398632,-0.606850097788344,90.9960128068036));
#8680=CARTESIAN_POINT('Ctrl Pts',(1.74311916661052,1.59020182115508,91.1232794412872));
#8681=CARTESIAN_POINT('Ctrl Pts',(-0.267372268586595,2.28195004315838,91.2429368924828));
#8682=CARTESIAN_POINT('Ctrl Pts',(-1.36442438513313,1.54816875793513,91.3201721321838));
#8683=CARTESIAN_POINT('Ctrl Pts',(-1.66796412351456,1.09611534438494,91.3549851603904));
#8684=CARTESIAN_POINT('',(1.16034898466941,-1.62253437445148,90.7500736540522));
#8685=CARTESIAN_POINT('Origin',(0.,0.,90.7500736540522));
#8686=CARTESIAN_POINT('Ctrl Pts',(1.16034898466941,-1.62253437445149,90.7500736540522));
#8687=CARTESIAN_POINT('Ctrl Pts',(1.17314904347898,-1.61338046346059,90.7510781037149));
#8688=CARTESIAN_POINT('Ctrl Pts',(1.18584074592424,-1.6040751090438,90.7520741371569));
#8689=CARTESIAN_POINT('Ctrl Pts',(1.21629818685645,-1.58118511405926,90.754467732357));
#8690=CARTESIAN_POINT('Ctrl Pts',(1.23394844976023,-1.56744982135387,90.7558576320957));
#8691=CARTESIAN_POINT('Ctrl Pts',(1.31553677040832,-1.50172597808865,90.7623129882304));
#8692=CARTESIAN_POINT('Ctrl Pts',(1.37644870744073,-1.44610123818527,90.767223643896));
#8693=CARTESIAN_POINT('Ctrl Pts',(1.4998823884772,-1.31849477652871,90.7777600138677));
#8694=CARTESIAN_POINT('Ctrl Pts',(1.56103893598951,-1.24548474182317,90.783368483509));
#8695=CARTESIAN_POINT('Ctrl Pts',(1.64770706696334,-1.12555848729566,90.7923069388478));
#8696=CARTESIAN_POINT('Ctrl Pts',(1.67694569491042,-1.08151422923847,90.7955369743538));
#8697=CARTESIAN_POINT('Ctrl Pts',(1.71942535119665,-1.0116523248723,90.8006218826066));
#8698=CARTESIAN_POINT('Ctrl Pts',(1.73391115998772,-0.986618432168437,90.8024365599979));
#8699=CARTESIAN_POINT('Ctrl Pts',(1.76046404777739,-0.938338619060236,90.8059284417133));
#8700=CARTESIAN_POINT('Ctrl Pts',(1.77262762735366,-0.915152568354784,90.807602042306));
#8701=CARTESIAN_POINT('Ctrl Pts',(1.80019886612251,-0.859983450464937,90.8115805946841));
#8702=CARTESIAN_POINT('Ctrl Pts',(1.81521562543524,-0.827816085726226,90.8138976352077));
#8703=CARTESIAN_POINT('Ctrl Pts',(1.87080253475281,-0.699948587126537,90.8231081504074));
#8704=CARTESIAN_POINT('Ctrl Pts',(1.90472058368382,-0.601551410959497,90.830206909549));
#8705=CARTESIAN_POINT('Ctrl Pts',(1.95976016705419,-0.389421489844373,90.8454705237484));
#8706=CARTESIAN_POINT('Ctrl Pts',(1.97898141212054,-0.275574199166582,90.8536406166416));
#8707=CARTESIAN_POINT('Ctrl Pts',(1.99134355319383,-0.122628503092087,90.8642704219524));
#8708=CARTESIAN_POINT('Ctrl Pts',(1.99332693643587,-0.0844686511425707,
90.8668926891416));
#8709=CARTESIAN_POINT('Ctrl Pts',(1.99486942905621,-0.0179928339290739,
90.8713866626133));
#8710=CARTESIAN_POINT('Ctrl Pts',(1.99492402917294,0.0103002136719869,90.8732759972948));
#8711=CARTESIAN_POINT('Ctrl Pts',(1.99408286963858,0.0537762631839919,90.8761345895388));
#8712=CARTESIAN_POINT('Ctrl Pts',(1.99361544708385,0.0689627639697828,90.8771247363347));
#8713=CARTESIAN_POINT('Ctrl Pts',(1.99241544078782,0.0973855824031539,90.8789604738342));
#8714=CARTESIAN_POINT('Ctrl Pts',(1.9917244097925,0.110621563021882,90.8798080400829));
#8715=CARTESIAN_POINT('Ctrl Pts',(1.98964201244626,0.144096074229982,90.8819342362994));
#8716=CARTESIAN_POINT('Ctrl Pts',(1.98807379735177,0.164321854025372,90.8832031574842));
#8717=CARTESIAN_POINT('Ctrl Pts',(1.97943171953755,0.257345723261733,90.8889816870942));
#8718=CARTESIAN_POINT('Ctrl Pts',(1.96866533397623,0.329751118414626,90.8933178064752));
#8719=CARTESIAN_POINT('Ctrl Pts',(1.92307623920396,0.551666289816138,90.9065569507854));
#8720=CARTESIAN_POINT('Ctrl Pts',(1.87498178573657,0.697854286959789,90.9152481262817));
#8721=CARTESIAN_POINT('Ctrl Pts',(1.79306404781305,0.875041254201998,90.9270025640284));
#8722=CARTESIAN_POINT('Ctrl Pts',(1.77432955902559,0.91243087898068,90.9295542663064));
#8723=CARTESIAN_POINT('Ctrl Pts',(1.74273613999407,0.970825807503868,90.9336728607101));
#8724=CARTESIAN_POINT('Ctrl Pts',(1.73063888479634,0.992230297683102,90.9352119720363));
#8725=CARTESIAN_POINT('Ctrl Pts',(1.70665945207541,1.03288556610933,90.9381957212619));
#8726=CARTESIAN_POINT('Ctrl Pts',(1.69483929904236,1.0521685967344,90.9396378370712));
#8727=CARTESIAN_POINT('Ctrl Pts',(1.66620630845414,1.09714479854448,90.9430677896392));
#8728=CARTESIAN_POINT('Ctrl Pts',(1.64912349622755,1.12265831047906,90.945065945843));
#8729=CARTESIAN_POINT('Ctrl Pts',(1.58692178572088,1.21107315235884,90.9521825386533));
#8730=CARTESIAN_POINT('Ctrl Pts',(1.53874260466519,1.27172618677324,90.9574205389424));
#8731=CARTESIAN_POINT('Ctrl Pts',(1.40000286675475,1.42692845832341,90.9717871906183));
#8732=CARTESIAN_POINT('Ctrl Pts',(1.30346770152365,1.51561912863029,90.981090801111));
#8733=CARTESIAN_POINT('Ctrl Pts',(1.16757685224896,1.61781736669191,90.9928981266502));
#8734=CARTESIAN_POINT('Ctrl Pts',(1.13551000684884,1.64048350387597,90.9955994120794));
#8735=CARTESIAN_POINT('Ctrl Pts',(1.07911858449896,1.67789685365977,91.000179808331));
#8736=CARTESIAN_POINT('Ctrl Pts',(1.05510942687394,1.69309747947808,91.0020792901247));
#8737=CARTESIAN_POINT('Ctrl Pts',(1.01826336814747,1.71533702009854,91.0049089206537));
#8738=CARTESIAN_POINT('Ctrl Pts',(1.00566121657515,1.7227556231055,91.0058619639392));
#8739=CARTESIAN_POINT('Ctrl Pts',(0.981510112217735,1.7366174882257,91.007658760689));
#8740=CARTESIAN_POINT('Ctrl Pts',(0.969976617984684,1.74308570822472,91.0085042286633));
#8741=CARTESIAN_POINT('Ctrl Pts',(0.941019432878275,1.75894905954882,91.0105978384044));
#8742=CARTESIAN_POINT('Ctrl Pts',(0.923518224841293,1.76820064682644,91.0118372017672));
#8743=CARTESIAN_POINT('Ctrl Pts',(0.851419248788649,1.80495141625567,91.0168495666815));
#8744=CARTESIAN_POINT('Ctrl Pts',(0.795704518339729,1.83019672626533,91.0205071714274));
#8745=CARTESIAN_POINT('Ctrl Pts',(0.619851178851142,1.9003269259806,91.0316569500777));
#8746=CARTESIAN_POINT('Ctrl Pts',(0.496488873647193,1.93622270316455,91.0389470664234));
#8747=CARTESIAN_POINT('Ctrl Pts',(0.322734561577925,1.96906989514896,91.0493616947144));
#8748=CARTESIAN_POINT('Ctrl Pts',(0.27462470607308,1.97635388295567,91.052257680539));
#8749=CARTESIAN_POINT('Ctrl Pts',(0.186967611432868,1.98636295532512,91.0575979725878));
#8750=CARTESIAN_POINT('Ctrl Pts',(0.147513622281268,1.98968190605767,91.0600246697606));
#8751=CARTESIAN_POINT('Ctrl Pts',(0.0829610438155578,1.99318169362283,91.0640471674946));
#8752=CARTESIAN_POINT('Ctrl Pts',(0.057910770585411,1.99406671158738,91.0656208336947));
#8753=CARTESIAN_POINT('Ctrl Pts',(0.00878138519335234,1.99487592846905,
91.0687351396053));
#8754=CARTESIAN_POINT('Ctrl Pts',(-0.015292867076133,1.9948366167766,91.0702743640615));
#8755=CARTESIAN_POINT('Ctrl Pts',(-0.0747348504066648,1.99366350093632,
91.0741097205133));
#8756=CARTESIAN_POINT('Ctrl Pts',(-0.110083193392411,1.99202431754119,91.076421073309));
#8757=CARTESIAN_POINT('Ctrl Pts',(-0.286286550827132,1.97914925676344,91.0881016207235));
#8758=CARTESIAN_POINT('Ctrl Pts',(-0.425692903973189,1.95391031228548,91.0978923727981));
#8759=CARTESIAN_POINT('Ctrl Pts',(-0.645225208120578,1.88954278972236,91.1138013561186));
#8760=CARTESIAN_POINT('Ctrl Pts',(-0.727505616938371,1.85941533891063,91.1198722607316));
#8761=CARTESIAN_POINT('Ctrl Pts',(-0.830580501290487,1.81378008056937,91.1274266453653));
#8762=CARTESIAN_POINT('Ctrl Pts',(-0.85342091740846,1.80314586879498,91.1290969117543));
#8763=CARTESIAN_POINT('Ctrl Pts',(-0.889209964017591,1.78565047319742,91.1317013172632));
#8764=CARTESIAN_POINT('Ctrl Pts',(-0.902294280195474,1.77907476977465,91.1326507195481));
#8765=CARTESIAN_POINT('Ctrl Pts',(-0.926546287624919,1.76655019596719,91.1344036387738));
#8766=CARTESIAN_POINT('Ctrl Pts',(-0.937731827196888,1.76063813753127,91.1352093013974));
#8767=CARTESIAN_POINT('Ctrl Pts',(-0.968624676250945,1.7439319511873,91.1374286153975));
#8768=CARTESIAN_POINT('Ctrl Pts',(-0.988207730889158,1.73291026721569,91.1388288278613));
#8769=CARTESIAN_POINT('Ctrl Pts',(-1.1195732026294,1.65602415182174,91.148205074385));
#8770=CARTESIAN_POINT('Ctrl Pts',(-1.22489847674672,1.5797126952943,91.1556545804726));
#8771=CARTESIAN_POINT('Ctrl Pts',(-1.40112681167,1.42373319352022,91.1693229533324));
#8772=CARTESIAN_POINT('Ctrl Pts',(-1.47449274185012,1.34760555965701,91.1754898202527));
#8773=CARTESIAN_POINT('Ctrl Pts',(-1.56504129653026,1.23735627940756,91.1841572987751));
#8774=CARTESIAN_POINT('Ctrl Pts',(-1.58778915038505,1.20802738662344,91.186439273085));
#8775=CARTESIAN_POINT('Ctrl Pts',(-1.62419313020345,1.15828582795485,91.1902829347968));
#8776=CARTESIAN_POINT('Ctrl Pts',(-1.63831456820407,1.13822435096106,91.1918262475269));
#8777=CARTESIAN_POINT('Ctrl Pts',(-1.6570976652941,1.11046640179257,91.1939544134049));
#8778=CARTESIAN_POINT('Ctrl Pts',(-1.66208285755213,1.10299087283048,91.1945268467398));
#8779=CARTESIAN_POINT('Ctrl Pts',(-1.66701720873947,1.09548217158769,91.1951011757363));
#8780=CARTESIAN_POINT('Origin',(0.,0.,89.2710285354474));
#8781=CARTESIAN_POINT('',(-1.66701720851066,1.09548217193587,92.1551526428301));
#8782=CARTESIAN_POINT('',(-1.66701737487201,1.09548191878042,91.9972724317));
#8783=CARTESIAN_POINT('',(-1.66701720851066,1.09548217193587,89.2710285354474));
#8784=CARTESIAN_POINT('',(-1.99466808022928,0.0010228270418267,91.429118747959));
#8785=CARTESIAN_POINT('Ctrl Pts',(-1.9947497379454,0.00102248069035476,
91.429118772657));
#8786=CARTESIAN_POINT('Ctrl Pts',(-1.99478604894113,-0.06981636243393,91.4336193689785));
#8787=CARTESIAN_POINT('Ctrl Pts',(-1.99104450452175,-0.140650429119896,
91.4381199653));
#8788=CARTESIAN_POINT('Ctrl Pts',(-1.98355300646027,-0.211056942701271,
91.4426205616215));
#8789=CARTESIAN_POINT('Ctrl Pts',(-1.97605859417038,-0.281490844751671,
91.4471229086964));
#8790=CARTESIAN_POINT('Ctrl Pts',(-1.96481138056007,-0.351496395942167,
91.4516252557713));
#8791=CARTESIAN_POINT('Ctrl Pts',(-1.94989092191128,-0.420657764873042,
91.4561276028462));
#8792=CARTESIAN_POINT('Ctrl Pts',(-1.93494812103891,-0.489922697561851,
91.4606366918348));
#8793=CARTESIAN_POINT('Ctrl Pts',(-1.91632119468705,-0.55834046408667,91.4651457808234));
#8794=CARTESIAN_POINT('Ctrl Pts',(-1.89414034210309,-0.62550773529796,91.469654869812));
#8795=CARTESIAN_POINT('Ctrl Pts',(-1.87194157105775,-0.69272926655858,91.474167601399));
#8796=CARTESIAN_POINT('Ctrl Pts',(-1.84618332850722,-0.758697853304446,
91.478680332986));
#8797=CARTESIAN_POINT('Ctrl Pts',(-1.81704398589159,-0.823030203476888,
91.4831930645729));
#8798=CARTESIAN_POINT('Ctrl Pts',(-1.7878445441515,-0.887495237422273,91.4877151035496));
#8799=CARTESIAN_POINT('Ctrl Pts',(-1.75525029179399,-0.950316877422571,
91.4922371425263));
#8800=CARTESIAN_POINT('Ctrl Pts',(-1.71948537196905,-1.01113679494144,91.4967591815029));
#8801=CARTESIAN_POINT('Ctrl Pts',(-1.6975505786476,-1.04843793603541,91.499532569248));
#8802=CARTESIAN_POINT('Ctrl Pts',(-1.67442402322111,-1.08498670633101,91.502305956993));
#8803=CARTESIAN_POINT('Ctrl Pts',(-1.65016502050455,-1.12070645916012,91.505079344738));
#8804=CARTESIAN_POINT('Ctrl Pts',(-1.61120871825323,-1.178066998825,91.5095329874751));
#8805=CARTESIAN_POINT('Ctrl Pts',(-1.56918069144311,-1.23350778322811,91.5139866302121));
#8806=CARTESIAN_POINT('Ctrl Pts',(-1.52429668529752,-1.28668068210065,91.5184402729491));
#8807=CARTESIAN_POINT('Ctrl Pts',(-1.47948026045186,-1.33977351918871,91.5228872098906));
#8808=CARTESIAN_POINT('Ctrl Pts',(-1.43181670431929,-1.39060487695719,91.5273341468322));
#8809=CARTESIAN_POINT('Ctrl Pts',(-1.38156468533898,-1.43885599791091,91.5317810837737));
#8810=CARTESIAN_POINT('Ctrl Pts',(-1.33137204957049,-1.48705010012997,91.5362227657344));
#8811=CARTESIAN_POINT('Ctrl Pts',(-1.27859737758551,-1.53266968386654,91.540664447695));
#8812=CARTESIAN_POINT('Ctrl Pts',(-1.22353800024705,-1.57543083772391,91.5451061296557));
#8813=CARTESIAN_POINT('Ctrl Pts',(-1.16851345644702,-1.61816493856382,91.5495450015682));
#8814=CARTESIAN_POINT('Ctrl Pts',(-1.11120746048929,-1.65804389727924,91.5539838734808));
#8815=CARTESIAN_POINT('Ctrl Pts',(-1.05195126414642,-1.69482332423198,91.5584227453934));
#8816=CARTESIAN_POINT('Ctrl Pts',(-0.992712410512399,-1.73159198682702,
91.5628603181664));
#8817=CARTESIAN_POINT('Ctrl Pts',(-0.931524905373209,-1.76526266036815,
91.5672978909395));
#8818=CARTESIAN_POINT('Ctrl Pts',(-0.868748401194261,-1.7956346448881,91.5717354637126));
#8819=CARTESIAN_POINT('Ctrl Pts',(-0.80596892783183,-1.82600806593269,91.5761732463726));
#8820=CARTESIAN_POINT('Ctrl Pts',(-0.741600748042559,-1.85308227707946,
91.5806110290327));
#8821=CARTESIAN_POINT('Ctrl Pts',(-0.676025878173996,-1.87670364590126,
91.5850488116927));
#8822=CARTESIAN_POINT('Ctrl Pts',(-0.610381473243961,-1.90035006263144,
91.5894913001415));
#8823=CARTESIAN_POINT('Ctrl Pts',(-0.543528285864839,-1.92053616273836,
91.5939337885904));
#8824=CARTESIAN_POINT('Ctrl Pts',(-0.475865064633682,-1.937157712413,91.5983762770393));
#8825=CARTESIAN_POINT('Ctrl Pts',(-0.408162420292586,-1.95378894642085,
91.6028213538471));
#8826=CARTESIAN_POINT('Ctrl Pts',(-0.339649283885739,-1.96685140454597,
91.607266430655));
#8827=CARTESIAN_POINT('Ctrl Pts',(-0.270733451114978,-1.97629222559503,
91.6117115074629));
#8828=CARTESIAN_POINT('Ctrl Pts',(-0.201696956710912,-1.98574957615323,
91.616164366956));
#8829=CARTESIAN_POINT('Ctrl Pts',(-0.132256846416913,-1.99157259079294,
91.620617226449));
#8830=CARTESIAN_POINT('Ctrl Pts',(-0.0628240830250762,-1.99376044124967,
91.625070085942));
#8831=CARTESIAN_POINT('Ctrl Pts',(-0.0250067825285576,-1.99495207750497,
91.6274953837019));
#8832=CARTESIAN_POINT('Ctrl Pts',(0.0128083646673936,-1.99506623435737,
91.6299206814618));
#8833=CARTESIAN_POINT('Ctrl Pts',(0.0505556209234334,-1.99410924768255,
91.6323459792217));
#8834=CARTESIAN_POINT('Ctrl Pts',(0.11987161759915,-1.99235191505098,91.6367995991172));
#8835=CARTESIAN_POINT('Ctrl Pts',(0.189233471968186,-1.98697260991991,91.6412532190127));
#8836=CARTESIAN_POINT('Ctrl Pts',(0.258231680319318,-1.97796460073973,91.6457068389081));
#8837=CARTESIAN_POINT('Ctrl Pts',(0.327126019380643,-1.96897015213653,91.6501537543638));
#8838=CARTESIAN_POINT('Ctrl Pts',(0.395657317348736,-1.95635790420461,91.6546006698195));
#8839=CARTESIAN_POINT('Ctrl Pts',(0.463417572739169,-1.94017311489891,91.6590475852751));
#8840=CARTESIAN_POINT('Ctrl Pts',(0.531097787415514,-1.9240074436158,91.6634892478833));
#8841=CARTESIAN_POINT('Ctrl Pts',(0.598008294462548,-1.90427772557105,91.6679309104914));
#8842=CARTESIAN_POINT('Ctrl Pts',(0.663749502519618,-1.88108058317685,91.6723725730996));
#8843=CARTESIAN_POINT('Ctrl Pts',(0.729449138692732,-1.85789810964774,91.6768114269933));
#8844=CARTESIAN_POINT('Ctrl Pts',(0.793980481995075,-1.83125272398766,91.681250280887));
#8845=CARTESIAN_POINT('Ctrl Pts',(0.856958848403317,-1.80129095224599,91.6856891347806));
#8846=CARTESIAN_POINT('Ctrl Pts',(0.919918802009486,-1.7713379403405,91.6901266908995));
#8847=CARTESIAN_POINT('Ctrl Pts',(0.981326238091841,-1.73807067739306,91.6945642470184));
#8848=CARTESIAN_POINT('Ctrl Pts',(1.04081787082229,-1.70168320267815,91.6990018031372));
#8849=CARTESIAN_POINT('Ctrl Pts',(1.10031233611009,-1.66529399545726,91.7034395705401));
#8850=CARTESIAN_POINT('Ctrl Pts',(1.1578904004571,-1.62578453904915,91.707877337943));
#8851=CARTESIAN_POINT('Ctrl Pts',(1.21321628176691,-1.58339313379706,91.7123151053459));
#8852=CARTESIAN_POINT('Ctrl Pts',(1.2686008584175,-1.54095675541633,91.7167575807854));
#8853=CARTESIAN_POINT('Ctrl Pts',(1.32172809347337,-1.495632623975,91.7212000562248));
#8854=CARTESIAN_POINT('Ctrl Pts',(1.37229471426436,-1.44769982375564,91.7256425316642));
#8855=CARTESIAN_POINT('Ctrl Pts',(1.42289081142372,-1.39973908247844,91.7300875967179));
#8856=CARTESIAN_POINT('Ctrl Pts',(1.47092298606983,-1.34916700091813,91.7345326617716));
#8857=CARTESIAN_POINT('Ctrl Pts',(1.51612629089565,-1.29629804927532,91.7389777268253));
#8858=CARTESIAN_POINT('Ctrl Pts',(1.5614087618025,-1.2433365064442,91.7434305766722));
#8859=CARTESIAN_POINT('Ctrl Pts',(1.60385217481339,-1.18807045192681,91.7478834265191));
#8860=CARTESIAN_POINT('Ctrl Pts',(1.64323364245756,-1.13084515243939,91.7523362763659));
#8861=CARTESIAN_POINT('Ctrl Pts',(1.66468453745377,-1.09967480852222,91.7547617221457));
#8862=CARTESIAN_POINT('Ctrl Pts',(1.6852277561755,-1.06792364144393,91.7571871679255));
#8863=CARTESIAN_POINT('Ctrl Pts',(1.70483308141496,-1.0356503884097,91.7596126137053));
#8864=CARTESIAN_POINT('Ctrl Pts',(1.74083141177058,-0.976391834410417,91.7640660975101));
#8865=CARTESIAN_POINT('Ctrl Pts',(1.77380789984148,-0.915136424797846,91.7685195813148));
#8866=CARTESIAN_POINT('Ctrl Pts',(1.80353546187275,-0.852224970455246,91.7729730651195));
#8867=CARTESIAN_POINT('Ctrl Pts',(1.83321825272986,-0.789408263864797,91.7774198417581));
#8868=CARTESIAN_POINT('Ctrl Pts',(1.85966162140974,-0.724940901765582,91.7818666183966));
#8869=CARTESIAN_POINT('Ctrl Pts',(1.88268302922411,-0.659190544510101,91.7863133950352));
#8870=CARTESIAN_POINT('Ctrl Pts',(1.90567722507073,-0.593517906072535,91.7907549154555));
#8871=CARTESIAN_POINT('Ctrl Pts',(1.92525733253197,-0.526565744437922,91.7951964358759));
#8872=CARTESIAN_POINT('Ctrl Pts',(1.9412885679162,-0.458722419964247,91.7996379562963));
#8873=CARTESIAN_POINT('Ctrl Pts',(1.95730965827062,-0.390922028710185,91.8040766659939));
#8874=CARTESIAN_POINT('Ctrl Pts',(1.96978621934225,-0.32223206882486,91.8085153756916));
#8875=CARTESIAN_POINT('Ctrl Pts',(1.97863350693547,-0.253055345195932,91.8129540853892));
#8876=CARTESIAN_POINT('Ctrl Pts',(1.98747820421534,-0.18389887516327,91.8173914955192));
#8877=CARTESIAN_POINT('Ctrl Pts',(1.99269567527279,-0.114256409796314,91.8218289056492));
#8878=CARTESIAN_POINT('Ctrl Pts',(1.99425271452269,-0.0445384454026968,
91.8262663157792));
#8879=CARTESIAN_POINT('Ctrl Pts',(1.99580982735564,0.0251828137443127,91.8307039356137));
#8880=CARTESIAN_POINT('Ctrl Pts',(1.99370615638435,0.0949790893618926,91.8351415554482));
#8881=CARTESIAN_POINT('Ctrl Pts',(1.98796060036666,0.164439088691927,91.8395791752827));
#8882=CARTESIAN_POINT('Ctrl Pts',(1.98220895047904,0.233972758907779,91.8440215017597));
#8883=CARTESIAN_POINT('Ctrl Pts',(1.97280774618898,0.303168951922588,91.8484638282367));
#8884=CARTESIAN_POINT('Ctrl Pts',(1.9598277722544,0.371621669982216,91.8529061547137));
#8885=CARTESIAN_POINT('Ctrl Pts',(1.94684023472766,0.440114276291528,91.8573510697895));
#8886=CARTESIAN_POINT('Ctrl Pts',(1.93026989321702,0.507862069508077,91.8617959848654));
#8887=CARTESIAN_POINT('Ctrl Pts',(1.91023802225024,0.574472158463305,91.8662408999412));
#8888=CARTESIAN_POINT('Ctrl Pts',(1.89017106752955,0.641198908112534,91.8706935998269));
#8889=CARTESIAN_POINT('Ctrl Pts',(1.86663064671297,0.706783515007433,91.8751462997126));
#8890=CARTESIAN_POINT('Ctrl Pts',(1.8397866825987,0.770851817817454,91.8795989995984));
#8891=CARTESIAN_POINT('Ctrl Pts',(1.82515655279538,0.805769447061747,91.8820257491286));
#8892=CARTESIAN_POINT('Ctrl Pts',(1.80954598416172,0.840237088275283,91.8844524986588));
#8893=CARTESIAN_POINT('Ctrl Pts',(1.79298810575163,0.874197469187127,91.886879248189));
#8894=CARTESIAN_POINT('Ctrl Pts',(1.76260114926658,0.936521433128998,91.8913328098439));
#8895=CARTESIAN_POINT('Ctrl Pts',(1.72890042286844,0.99738289868493,91.8957863714989));
#8896=CARTESIAN_POINT('Ctrl Pts',(1.69204986404861,1.05640656002937,91.9002399331538));
#8897=CARTESIAN_POINT('Ctrl Pts',(1.65525479373849,1.11534134524517,91.904686788764));
#8898=CARTESIAN_POINT('Ctrl Pts',(1.61531956165861,1.17244340664813,91.9091336443741));
#8899=CARTESIAN_POINT('Ctrl Pts',(1.5724547756546,1.22736039573592,91.9135804999842));
#8900=CARTESIAN_POINT('Ctrl Pts',(1.52964064386472,1.28221248826913,91.9180221006521));
#8901=CARTESIAN_POINT('Ctrl Pts',(1.48390413373731,1.33488425276784,91.9224637013199));
#8902=CARTESIAN_POINT('Ctrl Pts',(1.43549908588095,1.3850523228149,91.9269053019878));
#8903=CARTESIAN_POINT('Ctrl Pts',(1.38712466146663,1.43518865404436,91.931344092678));
#8904=CARTESIAN_POINT('Ctrl Pts',(1.33608538760082,1.48282408142388,91.9357828833683));
#8905=CARTESIAN_POINT('Ctrl Pts',(1.28267431049402,1.52766952437322,91.9402216740585));
#8906=CARTESIAN_POINT('Ctrl Pts',(1.22927886332582,1.57250184398638,91.9446591658042));
#8907=CARTESIAN_POINT('Ctrl Pts',(1.17351336556581,1.61454548519606,91.9490966575499));
#8908=CARTESIAN_POINT('Ctrl Pts',(1.11570519872292,1.6535505653117,91.9535341492957));
#8909=CARTESIAN_POINT('Ctrl Pts',(1.05789429347484,1.69255749311981,91.9579718512478));
#8910=CARTESIAN_POINT('Ctrl Pts',(0.998040934293289,1.72852530214157,91.9624095532));
#8911=CARTESIAN_POINT('Ctrl Pts',(0.936501343751632,1.76124751118387,91.9668472551522));
#8912=CARTESIAN_POINT('Ctrl Pts',(0.874896481356214,1.79400442697714,91.9712896639448));
#8913=CARTESIAN_POINT('Ctrl Pts',(0.811602251029684,1.82350864138877,91.9757320727375));
#8914=CARTESIAN_POINT('Ctrl Pts',(0.746998474200789,1.84960018437545,91.9801744815301));
#8915=CARTESIAN_POINT('Ctrl Pts',(0.682357049206668,1.87570693233573,91.984619479158));
#8916=CARTESIAN_POINT('Ctrl Pts',(0.616405021962518,1.89839689113825,91.989064476786));
#8917=CARTESIAN_POINT('Ctrl Pts',(0.549538486765532,1.91755965071845,91.9935094744139));
#8918=CARTESIAN_POINT('Ctrl Pts',(0.482554851703556,1.936755969037,91.9979622563337));
#8919=CARTESIAN_POINT('Ctrl Pts',(0.414653988835545,1.95241264749731,92.0024150382534));
#8920=CARTESIAN_POINT('Ctrl Pts',(0.346242539320402,1.96447032720399,92.0068678201732));
#8921=CARTESIAN_POINT('Ctrl Pts',(0.308969750142853,1.97103974441212,92.0092938410063));
#8922=CARTESIAN_POINT('Ctrl Pts',(0.271545501069042,1.97654173171664,92.0117198618395));
#8923=CARTESIAN_POINT('Ctrl Pts',(0.234035822213164,1.98097319427119,92.0141458826726));
#8924=CARTESIAN_POINT('Ctrl Pts',(0.165177654838381,1.9891082250047,92.0185994358268));
#8925=CARTESIAN_POINT('Ctrl Pts',(0.0957580885741036,1.99366488905668,92.0230529889811));
#8926=CARTESIAN_POINT('Ctrl Pts',(0.0261814775965268,1.99457817413378,92.0275065421353));
#8927=CARTESIAN_POINT('Ctrl Pts',(-0.0432903677013928,1.99549008402272,
92.0319533893072));
#8928=CARTESIAN_POINT('Ctrl Pts',(-0.112918302742501,1.99276949691071,92.0364002364791));
#8929=CARTESIAN_POINT('Ctrl Pts',(-0.182292051846247,1.98640307348073,92.040847083651));
#8930=CARTESIAN_POINT('Ctrl Pts',(-0.251583822506288,1.980044173206,92.0452886760167));
#8931=CARTESIAN_POINT('Ctrl Pts',(-0.320621518521699,1.97004803782135,92.0497302683824));
#8932=CARTESIAN_POINT('Ctrl Pts',(-0.388995869555428,1.95645336667369,92.054171860748));
#8933=CARTESIAN_POINT('Ctrl Pts',(-0.457326964862402,1.94286729593498,92.0586106432251));
#8934=CARTESIAN_POINT('Ctrl Pts',(-0.524995068504795,1.92568730078927,92.0630494257022));
#8935=CARTESIAN_POINT('Ctrl Pts',(-0.59159855460696,1.90500359912703,92.0674882081793));
#8936=CARTESIAN_POINT('Ctrl Pts',(-0.658182551705164,1.88432594977178,92.0719256918138));
#8937=CARTESIAN_POINT('Ctrl Pts',(-0.723702082251926,1.86014677425824,92.0763631754483));
#8938=CARTESIAN_POINT('Ctrl Pts',(-0.78776993029633,1.83260636783269,92.0808006590827));
#8939=CARTESIAN_POINT('Ctrl Pts',(-0.851840814932851,1.8050646560881,92.0852383530384));
#8940=CARTESIAN_POINT('Ctrl Pts',(-0.914459431517329,1.77416159271583,92.089676046994));
#8941=CARTESIAN_POINT('Ctrl Pts',(-0.97525948086811,1.74008520121196,92.0941137409497));
#8942=CARTESIAN_POINT('Ctrl Pts',(-1.03612402096819,1.70597266480286,92.0985561419773));
#8943=CARTESIAN_POINT('Ctrl Pts',(-1.0951657156417,1.6686803217795,92.102998543005));
#8944=CARTESIAN_POINT('Ctrl Pts',(-1.15204463276392,1.62844119532141,92.1074409440326));
#8945=CARTESIAN_POINT('Ctrl Pts',(-1.20895669794112,1.58817861819228,92.1118859340152));
#8946=CARTESIAN_POINT('Ctrl Pts',(-1.26370309232811,1.54496614297382,92.1163309239978));
#8947=CARTESIAN_POINT('Ctrl Pts',(-1.31597677668335,1.4990772781048,92.1207759139804));
#8948=CARTESIAN_POINT('Ctrl Pts',(-1.36834200855585,1.45310804752787,92.1252286885261));
#8949=CARTESIAN_POINT('Ctrl Pts',(-1.41822553528151,1.40445341256117,92.1296814630718));
#8950=CARTESIAN_POINT('Ctrl Pts',(-1.46535756086145,1.35342335628073,92.1341342376176));
#8951=CARTESIAN_POINT('Ctrl Pts',(-1.49103743407814,1.32561964194004,92.1365603307971));
#8952=CARTESIAN_POINT('Ctrl Pts',(-1.5159011992894,1.29711133444319,92.1389864239766));
#8953=CARTESIAN_POINT('Ctrl Pts',(-1.53991054849781,1.26795231184976,92.1414125171562));
#8954=CARTESIAN_POINT('Ctrl Pts',(-1.58523602325096,1.21290514955846,92.1459925590475));
#8955=CARTESIAN_POINT('Ctrl Pts',(-1.62770503759097,1.15530429146085,92.1505726009388));
#8956=CARTESIAN_POINT('Ctrl Pts',(-1.66701720851066,1.09548217193587,92.1551526428301));
#8957=CARTESIAN_POINT('Ctrl Pts',(-1.66796412351456,1.09611534438494,91.3549851603904));
#8958=CARTESIAN_POINT('Ctrl Pts',(-1.73430967354358,0.997308734995318,91.3625943436784));
#8959=CARTESIAN_POINT('Ctrl Pts',(-1.92014308949855,0.657612230849117,91.3873052709542));
#8960=CARTESIAN_POINT('Ctrl Pts',(-1.99323138819231,0.269843683907433,91.41201619823));
#8961=CARTESIAN_POINT('Ctrl Pts',(-1.99200409659199,0.00103412633720044,
91.4291179422178));
#8962=CARTESIAN_POINT('Ctrl Pts',(-1.66701720873947,1.09548217158769,91.1951011757363));
#8963=CARTESIAN_POINT('Ctrl Pts',(-1.67557932382123,1.08245302921121,91.1960977547751));
#8964=CARTESIAN_POINT('Ctrl Pts',(-1.68398835949459,1.06932400742616,91.1971000459174));
#8965=CARTESIAN_POINT('Ctrl Pts',(-1.71202140507325,1.02440514260801,91.200523546742));
#8966=CARTESIAN_POINT('Ctrl Pts',(-1.73090480249588,0.992165027452247,91.2029713836732));
#8967=CARTESIAN_POINT('Ctrl Pts',(-1.80883185370803,0.850115668057356,91.2137229628638));
#8968=CARTESIAN_POINT('Ctrl Pts',(-1.8584060144973,0.735450833854669,91.2223409935215));
#8969=CARTESIAN_POINT('Ctrl Pts',(-1.92088412850732,0.543341151059053,91.2364362574407));
#8970=CARTESIAN_POINT('Ctrl Pts',(-1.94051494292932,0.468420806961051,91.2418474567661));
#8971=CARTESIAN_POINT('Ctrl Pts',(-1.96182119974608,0.362269017879838,91.2492658810048));
#8972=CARTESIAN_POINT('Ctrl Pts',(-1.96719483880068,0.331852256753587,91.2513631997857));
#8973=CARTESIAN_POINT('Ctrl Pts',(-1.97550007184297,0.277502475802883,91.2550472633365));
#8974=CARTESIAN_POINT('Ctrl Pts',(-1.97870819664382,0.253618127637724,91.2566445985615));
#8975=CARTESIAN_POINT('Ctrl Pts',(-1.98312730478675,0.215493882486985,91.2591538310612));
#8976=CARTESIAN_POINT('Ctrl Pts',(-1.98461936074998,0.201289701017723,91.2600798094895));
#8977=CARTESIAN_POINT('Ctrl Pts',(-1.9872974410768,0.172858891701633,91.2619138148298));
#8978=CARTESIAN_POINT('Ctrl Pts',(-1.98848355629581,0.158633185401096,91.2628217483202));
#8979=CARTESIAN_POINT('Ctrl Pts',(-1.99128281501323,0.120064314340272,91.2652599793522));
#8980=CARTESIAN_POINT('Ctrl Pts',(-1.99260233042405,0.0957014522708389,
91.2667749776096));
#8981=CARTESIAN_POINT('Ctrl Pts',(-1.99812378007248,-0.0586309298590655,
91.2762476823262));
#8982=CARTESIAN_POINT('Ctrl Pts',(-1.99005564969632,-0.18874000020035,91.2836908192202));
#8983=CARTESIAN_POINT('Ctrl Pts',(-1.95303024900074,-0.418653261848093,
91.2972026299974));
#8984=CARTESIAN_POINT('Ctrl Pts',(-1.92886302470222,-0.518731382220453,
91.3032105393503));
#8985=CARTESIAN_POINT('Ctrl Pts',(-1.88578229316025,-0.651300216300443,
91.3116770229581));
#8986=CARTESIAN_POINT('Ctrl Pts',(-1.87351692648273,-0.685784874258854,
91.3139267886881));
#8987=CARTESIAN_POINT('Ctrl Pts',(-1.85156051344161,-0.742522086628909,
91.3177193875796));
#8988=CARTESIAN_POINT('Ctrl Pts',(-1.84239923379764,-0.764970825290077,
91.3192442299543));
#8989=CARTESIAN_POINT('Ctrl Pts',(-1.82324045126845,-0.809575443542693,
91.3223258433804));
#8990=CARTESIAN_POINT('Ctrl Pts',(-1.81324263369408,-0.831726641397818,
91.3238824176842));
#8991=CARTESIAN_POINT('Ctrl Pts',(-1.78704724524203,-0.887046763279057,
91.3278388273612));
#8992=CARTESIAN_POINT('Ctrl Pts',(-1.77032966423661,-0.9199578218795,91.3302564715431));
#8993=CARTESIAN_POINT('Ctrl Pts',(-1.69014280363983,-1.06752877731028,91.3413980861344));
#8994=CARTESIAN_POINT('Ctrl Pts',(-1.61639067780149,-1.17621073636466,91.3504799246466));
#8995=CARTESIAN_POINT('Ctrl Pts',(-1.48533658335459,-1.33350619318615,91.3647790548516));
#8996=CARTESIAN_POINT('Ctrl Pts',(-1.43503571289753,-1.38749302950276,91.3699321377992));
#8997=CARTESIAN_POINT('Ctrl Pts',(-1.36020150826005,-1.45937702748069,91.3770386660267));
#8998=CARTESIAN_POINT('Ctrl Pts',(-1.33807524244018,-1.479690602599,91.3790770660678));
#8999=CARTESIAN_POINT('Ctrl Pts',(-1.29778321330738,-1.51503848432675,91.3826668924804));
#9000=CARTESIAN_POINT('Ctrl Pts',(-1.27979382724325,-1.53026492983871,91.3842283645877));
#9001=CARTESIAN_POINT('Ctrl Pts',(-1.25062584040304,-1.55407883138959,91.3866894030774));
#9002=CARTESIAN_POINT('Ctrl Pts',(-1.2396191773746,-1.56287246469022,91.387602491826));
#9003=CARTESIAN_POINT('Ctrl Pts',(-1.21718947898448,-1.58040632693127,91.3894303844978));
#9004=CARTESIAN_POINT('Ctrl Pts',(-1.20576335706046,-1.5891410080481,91.3903448528038));
#9005=CARTESIAN_POINT('Ctrl Pts',(-1.17442155760878,-1.61256751174137,91.3928112400276));
#9006=CARTESIAN_POINT('Ctrl Pts',(-1.15432471305096,-1.62701400188971,91.3943474033065));
#9007=CARTESIAN_POINT('Ctrl Pts',(-1.06335128333963,-1.68987522693105,91.4011269088481));
#9008=CARTESIAN_POINT('Ctrl Pts',(-0.989656567701482,-1.73406373054063,
91.4061579598815));
#9009=CARTESIAN_POINT('Ctrl Pts',(-0.779341590488958,-1.84238210631005,
91.4199133512176));
#9010=CARTESIAN_POINT('Ctrl Pts',(-0.637968801043272,-1.89597917343904,
91.4285463309824));
#9011=CARTESIAN_POINT('Ctrl Pts',(-0.458170840760185,-1.94173100152174,
91.4398487481898));
#9012=CARTESIAN_POINT('Ctrl Pts',(-0.424211601296343,-1.94943173564965,
91.4419945967116));
#9013=CARTESIAN_POINT('Ctrl Pts',(-0.366707009382995,-1.96089802155084,
91.4456565615681));
#9014=CARTESIAN_POINT('Ctrl Pts',(-0.343263552849276,-1.96513743427046,
91.4471572598384));
#9015=CARTESIAN_POINT('Ctrl Pts',(-0.295199557599133,-1.97294283568278,
91.4502525870432));
#9016=CARTESIAN_POINT('Ctrl Pts',(-0.27057707998445,-1.97647012688136,91.4518481627151));
#9017=CARTESIAN_POINT('Ctrl Pts',(-0.20680417361142,-1.9843919335312,91.4560088253887));
#9018=CARTESIAN_POINT('Ctrl Pts',(-0.167579586730039,-1.98808853701402,
91.45859526912));
#9019=CARTESIAN_POINT('Ctrl Pts',(-0.0798498535103628,-1.99374174514934,
91.4644440003917));
#9020=CARTESIAN_POINT('Ctrl Pts',(-0.0313318172720462,-1.99509395068248,
91.4677221457275));
#9021=CARTESIAN_POINT('Ctrl Pts',(0.146285484972184,-1.99356375914313,91.479866602198));
#9022=CARTESIAN_POINT('Ctrl Pts',(0.274970381662822,-1.97992003533079,91.4889672513183));
#9023=CARTESIAN_POINT('Ctrl Pts',(0.458664157106047,-1.9421817350225,91.5019290226276));
#9024=CARTESIAN_POINT('Ctrl Pts',(0.515368606921603,-1.92791055064655,91.5059212686355));
#9025=CARTESIAN_POINT('Ctrl Pts',(0.590260402158344,-1.90552066553798,91.5111154396459));
#9026=CARTESIAN_POINT('Ctrl Pts',(0.609068002062043,-1.89959274324658,91.512413005821));
#9027=CARTESIAN_POINT('Ctrl Pts',(0.64058808141338,-1.88914170963453,91.5145724723778));
#9028=CARTESIAN_POINT('Ctrl Pts',(0.653347762670158,-1.88476689092099,91.5154423291691));
#9029=CARTESIAN_POINT('Ctrl Pts',(0.680977099075295,-1.87497949063178,91.5173155890082));
#9030=CARTESIAN_POINT('Ctrl Pts',(0.695828254476938,-1.86951891656941,91.5183162724433));
#9031=CARTESIAN_POINT('Ctrl Pts',(0.740716170149424,-1.85240519567818,91.5213264274254));
#9032=CARTESIAN_POINT('Ctrl Pts',(0.770538384695544,-1.84020007477372,91.5233065124223));
#9033=CARTESIAN_POINT('Ctrl Pts',(0.84273439974789,-1.80858982454666,91.5280818006507));
#9034=CARTESIAN_POINT('Ctrl Pts',(0.884749811014522,-1.78841177850315,91.5308452190301));
#9035=CARTESIAN_POINT('Ctrl Pts',(1.01338409869734,-1.72099069413277,91.5393691118898));
#9036=CARTESIAN_POINT('Ctrl Pts',(1.09723048164694,-1.66878467764027,91.5450240073601));
#9037=CARTESIAN_POINT('Ctrl Pts',(1.19100321263822,-1.60026410688594,91.5518112088524));
#9038=CARTESIAN_POINT('Ctrl Pts',(1.20499748792955,-1.58975309541588,91.5528369049176));
#9039=CARTESIAN_POINT('Ctrl Pts',(1.27540301861102,-1.53540815803632,91.5580695371411));
#9040=CARTESIAN_POINT('Ctrl Pts',(1.32956388383169,-1.48875433638958,91.5623368998203));
#9041=CARTESIAN_POINT('Ctrl Pts',(1.40287307230182,-1.41840933881711,91.5685712564255));
#9042=CARTESIAN_POINT('Ctrl Pts',(1.42416571533331,-1.39702890891455,91.5704420483364));
#9043=CARTESIAN_POINT('Ctrl Pts',(1.4611360939455,-1.35818229293506,91.5738055502104));
#9044=CARTESIAN_POINT('Ctrl Pts',(1.47700616769576,-1.34090660743516,91.5752894895947));
#9045=CARTESIAN_POINT('Ctrl Pts',(1.51011776599451,-1.30356117363778,91.5784750622594));
#9046=CARTESIAN_POINT('Ctrl Pts',(1.52727190598122,-1.28342035729944,91.5801799627468));
#9047=CARTESIAN_POINT('Ctrl Pts',(1.57450070073456,-1.22568056242885,91.5850342685134));
#9048=CARTESIAN_POINT('Ctrl Pts',(1.60362021998845,-1.18732760319835,91.5882206175824));
#9049=CARTESIAN_POINT('Ctrl Pts',(1.66869295526831,-1.09485534537592,91.5958183280696));
#9050=CARTESIAN_POINT('Ctrl Pts',(1.70344531005663,-1.03996021864376,91.6002654464387));
#9051=CARTESIAN_POINT('Ctrl Pts',(1.80143766910359,-0.867040755177769,91.6140296799328));
#9052=CARTESIAN_POINT('Ctrl Pts',(1.85553409605499,-0.744265730251361,91.6234951228334));
#9053=CARTESIAN_POINT('Ctrl Pts',(1.90691360074303,-0.586301970193441,91.6347501663742));
#9054=CARTESIAN_POINT('Ctrl Pts',(1.9161518954768,-0.555366244806632,91.6369110445818));
#9055=CARTESIAN_POINT('Ctrl Pts',(1.92879489433107,-0.508948212035358,91.6400759291906));
#9056=CARTESIAN_POINT('Ctrl Pts',(1.93277226487754,-0.493628847464306,91.6411080225453));
#9057=CARTESIAN_POINT('Ctrl Pts',(1.9397910655852,-0.465208557078174,91.6429977997215));
#9058=CARTESIAN_POINT('Ctrl Pts',(1.94288283164275,-0.452122430712377,91.643858004984));
#9059=CARTESIAN_POINT('Ctrl Pts',(1.95015483795353,-0.419890041959174,91.6459538653473));
#9060=CARTESIAN_POINT('Ctrl Pts',(1.95418568228366,-0.400711777083527,91.6471813526323));
#9061=CARTESIAN_POINT('Ctrl Pts',(1.96980637504549,-0.320538326643491,91.6522433806256));
#9062=CARTESIAN_POINT('Ctrl Pts',(1.9788290634956,-0.259073266478648,91.6559580373196));
#9063=CARTESIAN_POINT('Ctrl Pts',(2.00145621125214,-0.0314083848154977,
91.6694318399111));
#9064=CARTESIAN_POINT('Ctrl Pts',(1.99708636270522,0.135872062533571,91.6788355447133));
#9065=CARTESIAN_POINT('Ctrl Pts',(1.96535082321936,0.344015675837371,91.6915127572879));
#9066=CARTESIAN_POINT('Ctrl Pts',(1.95731360813261,0.387135191941691,91.694188987242));
#9067=CARTESIAN_POINT('Ctrl Pts',(1.94233162261265,0.455009759843278,91.6985019189054));
#9068=CARTESIAN_POINT('Ctrl Pts',(1.93631798078774,0.479956866190553,91.7001088520919));
#9069=CARTESIAN_POINT('Ctrl Pts',(1.92384545518493,0.527640580162321,91.7032257872347));
#9070=CARTESIAN_POINT('Ctrl Pts',(1.91746039507092,0.550392106677105,91.7047331464944));
#9071=CARTESIAN_POINT('Ctrl Pts',(1.90140057654431,0.603941446658325,91.70833126747));
#9072=CARTESIAN_POINT('Ctrl Pts',(1.89137966215194,0.634627602559148,91.710433099684));
#9073=CARTESIAN_POINT('Ctrl Pts',(1.84813443505409,0.756914806522421,91.7189760451027));
#9074=CARTESIAN_POINT('Ctrl Pts',(1.80896765972359,0.846257791933204,91.7256082575551));
#9075=CARTESIAN_POINT('Ctrl Pts',(1.6988699375753,1.05449057473166,91.7419282848842));
#9076=CARTESIAN_POINT('Ctrl Pts',(1.6217926772881,1.16957235055995,91.7517056387603));
#9077=CARTESIAN_POINT('Ctrl Pts',(1.51512467160417,1.29778466611345,91.7629563826147));
#9078=CARTESIAN_POINT('Ctrl Pts',(1.49633444120909,1.31940564194575,91.7648661385844));
#9079=CARTESIAN_POINT('Ctrl Pts',(1.46690557390785,1.35183022826784,91.767739943736));
#9080=CARTESIAN_POINT('Ctrl Pts',(1.45659936098922,1.36292892917057,91.7687254417333));
#9081=CARTESIAN_POINT('Ctrl Pts',(1.43674628162087,1.38382613758694,91.7705826188315));
#9082=CARTESIAN_POINT('Ctrl Pts',(1.42722345728877,1.39364553207016,91.7714557956476));
#9083=CARTESIAN_POINT('Ctrl Pts',(1.4027539968117,1.41836317565158,91.7736572157053));
#9084=CARTESIAN_POINT('Ctrl Pts',(1.38767007498224,1.43312411247091,91.7749752097799));
#9085=CARTESIAN_POINT('Ctrl Pts',(1.30774331981868,1.50889400906135,91.781776874104));
#9086=CARTESIAN_POINT('Ctrl Pts',(1.2390969401349,1.56575732856078,91.7870094347413));
#9087=CARTESIAN_POINT('Ctrl Pts',(1.04025906407855,1.70916921291684,91.8012776334048));
#9088=CARTESIAN_POINT('Ctrl Pts',(0.903374751413852,1.78530348559128,91.810201179693));
#9089=CARTESIAN_POINT('Ctrl Pts',(0.727551598145605,1.85764743259769,91.8217971848367));
#9090=CARTESIAN_POINT('Ctrl Pts',(0.695760828190992,1.86978661044983,91.8238963140656));
#9091=CARTESIAN_POINT('Ctrl Pts',(0.641353599884152,1.88898212410908,91.8275019398981));
#9092=CARTESIAN_POINT('Ctrl Pts',(0.618893038786636,1.89645965782163,91.8289941073558));
#9093=CARTESIAN_POINT('Ctrl Pts',(0.572413408395258,1.91101996362131,91.8320921716486));
#9094=CARTESIAN_POINT('Ctrl Pts',(0.548383493219682,1.91805366473135,91.833699381683));
#9095=CARTESIAN_POINT('Ctrl Pts',(0.485248602099012,1.93525024501677,91.8379390698288));
#9096=CARTESIAN_POINT('Ctrl Pts',(0.445957756683675,1.94468018044857,91.8405945899291));
#9097=CARTESIAN_POINT('Ctrl Pts',(0.299098904158719,1.97524220960155,91.8505880219016));
#9098=CARTESIAN_POINT('Ctrl Pts',(0.190143268837779,1.9886884513686,91.8581494306954));
#9099=CARTESIAN_POINT('Ctrl Pts',(-0.0362804851818633,1.99785038105052,
91.873946809047));
#9100=CARTESIAN_POINT('Ctrl Pts',(-0.153406868461913,1.99228322963201,91.8821631472331));
#9101=CARTESIAN_POINT('Ctrl Pts',(-0.292896635898926,1.97327206342784,91.891590669227));
#9102=CARTESIAN_POINT('Ctrl Pts',(-0.316359794682336,1.96964658642417,91.893163493957));
#9103=CARTESIAN_POINT('Ctrl Pts',(-0.353726227510946,1.96318781038201,91.8956417289748));
#9104=CARTESIAN_POINT('Ctrl Pts',(-0.367673065329059,1.96062366975797,91.8965607596371));
#9105=CARTESIAN_POINT('Ctrl Pts',(-0.395724085708324,1.95515659565229,91.8983955376101));
#9106=CARTESIAN_POINT('Ctrl Pts',(-0.409826494878345,1.95224925161995,91.8993110009162));
#9107=CARTESIAN_POINT('Ctrl Pts',(-0.448154128414568,1.94391401336998,91.9017831335129));
#9108=CARTESIAN_POINT('Ctrl Pts',(-0.472312265026185,1.93818602568922,91.9033239269178));
#9109=CARTESIAN_POINT('Ctrl Pts',(-0.578855065282055,1.91081377302493,91.9100671939426));
#9110=CARTESIAN_POINT('Ctrl Pts',(-0.659917992526919,1.88435494320403,91.9150613237878));
#9111=CARTESIAN_POINT('Ctrl Pts',(-0.879567033286966,1.79674060707064,91.9288133950842));
#9112=CARTESIAN_POINT('Ctrl Pts',(-1.01324101328546,1.72489237665278,91.9374767525121));
#9113=CARTESIAN_POINT('Ctrl Pts',(-1.16600183835751,1.61884850364597,91.9488072208559));
#9114=CARTESIAN_POINT('Ctrl Pts',(-1.19397412660394,1.59832922924135,91.9509453209955));
#9115=CARTESIAN_POINT('Ctrl Pts',(-1.24019268575352,1.56253476575578,91.9545964851102));
#9116=CARTESIAN_POINT('Ctrl Pts',(-1.25872690999296,1.54764313685414,91.9560942743908));
#9117=CARTESIAN_POINT('Ctrl Pts',(-1.2960817404471,1.51651485083386,91.9591854448061));
#9118=CARTESIAN_POINT('Ctrl Pts',(-1.31487381040935,1.50025062588985,91.9607798051385));
#9119=CARTESIAN_POINT('Ctrl Pts',(-1.36266970273427,1.45729616651561,91.9649407316049));
#9120=CARTESIAN_POINT('Ctrl Pts',(-1.39119391208288,1.43009089575,91.9675287552192));
#9121=CARTESIAN_POINT('Ctrl Pts',(-1.45302186770433,1.36752068885605,91.9733819195505));
#9122=CARTESIAN_POINT('Ctrl Pts',(-1.48587676392072,1.33174886184449,91.9766629977819));
#9123=CARTESIAN_POINT('Ctrl Pts',(-1.57140396963382,1.23151974034883,91.9856740456171));
#9124=CARTESIAN_POINT('Ctrl Pts',(-1.62137251005126,1.1649406487014,91.9914720109716));
#9125=CARTESIAN_POINT('Ctrl Pts',(-1.66701737487202,1.09548191878041,91.9972724317));
#9126=CARTESIAN_POINT('Origin',(0.,0.,89.2710285354474));
#9127=CARTESIAN_POINT('',(-1.66701720827313,1.09548217229732,92.9566930507716));
#9128=CARTESIAN_POINT('',(-1.66701723320527,1.09548213435759,92.7986587716037));
#9129=CARTESIAN_POINT('',(-1.66701720851066,1.09548217193587,89.2710285354474));
#9130=CARTESIAN_POINT('',(-1.99474929503159,-0.00167704232401422,92.229118772657));
#9131=CARTESIAN_POINT('Ctrl Pts',(-1.66701720827313,1.09548217229732,92.9566930507716));
#9132=CARTESIAN_POINT('Ctrl Pts',(-1.66512381604442,1.09836338525276,92.9564629794761));
#9133=CARTESIAN_POINT('Ctrl Pts',(-1.66322292902265,1.10123972771993,92.956232653761));
#9134=CARTESIAN_POINT('Ctrl Pts',(-1.63018205132079,1.1509550941144,92.9522405013284));
#9135=CARTESIAN_POINT('Ctrl Pts',(-1.59708453028584,1.19645780862156,92.9484138355263));
#9136=CARTESIAN_POINT('Ctrl Pts',(-1.47970949905464,1.34426358271211,92.9354182963228));
#9137=CARTESIAN_POINT('Ctrl Pts',(-1.38717854340582,1.4395550287022,92.9260494118629));
#9138=CARTESIAN_POINT('Ctrl Pts',(-1.25228112725285,1.55330350242768,92.9139562448849));
#9139=CARTESIAN_POINT('Ctrl Pts',(-1.21774614593903,1.58052355681295,92.9109813844852));
#9140=CARTESIAN_POINT('Ctrl Pts',(-1.16925476596872,1.61620998206909,92.9069958285298));
#9141=CARTESIAN_POINT('Ctrl Pts',(-1.15605453136798,1.6256781279405,92.9059295344719));
#9142=CARTESIAN_POINT('Ctrl Pts',(-1.13174286592118,1.642670280379,92.9040016017614));
#9143=CARTESIAN_POINT('Ctrl Pts',(-1.12066857875206,1.65024529753811,92.9031368139206));
#9144=CARTESIAN_POINT('Ctrl Pts',(-1.09622385579789,1.66660634725702,92.9012578430934));
#9145=CARTESIAN_POINT('Ctrl Pts',(-1.08282289954378,1.67534416390961,92.9002466888766));
#9146=CARTESIAN_POINT('Ctrl Pts',(-1.04125342754282,1.70174148086608,92.897163153061));
#9147=CARTESIAN_POINT('Ctrl Pts',(-1.01274612410691,1.71885960544245,92.8951223607961));
#9148=CARTESIAN_POINT('Ctrl Pts',(-0.84937331862725,1.81148549497801,92.8837597999284));
#9149=CARTESIAN_POINT('Ctrl Pts',(-0.706510164299463,1.87183523764905,92.8750430700305));
#9150=CARTESIAN_POINT('Ctrl Pts',(-0.484671798284654,1.93648402682211,92.8614881239828));
#9151=CARTESIAN_POINT('Ctrl Pts',(-0.410080563385768,1.95364002248051,92.8569342095646));
#9152=CARTESIAN_POINT('Ctrl Pts',(-0.304300620752226,1.97164377598798,92.8503584569659));
#9153=CARTESIAN_POINT('Ctrl Pts',(-0.273793309906842,1.97611110740478,92.8484489675302));
#9154=CARTESIAN_POINT('Ctrl Pts',(-0.21984103025048,1.98273830019026,92.84504252305));
#9155=CARTESIAN_POINT('Ctrl Pts',(-0.196438018131312,1.98519351032647,92.8435552040201));
#9156=CARTESIAN_POINT('Ctrl Pts',(-0.147003864983722,1.98949698004184,92.8403905890866));
#9157=CARTESIAN_POINT('Ctrl Pts',(-0.120969083208511,1.99124954314883,92.8387105532682));
#9158=CARTESIAN_POINT('Ctrl Pts',(-0.0488206744255768,1.99468619157877,
92.8340149021936));
#9159=CARTESIAN_POINT('Ctrl Pts',(-0.00267406652750284,1.99528161792044,
92.8309661733468));
#9160=CARTESIAN_POINT('Ctrl Pts',(0.104374352442575,1.99294938453869,92.8237863606924));
#9161=CARTESIAN_POINT('Ctrl Pts',(0.165202414545443,1.98883090387109,92.8196250521618));
#9162=CARTESIAN_POINT('Ctrl Pts',(0.311617239347066,1.97215425742549,92.8094447888385));
#9163=CARTESIAN_POINT('Ctrl Pts',(0.396764083393373,1.95680229203769,92.8033849086056));
#9164=CARTESIAN_POINT('Ctrl Pts',(0.55326688231232,1.91794749495535,92.7921705483738));
#9165=CARTESIAN_POINT('Ctrl Pts',(0.624825553610229,1.89584333655704,92.7870136502784));
#9166=CARTESIAN_POINT('Ctrl Pts',(0.714411738766203,1.86254483243037,92.7806481481676));
#9167=CARTESIAN_POINT('Ctrl Pts',(0.733732086686501,1.85501878513223,92.779281059553));
#9168=CARTESIAN_POINT('Ctrl Pts',(0.765421092324284,1.84210205798646,92.7770523118576));
#9169=CARTESIAN_POINT('Ctrl Pts',(0.777858340687367,1.83688483205883,92.7761811175238));
#9170=CARTESIAN_POINT('Ctrl Pts',(0.804245992164879,1.82549953327339,92.7743414715752));
#9171=CARTESIAN_POINT('Ctrl Pts',(0.818180149032501,1.81929696350458,92.7733750417506));
#9172=CARTESIAN_POINT('Ctrl Pts',(0.858535479865199,1.80077597720875,92.7705868704248));
#9173=CARTESIAN_POINT('Ctrl Pts',(0.884760519831416,1.78803700051856,92.7687885144857));
#9174=CARTESIAN_POINT('Ctrl Pts',(1.04928675523246,1.70361061791707,92.7575342037621));
#9175=CARTESIAN_POINT('Ctrl Pts',(1.17908145383222,1.61649908228052,92.7487466732126));
#9176=CARTESIAN_POINT('Ctrl Pts',(1.30244256925268,1.51086549218848,92.7392382788848));
#9177=CARTESIAN_POINT('Ctrl Pts',(1.30743777834954,1.50654493350637,92.7388511491093));
#9178=CARTESIAN_POINT('Ctrl Pts',(1.36919806408038,1.45258745639231,92.7340375230737));
#9179=CARTESIAN_POINT('Ctrl Pts',(1.42312077808083,1.39979971139823,92.7295448296975));
#9180=CARTESIAN_POINT('Ctrl Pts',(1.49461554727972,1.32139888167711,92.7230409700689));
#9181=CARTESIAN_POINT('Ctrl Pts',(1.5147803578578,1.29823377942307,92.7211385771524));
#9182=CARTESIAN_POINT('Ctrl Pts',(1.54942762486827,1.25652480124698,92.7177401249473));
#9183=CARTESIAN_POINT('Ctrl Pts',(1.56413206052924,1.23817258933805,92.7162535445554));
#9184=CARTESIAN_POINT('Ctrl Pts',(1.59449774242884,1.19886967185534,92.7130855916059));
#9185=CARTESIAN_POINT('Ctrl Pts',(1.61007812152772,1.17786241759925,92.7114013877577));
#9186=CARTESIAN_POINT('Ctrl Pts',(1.65218763174429,1.11868837558988,92.7066790831089));
#9187=CARTESIAN_POINT('Ctrl Pts',(1.67780118160053,1.07989363333188,92.7036072340099));
#9188=CARTESIAN_POINT('Ctrl Pts',(1.73416025946046,0.98767942711209,92.6963578677965));
#9189=CARTESIAN_POINT('Ctrl Pts',(1.76383083329037,0.933660627355826,92.6921492376621));
#9190=CARTESIAN_POINT('Ctrl Pts',(1.82900780333406,0.800766437993345,92.6819193565281));
#9191=CARTESIAN_POINT('Ctrl Pts',(1.86197932191981,0.720783405219669,92.675859132894));
#9192=CARTESIAN_POINT('Ctrl Pts',(1.91326597479264,0.569098332921683,92.6647268650887));
#9193=CARTESIAN_POINT('Ctrl Pts',(1.93298742561041,0.498017310291534,92.6596502928297));
#9194=CARTESIAN_POINT('Ctrl Pts',(1.95314709962975,0.405797596330233,92.6533638192294));
#9195=CARTESIAN_POINT('Ctrl Pts',(1.95724958197575,0.38552488663339,92.6520002019566));
#9196=CARTESIAN_POINT('Ctrl Pts',(1.96350373150585,0.35194078766674,92.6497754400328));
#9197=CARTESIAN_POINT('Ctrl Pts',(1.96583700966981,0.338665198776039,92.6489048300368));
#9198=CARTESIAN_POINT('Ctrl Pts',(1.97052669084244,0.310298805258759,92.6470645062734));
#9199=CARTESIAN_POINT('Ctrl Pts',(1.97284466174229,0.295202920754279,92.6460968480187));
#9200=CARTESIAN_POINT('Ctrl Pts',(1.97909725818879,0.251112834248299,92.6433008190052));
#9201=CARTESIAN_POINT('Ctrl Pts',(1.98256779897893,0.222055713174705,92.6414960369726));
#9202=CARTESIAN_POINT('Ctrl Pts',(1.99865029732456,0.056555362018515,92.6313780426267));
#9203=CARTESIAN_POINT('Ctrl Pts',(1.99781750710646,-0.0808364886002574,
92.6235797722326));
#9204=CARTESIAN_POINT('Ctrl Pts',(1.97235127928098,-0.313467754021576,92.6099561622677));
#9205=CARTESIAN_POINT('Ctrl Pts',(1.95478429833044,-0.408958465645835,92.6042431871923));
#9206=CARTESIAN_POINT('Ctrl Pts',(1.92215941976946,-0.534214770727629,92.5963290008082));
#9207=CARTESIAN_POINT('Ctrl Pts',(1.91320778182807,-0.565436161204636,92.594321230139));
#9208=CARTESIAN_POINT('Ctrl Pts',(1.89641966548098,-0.619015767150256,92.5908068167942));
#9209=CARTESIAN_POINT('Ctrl Pts',(1.88893953976302,-0.641479075489736,92.5893121025613));
#9210=CARTESIAN_POINT('Ctrl Pts',(1.8725357452177,-0.687963560479017,92.586171812602));
#9211=CARTESIAN_POINT('Ctrl Pts',(1.86354551565167,-0.711956450074776,92.5845242336411));
#9212=CARTESIAN_POINT('Ctrl Pts',(1.83803151686993,-0.776250307171098,92.5800337604902));
#9213=CARTESIAN_POINT('Ctrl Pts',(1.82064666239968,-0.816192158622653,92.5771624645826));
#9214=CARTESIAN_POINT('Ctrl Pts',(1.76864290545093,-0.925725573033864,92.5690546812247));
#9215=CARTESIAN_POINT('Ctrl Pts',(1.73124625090235,-0.993906353143329,92.5637337001686));
#9216=CARTESIAN_POINT('Ctrl Pts',(1.61331812442402,-1.18196924372334,92.5483395797541));
#9217=CARTESIAN_POINT('Ctrl Pts',(1.52362577322996,-1.29553621978236,92.5381206207385));
#9218=CARTESIAN_POINT('Ctrl Pts',(1.40622023928125,-1.41495903748831,92.5269162865922));
#9219=CARTESIAN_POINT('Ctrl Pts',(1.38968877526365,-1.43119867908737,92.5253823455063));
#9220=CARTESIAN_POINT('Ctrl Pts',(1.36267266306689,-1.45682827714503,92.5229500419429));
#9221=CARTESIAN_POINT('Ctrl Pts',(1.35236546507571,-1.46640141269237,92.5220388732788));
#9222=CARTESIAN_POINT('Ctrl Pts',(1.33120429780437,-1.48564259021605,92.52020360882));
#9223=CARTESIAN_POINT('Ctrl Pts',(1.32034430846007,-1.495302553684,92.5192800627295));
#9224=CARTESIAN_POINT('Ctrl Pts',(1.29015154525115,-1.52157358064041,92.5167591975319));
#9225=CARTESIAN_POINT('Ctrl Pts',(1.27060384742114,-1.53793471099332,92.5151788294073));
#9226=CARTESIAN_POINT('Ctrl Pts',(1.22473274330075,-1.57485632299711,92.5115734706857));
#9227=CARTESIAN_POINT('Ctrl Pts',(1.19819551642144,-1.59513963810258,92.5095631387166));
#9228=CARTESIAN_POINT('Ctrl Pts',(1.09797276867935,-1.66783016920479,92.5021942735151));
#9229=CARTESIAN_POINT('Ctrl Pts',(1.02125738519878,-1.71587782844855,92.4969836481084));
#9230=CARTESIAN_POINT('Ctrl Pts',(0.847769588897766,-1.80876439191976,92.4855665615558));
#9231=CARTESIAN_POINT('Ctrl Pts',(0.75013898529938,-1.85138607025453,92.4793600471662));
#9232=CARTESIAN_POINT('Ctrl Pts',(0.614566799610138,-1.89807973439372,92.4706530171061));
#9233=CARTESIAN_POINT('Ctrl Pts',(0.579224922797734,-1.9091613994254,92.4683767978636));
#9234=CARTESIAN_POINT('Ctrl Pts',(0.520097644003237,-1.92590822975462,92.4645461644899));
#9235=CARTESIAN_POINT('Ctrl Pts',(0.496479181757247,-1.93213157046368,92.4630102124657));
#9236=CARTESIAN_POINT('Ctrl Pts',(0.449036207356767,-1.94370522938138,92.4599104069859));
#9237=CARTESIAN_POINT('Ctrl Pts',(0.425215900680437,-1.94905486943253,92.4583468333448));
#9238=CARTESIAN_POINT('Ctrl Pts',(0.36508809144613,-1.96140388089001,92.4543794346653));
#9239=CARTESIAN_POINT('Ctrl Pts',(0.328674292161789,-1.96783317525256,92.4519579230179));
#9240=CARTESIAN_POINT('Ctrl Pts',(0.18823846661758,-1.98862225337355,92.4425416943105));
#9241=CARTESIAN_POINT('Ctrl Pts',(0.0833340461069003,-1.99577109174912,
92.4353344691009));
#9242=CARTESIAN_POINT('Ctrl Pts',(-0.153055666163285,-1.99320737284861,
92.4188830011419));
#9243=CARTESIAN_POINT('Ctrl Pts',(-0.284022896300073,-1.97879678781788,
92.4096160131897));
#9244=CARTESIAN_POINT('Ctrl Pts',(-0.434377101032974,-1.94700753477385,
92.399351377401));
#9245=CARTESIAN_POINT('Ctrl Pts',(-0.456050581643854,-1.94204525526638,
92.3978817343252));
#9246=CARTESIAN_POINT('Ctrl Pts',(-0.489792026253793,-1.9337238810199,92.3956141841978));
#9247=CARTESIAN_POINT('Ctrl Pts',(-0.501918349230599,-1.93061188979822,
92.3948034074975));
#9248=CARTESIAN_POINT('Ctrl Pts',(-0.527836765331375,-1.92369970137956,
92.3930805982362));
#9249=CARTESIAN_POINT('Ctrl Pts',(-0.54161901417274,-1.9198648561112,92.3921706603953));
#9250=CARTESIAN_POINT('Ctrl Pts',(-0.578754295923217,-1.90910040108312,
92.3897326495691));
#9251=CARTESIAN_POINT('Ctrl Pts',(-0.602024335072754,-1.90189055984074,
92.3882197132617));
#9252=CARTESIAN_POINT('Ctrl Pts',(-0.702192348769968,-1.86883230099175,
92.3817480125527));
#9253=CARTESIAN_POINT('Ctrl Pts',(-0.777612256578105,-1.83873053833885,
92.3769787560407));
#9254=CARTESIAN_POINT('Ctrl Pts',(-0.994343385309559,-1.73649920003214,
92.3630263379002));
#9255=CARTESIAN_POINT('Ctrl Pts',(-1.12910886947991,-1.65204649319573,92.3539746838506));
#9256=CARTESIAN_POINT('Ctrl Pts',(-1.27867455853763,-1.53138940789677,92.3422478967131));
#9257=CARTESIAN_POINT('Ctrl Pts',(-1.30434970509759,-1.50958066520973,92.3401689376513));
#9258=CARTESIAN_POINT('Ctrl Pts',(-1.34706822140963,-1.4713913997486,92.3365867774337));
#9259=CARTESIAN_POINT('Ctrl Pts',(-1.36439550319081,-1.45533854398623,92.3350974252666));
#9260=CARTESIAN_POINT('Ctrl Pts',(-1.39956898576976,-1.42157175559462,92.331995182526));
#9261=CARTESIAN_POINT('Ctrl Pts',(-1.41737339220613,-1.40382056297502,92.3303807974477));
#9262=CARTESIAN_POINT('Ctrl Pts',(-1.46328595469061,-1.35628125464582,92.3260970787846));
#9263=CARTESIAN_POINT('Ctrl Pts',(-1.4908192484125,-1.32595708371911,92.3234037911163));
#9264=CARTESIAN_POINT('Ctrl Pts',(-1.57768093285815,-1.22416308561304,92.3144827358484));
#9265=CARTESIAN_POINT('Ctrl Pts',(-1.63294954215236,-1.14940182351029,92.3081079748186));
#9266=CARTESIAN_POINT('Ctrl Pts',(-1.75130124523737,-0.96345454898082,92.2927825172896));
#9267=CARTESIAN_POINT('Ctrl Pts',(-1.80931854440083,-0.849511601192616,
92.2837850095712));
#9268=CARTESIAN_POINT('Ctrl Pts',(-1.86582911150276,-0.705989065833395,
92.2734085102));
#9269=CARTESIAN_POINT('Ctrl Pts',(-1.87510184208267,-0.680978765927614,
92.2716344290136));
#9270=CARTESIAN_POINT('Ctrl Pts',(-1.88872639309898,-0.641839795069339,
92.2689187658891));
#9271=CARTESIAN_POINT('Ctrl Pts',(-1.89342719833468,-0.627836912269911,
92.2679590579857));
#9272=CARTESIAN_POINT('Ctrl Pts',(-1.90224836965651,-0.600559601880096,
92.2661143122533));
#9273=CARTESIAN_POINT('Ctrl Pts',(-1.90638628842404,-0.587292115015154,
92.2652284298843));
#9274=CARTESIAN_POINT('Ctrl Pts',(-1.91680040188146,-0.55263081355425,92.2629411117079));
#9275=CARTESIAN_POINT('Ctrl Pts',(-1.92285741684199,-0.53117233542612,92.2615516560956));
#9276=CARTESIAN_POINT('Ctrl Pts',(-1.95473128816408,-0.410551123424886,
92.2538661210989));
#9277=CARTESIAN_POINT('Ctrl Pts',(-1.97324006091968,-0.309604766890619,
92.2478981624538));
#9278=CARTESIAN_POINT('Ctrl Pts',(-1.99107547179722,-0.139222425586477,
92.237957398685));
#9279=CARTESIAN_POINT('Ctrl Pts',(-1.99469315035772,-0.0704487531436606,
92.2339810148349));
#9280=CARTESIAN_POINT('Ctrl Pts',(-1.99474933524002,-0.00162851450148592,
92.2299465820693));
#9281=CARTESIAN_POINT('Ctrl Pts',(-1.66701720851066,1.09548217193587,92.1551526428301));
#9282=CARTESIAN_POINT('Ctrl Pts',(-1.70501540924007,1.03765954722219,92.1595796013792));
#9283=CARTESIAN_POINT('Ctrl Pts',(-1.74006413474923,0.977762240127359,92.1640065599282));
#9284=CARTESIAN_POINT('Ctrl Pts',(-1.77193162675481,0.916125467720477,92.1684335184773));
#9285=CARTESIAN_POINT('Ctrl Pts',(-1.80376472481447,0.854555218647657,92.1728556990987));
#9286=CARTESIAN_POINT('Ctrl Pts',(-1.83242317544167,0.791249665360261,92.17727787972));
#9287=CARTESIAN_POINT('Ctrl Pts',(-1.85771941210735,0.726571502592491,92.1817000603414));
#9288=CARTESIAN_POINT('Ctrl Pts',(-1.88300011777082,0.661933049948511,92.1861195258989));
#9289=CARTESIAN_POINT('Ctrl Pts',(-1.90492252194614,0.595924117470595,92.1905389914565));
#9290=CARTESIAN_POINT('Ctrl Pts',(-1.92334651255382,0.528928875319798,92.194958457014));
#9291=CARTESIAN_POINT('Ctrl Pts',(-1.9417636630176,0.461958506015848,92.199376281788));
#9292=CARTESIAN_POINT('Ctrl Pts',(-1.95668485112832,0.394003031190437,92.203794106562));
#9293=CARTESIAN_POINT('Ctrl Pts',(-1.96801992106826,0.325461445917162,92.208211931336));
#9294=CARTESIAN_POINT('Ctrl Pts',(-1.97935880191346,0.256896816631853,92.2126312414041));
#9295=CARTESIAN_POINT('Ctrl Pts',(-1.98710907499091,0.18774617111172,92.2170505514721));
#9296=CARTESIAN_POINT('Ctrl Pts',(-1.99123202715443,0.11841696050171,92.2214698615402));
#9297=CARTESIAN_POINT('Ctrl Pts',(-1.993610686127,0.0784187887213646,92.2240194985791));
#9298=CARTESIAN_POINT('Ctrl Pts',(-1.99478295639525,0.0383612921081724,
92.226569135618));
#9299=CARTESIAN_POINT('Ctrl Pts',(-1.99474929503159,-0.00167704232401422,
92.229118772657));
#9300=CARTESIAN_POINT('',(-1.99474967489821,0.00113885621706795,92.0696038375131));
#9301=CARTESIAN_POINT('Ctrl Pts',(-1.66701737487202,1.09548191878041,91.9972724317));
#9302=CARTESIAN_POINT('Ctrl Pts',(-1.69219537653955,1.0571680356165,92.000471981164));
#9303=CARTESIAN_POINT('Ctrl Pts',(-1.71605789380988,1.017977927257,92.0036711945253));
#9304=CARTESIAN_POINT('Ctrl Pts',(-1.7674044424413,0.926698891525834,92.0109141311246));
#9305=CARTESIAN_POINT('Ctrl Pts',(-1.79397031634323,0.874163037773306,92.0149358977278));
#9306=CARTESIAN_POINT('Ctrl Pts',(-1.82632555717588,0.802468062534797,92.0201647506246));
#9307=CARTESIAN_POINT('Ctrl Pts',(-1.83420553094384,0.784289599424951,92.0214689004776));
#9308=CARTESIAN_POINT('Ctrl Pts',(-1.84698924707399,0.753551545934536,92.0236343527134));
#9309=CARTESIAN_POINT('Ctrl Pts',(-1.85203870088538,0.741054589587858,92.0245037834866));
#9310=CARTESIAN_POINT('Ctrl Pts',(-1.8627016202186,0.713874826225009,92.0263701732936));
#9311=CARTESIAN_POINT('Ctrl Pts',(-1.86826883068011,0.699175377519772,92.0273645315911));
#9312=CARTESIAN_POINT('Ctrl Pts',(-1.8845335188224,0.654648736378609,92.0303358761883));
#9313=CARTESIAN_POINT('Ctrl Pts',(-1.89469511400359,0.6246296737299,92.0322845171412));
#9314=CARTESIAN_POINT('Ctrl Pts',(-1.91768981397806,0.550964476823735,92.0369635411917));
#9315=CARTESIAN_POINT('Ctrl Pts',(-1.92975387028652,0.507096192033644,92.0396637559236));
#9316=CARTESIAN_POINT('Ctrl Pts',(-1.97639160174966,0.311587330246312,92.0514701542936));
#9317=CARTESIAN_POINT('Ctrl Pts',(-1.99466089793704,0.156635056505689,92.0602755466886));
#9318=CARTESIAN_POINT('Ctrl Pts',(-1.99474967489821,0.00113885621706795,
92.0696038375131));
#9319=CARTESIAN_POINT('Ctrl Pts',(-1.99474967628819,0.00113641901575271,
92.069603983722));
#9320=CARTESIAN_POINT('Ctrl Pts',(-1.99476815930295,-0.0313067090923167,
92.0715502633252));
#9321=CARTESIAN_POINT('Ctrl Pts',(-1.99399514718505,-0.0637444795486412,
92.0735154383802));
#9322=CARTESIAN_POINT('Ctrl Pts',(-1.99109370651439,-0.123869624873462,
92.0772043722034));
#9323=CARTESIAN_POINT('Ctrl Pts',(-1.98917761274169,-0.151559029694067,
92.0789215260781));
#9324=CARTESIAN_POINT('Ctrl Pts',(-1.9846989271426,-0.201212005455588,92.0820386507972));
#9325=CARTESIAN_POINT('Ctrl Pts',(-1.98234763062877,-0.223190300630611,
92.0834318024355));
#9326=CARTESIAN_POINT('Ctrl Pts',(-1.97694509971369,-0.266821314003556,
92.0862262487283));
#9327=CARTESIAN_POINT('Ctrl Pts',(-1.97390207845581,-0.288471943710301,
92.0876270977286));
#9328=CARTESIAN_POINT('Ctrl Pts',(-1.96486297577387,-0.345916170498519,
92.0913835897934));
#9329=CARTESIAN_POINT('Ctrl Pts',(-1.95824514205408,-0.381602132725231,
92.093758594248));
#9330=CARTESIAN_POINT('Ctrl Pts',(-1.92253348233093,-0.548621053328147,
92.105076283791));
#9331=CARTESIAN_POINT('Ctrl Pts',(-1.8811808201895,-0.676955081330919,92.1143990859579));
#9332=CARTESIAN_POINT('Ctrl Pts',(-1.79851367188029,-0.865740088117418,
92.12878224574));
#9333=CARTESIAN_POINT('Ctrl Pts',(-1.7662707031514,-0.929755870915924,92.1337808611449));
#9334=CARTESIAN_POINT('Ctrl Pts',(-1.71594042541975,-1.01757135162152,92.1407053723335));
#9335=CARTESIAN_POINT('Ctrl Pts',(-1.70065764708605,-1.04291262395225,92.1427116766899));
#9336=CARTESIAN_POINT('Ctrl Pts',(-1.67232555717517,-1.08761166310955,92.146253346622));
#9337=CARTESIAN_POINT('Ctrl Pts',(-1.6594896710628,-1.1070980284683,92.1477982892483));
#9338=CARTESIAN_POINT('Ctrl Pts',(-1.63835559680957,-1.13798820544017,92.1502433588491));
#9339=CARTESIAN_POINT('Ctrl Pts',(-1.63027356029034,-1.14953659072281,92.1511565267063));
#9340=CARTESIAN_POINT('Ctrl Pts',(-1.61363733911933,-1.17277959791909,92.1529909428631));
#9341=CARTESIAN_POINT('Ctrl Pts',(-1.60507686729099,-1.18446854280788,92.1539117224658));
#9342=CARTESIAN_POINT('Ctrl Pts',(-1.58123720889065,-1.21628740220106,92.1564165141851));
#9343=CARTESIAN_POINT('Ctrl Pts',(-1.565701167694,-1.23622253140346,92.1579839279255));
#9344=CARTESIAN_POINT('Ctrl Pts',(-1.46850819467474,-1.35616336391058,92.1674397269088));
#9345=CARTESIAN_POINT('Ctrl Pts',(-1.37767138002826,-1.44835238372914,92.174832417256));
#9346=CARTESIAN_POINT('Ctrl Pts',(-1.20651129000893,-1.59127831962814,92.1877771006588));
#9347=CARTESIAN_POINT('Ctrl Pts',(-1.13031988870464,-1.64627184677635,92.1932612864709));
#9348=CARTESIAN_POINT('Ctrl Pts',(-1.01577335023588,-1.71723769631638,92.2014027876154));
#9349=CARTESIAN_POINT('Ctrl Pts',(-0.98034823541893,-1.73770474739748,92.2039064470741));
#9350=CARTESIAN_POINT('Ctrl Pts',(-0.922187429267494,-1.76896277328122,
92.2080109138262));
#9351=CARTESIAN_POINT('Ctrl Pts',(-0.89983214263199,-1.7804384209886,92.2095870928512));
#9352=CARTESIAN_POINT('Ctrl Pts',(-0.85605686821332,-1.80187456212417,92.2126739799368));
#9353=CARTESIAN_POINT('Ctrl Pts',(-0.834664915709949,-1.81188291516373,
92.214182678758));
#9354=CARTESIAN_POINT('Ctrl Pts',(-0.782332780157432,-1.83524339258574,
92.2178763408885));
#9355=CARTESIAN_POINT('Ctrl Pts',(-0.751223123118983,-1.84819546526699,
92.2200745519905));
#9356=CARTESIAN_POINT('Ctrl Pts',(-0.572070556305459,-1.91751261430636,
92.2327549983201));
#9357=CARTESIAN_POINT('Ctrl Pts',(-0.418078800007309,-1.9568628735305,92.2438024117842));
#9358=CARTESIAN_POINT('Ctrl Pts',(-0.180610869034097,-1.98821459869155,
92.2605007860614));
#9359=CARTESIAN_POINT('Ctrl Pts',(-0.0995498011176361,-1.99391815172663,
92.2661293205249));
#9360=CARTESIAN_POINT('Ctrl Pts',(0.00600012830176016,-1.99488973904457,
92.2732053170416));
#9361=CARTESIAN_POINT('Ctrl Pts',(0.0303645644341954,-1.99466769008684,
92.2748209310496));
#9362=CARTESIAN_POINT('Ctrl Pts',(0.0690181916411301,-1.99360694258104,
92.2773496155312));
#9363=CARTESIAN_POINT('Ctrl Pts',(0.083312203281262,-1.9930607767081,92.2782772284045));
#9364=CARTESIAN_POINT('Ctrl Pts',(0.110098035469349,-1.99174862121941,92.2799999046068));
#9365=CARTESIAN_POINT('Ctrl Pts',(0.122590798061702,-1.99101875016146,92.2807969743612));
#9366=CARTESIAN_POINT('Ctrl Pts',(0.157239976173884,-1.98866705251675,92.2829920247745));
#9367=CARTESIAN_POINT('Ctrl Pts',(0.179378124642974,-1.98679255132669,92.2843767087599));
#9368=CARTESIAN_POINT('Ctrl Pts',(0.332357579302097,-1.97126130246421,92.2938504944873));
#9369=CARTESIAN_POINT('Ctrl Pts',(0.461615382922778,-1.94505853645239,92.3013900749511));
#9370=CARTESIAN_POINT('Ctrl Pts',(0.687630253288546,-1.87541993108513,92.3151134721051));
#9371=CARTESIAN_POINT('Ctrl Pts',(0.785293372111633,-1.83666726471702,92.3212396356086));
#9372=CARTESIAN_POINT('Ctrl Pts',(0.912623034940053,-1.77412305952781,92.3298548294559));
#9373=CARTESIAN_POINT('Ctrl Pts',(0.945333952688054,-1.7569111772095,92.3321265918226));
#9374=CARTESIAN_POINT('Ctrl Pts',(0.998820004138919,-1.72684155814258,92.3359515751138));
#9375=CARTESIAN_POINT('Ctrl Pts',(1.01987150916701,-1.71449269095366,92.3374864431387));
#9376=CARTESIAN_POINT('Ctrl Pts',(1.06152088476724,-1.68902254371992,92.340585479545));
#9377=CARTESIAN_POINT('Ctrl Pts',(1.08211487578369,-1.67590305494017,92.3421493946391));
#9378=CARTESIAN_POINT('Ctrl Pts',(1.1333173489969,-1.6419470449696,92.3461205773597));
#9379=CARTESIAN_POINT('Ctrl Pts',(1.16359504893925,-1.62063091736894,92.3485456144877));
#9380=CARTESIAN_POINT('Ctrl Pts',(1.29657722448443,-1.52136048375288,92.3595533379029));
#9381=CARTESIAN_POINT('Ctrl Pts',(1.39215854268234,-1.43441119369384,92.3684781384058));
#9382=CARTESIAN_POINT('Ctrl Pts',(1.52859241424551,-1.28373081793755,92.3826631260226));
#9383=CARTESIAN_POINT('Ctrl Pts',(1.57539338828112,-1.22584505927741,92.3878590973772));
#9384=CARTESIAN_POINT('Ctrl Pts',(1.63649785459933,-1.14097076994958,92.3950192067337));
#9385=CARTESIAN_POINT('Ctrl Pts',(1.65358425681368,-1.11606398332346,92.3970684686953));
#9386=CARTESIAN_POINT('Ctrl Pts',(1.68305038840129,-1.07094812764809,92.4006767969649));
#9387=CARTESIAN_POINT('Ctrl Pts',(1.69564797344349,-1.05088846742278,92.4022459356625));
#9388=CARTESIAN_POINT('Ctrl Pts',(1.71520477076662,-1.01847966244255,92.4047196196261));
#9389=CARTESIAN_POINT('Ctrl Pts',(1.72239452261107,-1.00627301064675,92.4056377148263));
#9390=CARTESIAN_POINT('Ctrl Pts',(1.73573820717803,-0.983056196120208,92.4073568373933));
#9391=CARTESIAN_POINT('Ctrl Pts',(1.74191885440136,-0.972062412678964,92.4081596425926));
#9392=CARTESIAN_POINT('Ctrl Pts',(1.75896963249874,-0.94104851785814,92.410395122327));
#9393=CARTESIAN_POINT('Ctrl Pts',(1.76960205299495,-0.920899103926255,92.4118136511195));
#9394=CARTESIAN_POINT('Ctrl Pts',(1.83699204524145,-0.787709596826022,92.4209997007485));
#9395=CARTESIAN_POINT('Ctrl Pts',(1.88323969305942,-0.669658356904713,92.4282659318206));
#9396=CARTESIAN_POINT('Ctrl Pts',(1.9476831258567,-0.44411064011118,92.4418721483562));
#9397=CARTESIAN_POINT('Ctrl Pts',(1.96887517062733,-0.337981237456235,92.448170376723));
#9398=CARTESIAN_POINT('Ctrl Pts',(1.98568838712542,-0.193557930276693,92.4569955553312));
#9399=CARTESIAN_POINT('Ctrl Pts',(1.98896466913657,-0.15634037400082,92.4592907518267));
#9400=CARTESIAN_POINT('Ctrl Pts',(1.99265484680723,-0.0946219287196938,
92.4631438043902));
#9401=CARTESIAN_POINT('Ctrl Pts',(1.99366581253361,-0.0701654480856943,
92.4646827019488));
#9402=CARTESIAN_POINT('Ctrl Pts',(1.99478425822608,-0.0213566764327326,
92.467781019639));
#9403=CARTESIAN_POINT('Ctrl Pts',(1.994896315478,0.00299127359219256,92.4693400233891));
#9404=CARTESIAN_POINT('Ctrl Pts',(1.9940607197209,0.0639640262856332,92.4732802494589));
#9405=CARTESIAN_POINT('Ctrl Pts',(1.99254981671886,0.100570790967986,92.4756786593363));
#9406=CARTESIAN_POINT('Ctrl Pts',(1.98351299647704,0.231729203991478,92.4843946324364));
#9407=CARTESIAN_POINT('Ctrl Pts',(1.97025543103971,0.325747885601911,92.4908797553944));
#9408=CARTESIAN_POINT('Ctrl Pts',(1.93321044483757,0.498409033692966,92.5031387257009));
#9409=CARTESIAN_POINT('Ctrl Pts',(1.91115664424411,0.577229874277698,92.5088742771932));
#9410=CARTESIAN_POINT('Ctrl Pts',(1.86965981403512,0.696705358554105,92.517641911271));
#9411=CARTESIAN_POINT('Ctrl Pts',(1.85357548667641,0.738433834987035,92.5207177122762));
#9412=CARTESIAN_POINT('Ctrl Pts',(1.82386280549038,0.808413695952085,92.5258631834048));
#9413=CARTESIAN_POINT('Ctrl Pts',(1.81094608765506,0.836948478242977,92.5279574710078));
#9414=CARTESIAN_POINT('Ctrl Pts',(1.79057389348865,0.87927108546852,92.5310456031421));
#9415=CARTESIAN_POINT('Ctrl Pts',(1.78361978028004,0.893293360548532,92.5320657014294));
#9416=CARTESIAN_POINT('Ctrl Pts',(1.77036206543856,0.919253998929284,92.5339465634377));
#9417=CARTESIAN_POINT('Ctrl Pts',(1.7641015614015,0.931211816650328,92.5348095751338));
#9418=CARTESIAN_POINT('Ctrl Pts',(1.74828863966369,0.960683242878534,92.5369298949156));
#9419=CARTESIAN_POINT('Ctrl Pts',(1.73859407198787,0.978118697683891,92.5381785490521));
#9420=CARTESIAN_POINT('Ctrl Pts',(1.6973480044638,1.04974728484298,92.5432967129143));
#9421=CARTESIAN_POINT('Ctrl Pts',(1.6635088644478,1.10258756480942,92.5470450258289));
#9422=CARTESIAN_POINT('Ctrl Pts',(1.5544104174522,1.25645852162732,92.5581458891424));
#9423=CARTESIAN_POINT('Ctrl Pts',(1.47202697515336,1.35204205087646,92.5653154421523));
#9424=CARTESIAN_POINT('Ctrl Pts',(1.34648623473052,1.47251987115408,92.5755693772603));
#9425=CARTESIAN_POINT('Ctrl Pts',(1.31060017425249,1.50454866920715,92.5784337306157));
#9426=CARTESIAN_POINT('Ctrl Pts',(1.24347023939924,1.56023754823306,92.5837153266097));
#9427=CARTESIAN_POINT('Ctrl Pts',(1.21261967764178,1.58433350265185,92.5861153275308));
#9428=CARTESIAN_POINT('Ctrl Pts',(1.16109548349719,1.62218985668829,92.5900944879414));
#9429=CARTESIAN_POINT('Ctrl Pts',(1.14083777701438,1.63649984131077,92.5916519042782));
#9430=CARTESIAN_POINT('Ctrl Pts',(1.10062225286171,1.66379835284803,92.5947331400346));
#9431=CARTESIAN_POINT('Ctrl Pts',(1.0806882295598,1.676814590656,92.5962555504483));
#9432=CARTESIAN_POINT('Ctrl Pts',(1.03098094237594,1.70801721083492,92.6000422852632));
#9433=CARTESIAN_POINT('Ctrl Pts',(1.00095538791277,1.72578461932781,92.6023215319823));
#9434=CARTESIAN_POINT('Ctrl Pts',(0.839566503058463,1.81565660722181,92.6145375633317));
#9435=CARTESIAN_POINT('Ctrl Pts',(0.700873915672799,1.87356401295225,92.6249672194005));
#9436=CARTESIAN_POINT('Ctrl Pts',(0.49610438072653,1.93311532000006,92.6398431270132));
#9437=CARTESIAN_POINT('Ctrl Pts',(0.434357593804084,1.94791905622915,92.6442570940759));
#9438=CARTESIAN_POINT('Ctrl Pts',(0.333336152459379,1.9670953042262,92.6512739442206));
#9439=CARTESIAN_POINT('Ctrl Pts',(0.294452992895344,1.97329035287538,92.6539262460606));
#9440=CARTESIAN_POINT('Ctrl Pts',(0.238560656324332,1.98050624430187,92.6576468419131));
#9441=CARTESIAN_POINT('Ctrl Pts',(0.221684207796456,1.98246622439639,92.6587583271979));
#9442=CARTESIAN_POINT('Ctrl Pts',(0.191560436821653,1.98557520357651,92.6607186031166));
#9443=CARTESIAN_POINT('Ctrl Pts',(0.178323941693687,1.98680771154917,92.6615716197845));
#9444=CARTESIAN_POINT('Ctrl Pts',(0.14756488091511,1.98936192843031,92.6635350663576));
#9445=CARTESIAN_POINT('Ctrl Pts',(0.130035708517556,1.99058459823705,92.6646401775549));
#9446=CARTESIAN_POINT('Ctrl Pts',(0.0723021803309049,1.99384561271655,92.6682411991543));
#9447=CARTESIAN_POINT('Ctrl Pts',(0.0320499559405096,1.99489879431462,92.6706901911525));
#9448=CARTESIAN_POINT('Ctrl Pts',(-0.155797303403388,1.99412570932591,92.6819446811642));
#9449=CARTESIAN_POINT('Ctrl Pts',(-0.302869596073771,1.97714092263479,92.6902856592983));
#9450=CARTESIAN_POINT('Ctrl Pts',(-0.496328578656435,1.93268606047646,92.7019533132019));
#9451=CARTESIAN_POINT('Ctrl Pts',(-0.54547001421628,1.91939559110178,92.7049762794578));
#9452=CARTESIAN_POINT('Ctrl Pts',(-0.632941426173635,1.89210799916847,92.7105136017045));
#9453=CARTESIAN_POINT('Ctrl Pts',(-0.671452364808724,1.87878655045879,92.7130077213859));
#9454=CARTESIAN_POINT('Ctrl Pts',(-0.732982038367703,1.85536916631048,92.7171006113603));
#9455=CARTESIAN_POINT('Ctrl Pts',(-0.756266077986385,1.8460007961403,92.7186750234803));
#9456=CARTESIAN_POINT('Ctrl Pts',(-0.801119128896851,1.82696309018992,92.7217611632136));
#9457=CARTESIAN_POINT('Ctrl Pts',(-0.822705296035073,1.81734474105831,92.7232709344411));
#9458=CARTESIAN_POINT('Ctrl Pts',(-0.874732667651834,1.79304552892249,92.7269722129532));
#9459=CARTESIAN_POINT('Ctrl Pts',(-0.904980578709403,1.77797059267601,92.729177105323));
#9460=CARTESIAN_POINT('Ctrl Pts',(-1.0741618171987,1.68821834140363,92.7418211758236));
#9461=CARTESIAN_POINT('Ctrl Pts',(-1.2042141765976,1.59804757812337,92.7528195916793));
#9462=CARTESIAN_POINT('Ctrl Pts',(-1.38333298708292,1.43946836765162,92.7694982137849));
#9463=CARTESIAN_POINT('Ctrl Pts',(-1.44103041200812,1.38170651202603,92.7751541092078));
#9464=CARTESIAN_POINT('Ctrl Pts',(-1.51119050239875,1.30227743026863,92.7822590581783));
#9465=CARTESIAN_POINT('Ctrl Pts',(-1.52701197316126,1.2836891378177,92.7838777248946));
#9466=CARTESIAN_POINT('Ctrl Pts',(-1.55156404018349,1.25374695583476,92.786409995634));
#9467=CARTESIAN_POINT('Ctrl Pts',(-1.56051993562089,1.2425819736411,92.7873382094275));
#9468=CARTESIAN_POINT('Ctrl Pts',(-1.57815319761975,1.22010785991952,92.7891732460102));
#9469=CARTESIAN_POINT('Ctrl Pts',(-1.58683105974168,1.20880019916237,92.7900800745711));
#9470=CARTESIAN_POINT('Ctrl Pts',(-1.60986288414226,1.17811314671413,92.7925000623752));
#9471=CARTESIAN_POINT('Ctrl Pts',(-1.62398831827379,1.15856426500583,92.7939984641872));
#9472=CARTESIAN_POINT('Ctrl Pts',(-1.64770140204872,1.12446036815093,92.7965481036753));
#9473=CARTESIAN_POINT('Ctrl Pts',(-1.65745570970042,1.11003209729936,92.7976075187219));
#9474=CARTESIAN_POINT('Ctrl Pts',(-1.66701723320527,1.09548213435758,92.7986587716037));
#9475=CARTESIAN_POINT('Origin',(0.,0.,89.2710285354474));
#9476=CARTESIAN_POINT('',(-1.66701713450993,1.09548228454426,93.7559248887299));
#9477=CARTESIAN_POINT('',(-1.66701733785599,1.09548197510845,93.5957235785224));
#9478=CARTESIAN_POINT('',(-1.66701720851066,1.09548217193587,89.2710285354474));
#9479=CARTESIAN_POINT('Ctrl Pts',(-1.66701713450993,1.09548228454426,93.7559248887299));
#9480=CARTESIAN_POINT('Ctrl Pts',(-1.63542234952196,1.14356069592451,93.7525427819055));
#9481=CARTESIAN_POINT('Ctrl Pts',(-1.60175109836394,1.19026704693653,93.7491185570963));
#9482=CARTESIAN_POINT('Ctrl Pts',(-1.54306510953131,1.26465803650423,93.7433659959786));
#9483=CARTESIAN_POINT('Ctrl Pts',(-1.51922723760391,1.29319689533183,93.7410811748776));
#9484=CARTESIAN_POINT('Ctrl Pts',(-1.47841484587907,1.33937108039223,93.7372402368012));
#9485=CARTESIAN_POINT('Ctrl Pts',(-1.4618878920162,1.35739053083534,93.7357028037696));
#9486=CARTESIAN_POINT('Ctrl Pts',(-1.42822317223878,1.39276733554216,93.732603267755));
#9487=CARTESIAN_POINT('Ctrl Pts',(-1.41108995532366,1.41012316162491,93.7310415046378));
#9488=CARTESIAN_POINT('Ctrl Pts',(-1.36729464985399,1.45288994709965,93.7270855334408));
#9489=CARTESIAN_POINT('Ctrl Pts',(-1.34023989165373,1.47788382209803,93.7246738541496));
#9490=CARTESIAN_POINT('Ctrl Pts',(-1.21310414035976,1.58897197145637,93.713477938339));
#9491=CARTESIAN_POINT('Ctrl Pts',(-1.10533562312598,1.66573610214229,93.7043317525641));
#9492=CARTESIAN_POINT('Ctrl Pts',(-0.900776132060031,1.78280329532145,93.6878833589033));
#9493=CARTESIAN_POINT('Ctrl Pts',(-0.806867613665749,1.8272256071364,93.6806395734607));
#9494=CARTESIAN_POINT('Ctrl Pts',(-0.688664218951933,1.87224107944017,93.6721834399008));
#9495=CARTESIAN_POINT('Ctrl Pts',(-0.667266915805027,1.87997341354761,93.6706783953537));
#9496=CARTESIAN_POINT('Ctrl Pts',(-0.632510311839856,1.89186516681706,93.66828012238));
#9497=CARTESIAN_POINT('Ctrl Pts',(-0.619231775508093,1.89625292433228,93.6673746904563));
#9498=CARTESIAN_POINT('Ctrl Pts',(-0.591956855281497,1.90494856766909,93.6655384661907));
#9499=CARTESIAN_POINT('Ctrl Pts',(-0.577957162684838,1.90924265463408,93.6646084317539));
#9500=CARTESIAN_POINT('Ctrl Pts',(-0.538942904382735,1.9207409141232,93.6620478302636));
#9501=CARTESIAN_POINT('Ctrl Pts',(-0.51383184360503,1.92761046360899,93.6604351136759));
#9502=CARTESIAN_POINT('Ctrl Pts',(-0.364238945804778,1.96540281758391,93.6509970658309));
#9503=CARTESIAN_POINT('Ctrl Pts',(-0.237131541205012,1.98475546695384,93.6436530643455));
#9504=CARTESIAN_POINT('Ctrl Pts',(-0.0159020677013387,1.99686611905797,
93.6307903400082));
#9505=CARTESIAN_POINT('Ctrl Pts',(0.0774671278218953,1.99542574557168,93.6253391504231));
#9506=CARTESIAN_POINT('Ctrl Pts',(0.211189295057473,1.9839616263326,93.6172304543193));
#9507=CARTESIAN_POINT('Ctrl Pts',(0.251872146285257,1.97920810452988,93.6147240332468));
#9508=CARTESIAN_POINT('Ctrl Pts',(0.317246763879554,1.96952128542069,93.6106159510326));
#9509=CARTESIAN_POINT('Ctrl Pts',(0.342042807810405,1.96536669054304,93.609038992585));
#9510=CARTESIAN_POINT('Ctrl Pts',(0.389969561788923,1.95640210028981,93.6059511533259));
#9511=CARTESIAN_POINT('Ctrl Pts',(0.413106449407846,1.95164761652855,93.6044422942812));
#9512=CARTESIAN_POINT('Ctrl Pts',(0.463821976024148,1.94028368203812,93.6010926142209));
#9513=CARTESIAN_POINT('Ctrl Pts',(0.491354682476796,1.93349477127464,93.5992462864226));
#9514=CARTESIAN_POINT('Ctrl Pts',(0.594922068193883,1.90560258747591,93.5921919718257));
#9515=CARTESIAN_POINT('Ctrl Pts',(0.669818411294887,1.88058346954879,93.5868620405255));
#9516=CARTESIAN_POINT('Ctrl Pts',(0.884090929361408,1.79457930315383,93.5709818855701));
#9517=CARTESIAN_POINT('Ctrl Pts',(1.0182113577112,1.72202650218283,93.5601865710314));
#9518=CARTESIAN_POINT('Ctrl Pts',(1.16969257161417,1.61614487213413,93.5476564622014));
#9519=CARTESIAN_POINT('Ctrl Pts',(1.19612934275542,1.5966777504839,93.5454579227881));
#9520=CARTESIAN_POINT('Ctrl Pts',(1.23466016862367,1.56681057405204,93.5422498259342));
#9521=CARTESIAN_POINT('Ctrl Pts',(1.24712834807564,1.55690463132253,93.5412111191029));
#9522=CARTESIAN_POINT('Ctrl Pts',(1.26989398043794,1.53836838629555,93.5393155168166));
#9523=CARTESIAN_POINT('Ctrl Pts',(1.28022437495878,1.52978219818604,93.5384559624389));
#9524=CARTESIAN_POINT('Ctrl Pts',(1.30529226701484,1.50851502628617,93.5363702730614));
#9525=CARTESIAN_POINT('Ctrl Pts',(1.31993242984823,1.4957218778217,93.5351520793587));
#9526=CARTESIAN_POINT('Ctrl Pts',(1.37590909033274,1.44534517420562,93.5304831569122));
#9527=CARTESIAN_POINT('Ctrl Pts',(1.41584981420338,1.4062428295479,93.52712738481));
#9528=CARTESIAN_POINT('Ctrl Pts',(1.5444669328074,1.26928169552506,93.5160208047763));
#9529=CARTESIAN_POINT('Ctrl Pts',(1.62506047987489,1.16431736586136,93.5085201825453));
#9530=CARTESIAN_POINT('Ctrl Pts',(1.72052360439719,1.01055619696129,93.4978634622076));
#9531=CARTESIAN_POINT('Ctrl Pts',(1.7448097841133,0.96802048697242,93.4949493176046));
#9532=CARTESIAN_POINT('Ctrl Pts',(1.78588409374039,0.889504135852703,93.4895870781914));
#9533=CARTESIAN_POINT('Ctrl Pts',(1.80321019461239,0.85383386781165,93.4871571365949));
#9534=CARTESIAN_POINT('Ctrl Pts',(1.82966779540116,0.794961202009411,93.4831415325032));
#9535=CARTESIAN_POINT('Ctrl Pts',(1.83944793001755,0.772061381717299,93.4815784277842));
#9536=CARTESIAN_POINT('Ctrl Pts',(1.85771576220401,0.726969035081655,93.478495111394));
#9537=CARTESIAN_POINT('Ctrl Pts',(1.86624068370553,0.704796041886973,93.4769764838878));
#9538=CARTESIAN_POINT('Ctrl Pts',(1.88618329361931,0.650025282652543,93.4732167961798));
#9539=CARTESIAN_POINT('Ctrl Pts',(1.89715384104378,0.617274121355461,93.4709613146153));
#9540=CARTESIAN_POINT('Ctrl Pts',(1.95192163866515,0.438488075045035,93.4586022210182));
#9541=CARTESIAN_POINT('Ctrl Pts',(1.97970989498057,0.28810302838385,93.4479843390764));
#9542=CARTESIAN_POINT('Ctrl Pts',(1.99604001308518,0.0492366612757203,93.4312855684801));
#9543=CARTESIAN_POINT('Ctrl Pts',(1.9962884106473,-0.0378834358126214,93.4252433147478));
#9544=CARTESIAN_POINT('Ctrl Pts',(1.98938237459944,-0.148096772724516,93.4178523196876));
#9545=CARTESIAN_POINT('Ctrl Pts',(1.98750856810158,-0.17141964038473,93.4163030070519));
#9546=CARTESIAN_POINT('Ctrl Pts',(1.98384746537211,-0.208748418053945,93.4138525697228));
#9547=CARTESIAN_POINT('Ctrl Pts',(1.98232112604231,-0.22277714930768,93.4129383160795));
#9548=CARTESIAN_POINT('Ctrl Pts',(1.97892720571701,-0.251165926479747,93.4111033170167));
#9549=CARTESIAN_POINT('Ctrl Pts',(1.97705189507359,-0.265524092341655,93.4101830148195));
#9550=CARTESIAN_POINT('Ctrl Pts',(1.97148237757333,-0.304828984847685,93.4076819529907));
#9551=CARTESIAN_POINT('Ctrl Pts',(1.96747108398963,-0.329728897913695,93.4061177032218));
#9552=CARTESIAN_POINT('Ctrl Pts',(1.94536349641327,-0.452129863912211,93.3984984328528));
#9553=CARTESIAN_POINT('Ctrl Pts',(1.92048468622102,-0.548272938864789,93.3927297738895));
#9554=CARTESIAN_POINT('Ctrl Pts',(1.85867525994805,-0.730046628860321,93.3815915412368));
#9555=CARTESIAN_POINT('Ctrl Pts',(1.82270008116151,-0.815723743515311,93.3762326014404));
#9556=CARTESIAN_POINT('Ctrl Pts',(1.76199549100926,-0.936033779889465,93.3682377811264));
#9557=CARTESIAN_POINT('Ctrl Pts',(1.74192245224126,-0.972878820870892,93.3657220846679));
#9558=CARTESIAN_POINT('Ctrl Pts',(1.7027555322045,-1.03966823085816,93.3610100861994));
#9559=CARTESIAN_POINT('Ctrl Pts',(1.68399491551085,-1.06978844545612,93.358825257753));
#9560=CARTESIAN_POINT('Ctrl Pts',(1.65113115363754,-1.11954310308252,93.3551036202207));
#9561=CARTESIAN_POINT('Ctrl Pts',(1.63745598321047,-1.13945103735588,93.353582967134));
#9562=CARTESIAN_POINT('Ctrl Pts',(1.61074813931592,-1.17685759659768,93.3506622647059));
#9563=CARTESIAN_POINT('Ctrl Pts',(1.59778316899034,-1.1944003738574,93.3492649895696));
#9564=CARTESIAN_POINT('Ctrl Pts',(1.56270203298898,-1.24027478428027,93.3455354534106));
#9565=CARTESIAN_POINT('Ctrl Pts',(1.54010425564317,-1.26822623680201,93.3431843645177));
#9566=CARTESIAN_POINT('Ctrl Pts',(1.42494620494502,-1.40304744435642,93.3314409294363));
#9567=CARTESIAN_POINT('Ctrl Pts',(1.32197317531648,-1.50046278816646,93.3216212580264));
#9568=CARTESIAN_POINT('Ctrl Pts',(1.13400042410198,-1.64380890371644,93.3051250021431));
#9569=CARTESIAN_POINT('Ctrl Pts',(1.05437805064002,-1.69598190605259,93.2985041838583));
#9570=CARTESIAN_POINT('Ctrl Pts',(0.950923003430365,-1.75365875039872,93.2905769948661));
#9571=CARTESIAN_POINT('Ctrl Pts',(0.930314193468688,-1.76467821069174,93.2890296093495));
#9572=CARTESIAN_POINT('Ctrl Pts',(0.896962074551349,-1.78176472829155,93.2865814463969));
#9573=CARTESIAN_POINT('Ctrl Pts',(0.88434024567389,-1.78806288405536,93.2856675805637));
#9574=CARTESIAN_POINT('Ctrl Pts',(0.858622418064512,-1.80055684321425,93.2838325567028));
#9575=CARTESIAN_POINT('Ctrl Pts',(0.84552370977621,-1.8067448879044,93.2829118550947));
#9576=CARTESIAN_POINT('Ctrl Pts',(0.809411081498878,-1.8233263154625,93.2804083573384));
#9577=CARTESIAN_POINT('Ctrl Pts',(0.786264652228859,-1.83342662411646,93.2788421250531));
#9578=CARTESIAN_POINT('Ctrl Pts',(0.675134937370769,-1.87942794485256,93.271474877985));
#9579=CARTESIAN_POINT('Ctrl Pts',(0.584844393176332,-1.90945471522781,93.2659351030583));
#9580=CARTESIAN_POINT('Ctrl Pts',(0.366720947273009,-1.96505943854661,93.2528700881494));
#9581=CARTESIAN_POINT('Ctrl Pts',(0.237863649597003,-1.98478224007977,93.2453809313963));
#9582=CARTESIAN_POINT('Ctrl Pts',(0.0682470178642263,-1.99397981054131,
93.2351038178705));
#9583=CARTESIAN_POINT('Ctrl Pts',(0.0284327365951741,-1.99494470895301,
93.2326638763106));
#9584=CARTESIAN_POINT('Ctrl Pts',(-0.0363124433474292,-1.99457527449754,
93.2286361928083));
#9585=CARTESIAN_POINT('Ctrl Pts',(-0.0612372602153259,-1.99396565341182,
93.2270712849548));
#9586=CARTESIAN_POINT('Ctrl Pts',(-0.109856255472506,-1.991864082626,93.2239874877438));
#9587=CARTESIAN_POINT('Ctrl Pts',(-0.133548197247356,-1.99041596627606,
93.2224702412883));
#9588=CARTESIAN_POINT('Ctrl Pts',(-0.191517940135283,-1.98583306987759,
93.2187198485343));
#9589=CARTESIAN_POINT('Ctrl Pts',(-0.225750181422961,-1.98223326406348,
93.2164724484884));
#9590=CARTESIAN_POINT('Ctrl Pts',(-0.411879725121675,-1.95777639357405,
93.2040664700141));
#9591=CARTESIAN_POINT('Ctrl Pts',(-0.561056558839647,-1.92034719147979,
93.1933864311598));
#9592=CARTESIAN_POINT('Ctrl Pts',(-0.783055747182841,-1.83654870995879,
93.1768375736369));
#9593=CARTESIAN_POINT('Ctrl Pts',(-0.859718407371368,-1.80193618974015,
93.1710040094987));
#9594=CARTESIAN_POINT('Ctrl Pts',(-0.955795656056625,-1.75102600781155,
93.1637111095717));
#9595=CARTESIAN_POINT('Ctrl Pts',(-0.977401302949993,-1.73905843550621,
93.162072641649));
#9596=CARTESIAN_POINT('Ctrl Pts',(-1.01122214150283,-1.71949525666128,93.1595167903076));
#9597=CARTESIAN_POINT('Ctrl Pts',(-1.02358634144263,-1.71216389102741,93.158584366459));
#9598=CARTESIAN_POINT('Ctrl Pts',(-1.04800884303798,-1.69732341220236,93.1567481423143));
#9599=CARTESIAN_POINT('Ctrl Pts',(-1.06006828143407,-1.6898179089451,93.1558442256011));
#9600=CARTESIAN_POINT('Ctrl Pts',(-1.09216670589695,-1.66936175380594,93.1534428921319));
#9601=CARTESIAN_POINT('Ctrl Pts',(-1.11205589586242,-1.65617890984342,93.1519598293279));
#9602=CARTESIAN_POINT('Ctrl Pts',(-1.22654571179452,-1.57730067901706,93.1434217396586));
#9603=CARTESIAN_POINT('Ctrl Pts',(-1.31556089751201,-1.50386084621574,93.1367707306215));
#9604=CARTESIAN_POINT('Ctrl Pts',(-1.47757919337974,-1.34473346967987,93.1236042268181));
#9605=CARTESIAN_POINT('Ctrl Pts',(-1.55066524040848,-1.25975505137283,93.1171101707527));
#9606=CARTESIAN_POINT('Ctrl Pts',(-1.63973962949609,-1.13661308781823,93.107918319004));
#9607=CARTESIAN_POINT('Ctrl Pts',(-1.66225400167881,-1.10342496961415,93.1054620547317));
#9608=CARTESIAN_POINT('Ctrl Pts',(-1.69714745910588,-1.04849519934693,93.1014146453806));
#9609=CARTESIAN_POINT('Ctrl Pts',(-1.71014512693099,-1.02715881691861,93.0998467880661));
#9610=CARTESIAN_POINT('Ctrl Pts',(-1.73468822411039,-0.985112303192881,
93.0967621305723));
#9611=CARTESIAN_POINT('Ctrl Pts',(-1.74627190542321,-0.964429280296744,
93.0952470681473));
#9612=CARTESIAN_POINT('Ctrl Pts',(-1.77367434611226,-0.913388446268949,
93.0915114532353));
#9613=CARTESIAN_POINT('Ctrl Pts',(-1.78908504955663,-0.882821377165541,
93.0892769127863));
#9614=CARTESIAN_POINT('Ctrl Pts',(-1.86975554889749,-0.712015157965876,
93.0767972806393));
#9615=CARTESIAN_POINT('Ctrl Pts',(-1.91930871268802,-0.564968601757438,
93.0660192736889));
#9616=CARTESIAN_POINT('Ctrl Pts',(-1.96962984439087,-0.327614473729624,
93.0490995597353));
#9617=CARTESIAN_POINT('Ctrl Pts',(-1.98216658254263,-0.240398406497281,
93.0429930711034));
#9618=CARTESIAN_POINT('Ctrl Pts',(-1.99059247291952,-0.130603619848218,
93.0356398187603));
#9619=CARTESIAN_POINT('Ctrl Pts',(-1.99191700890647,-0.108546887912068,
93.0341796057686));
#9620=CARTESIAN_POINT('Ctrl Pts',(-1.99347565435247,-0.0726254471688885,
93.0318339437613));
#9621=CARTESIAN_POINT('Ctrl Pts',(-1.99393215967216,-0.0587726656381613,
93.0309372164655));
#9622=CARTESIAN_POINT('Ctrl Pts',(-1.99457817977182,-0.0300893687053928,
93.0290981675887));
#9623=CARTESIAN_POINT('Ctrl Pts',(-1.99474676737995,-0.0152595094716535,
93.0281569498896));
#9624=CARTESIAN_POINT('Ctrl Pts',(-1.99475574941179,0.0265445322984926,
93.0255273525876));
#9625=CARTESIAN_POINT('Ctrl Pts',(-1.99421444596626,0.0535165395315901,
93.0238584318743));
#9626=CARTESIAN_POINT('Ctrl Pts',(-1.99166871276284,0.116570099224328,93.0200045051092));
#9627=CARTESIAN_POINT('Ctrl Pts',(-1.98923067787367,0.152625152091631,93.0178372290286));
#9628=CARTESIAN_POINT('Ctrl Pts',(-1.97569999132832,0.295096090152994,93.0093496744791));
#9629=CARTESIAN_POINT('Ctrl Pts',(-1.95703410190557,0.400614195767204,93.0032246938392));
#9630=CARTESIAN_POINT('Ctrl Pts',(-1.90603995020134,0.59583853457678,92.9914713735557));
#9631=CARTESIAN_POINT('Ctrl Pts',(-1.8755814767033,0.685713634188596,92.9858815489744));
#9632=CARTESIAN_POINT('Ctrl Pts',(-1.8262909088681,0.802956805797081,92.9781042495431));
#9633=CARTESIAN_POINT('Ctrl Pts',(-1.81300356778381,0.832523869077009,92.9761002412399));
#9634=CARTESIAN_POINT('Ctrl Pts',(-1.78877841201611,0.883096504406376,92.9725901461986));
#9635=CARTESIAN_POINT('Ctrl Pts',(-1.77817579208428,0.90425572571023,92.9710959010078));
#9636=CARTESIAN_POINT('Ctrl Pts',(-1.75530454969179,0.947940497351477,92.9679544110535));
#9637=CARTESIAN_POINT('Ctrl Pts',(-1.74297295375286,0.97042796173567,92.9663051230171));
#9638=CARTESIAN_POINT('Ctrl Pts',(-1.71018699218662,1.02757345904019,92.9620278099911));
#9639=CARTESIAN_POINT('Ctrl Pts',(-1.68911241391379,1.06185945441587,92.959377899959));
#9640=CARTESIAN_POINT('Ctrl Pts',(-1.66701720827313,1.09548217229732,92.9566930507716));
#9641=CARTESIAN_POINT('Ctrl Pts',(-1.66701723320527,1.09548213435758,92.7986587716037));
#9642=CARTESIAN_POINT('Ctrl Pts',(-1.73358277777417,0.994188004171587,92.8059773982349));
#9643=CARTESIAN_POINT('Ctrl Pts',(-1.79080430631276,0.886996499275212,92.8129129536139));
#9644=CARTESIAN_POINT('Ctrl Pts',(-1.86506916841054,0.71092520135945,92.8240199321402));
#9645=CARTESIAN_POINT('Ctrl Pts',(-1.88879600493002,0.645249106260805,92.8281028737192));
#9646=CARTESIAN_POINT('Ctrl Pts',(-1.92366094116969,0.530189561905406,92.8352931399461));
#9647=CARTESIAN_POINT('Ctrl Pts',(-1.93645245705138,0.481376828343128,92.8383541327785));
#9648=CARTESIAN_POINT('Ctrl Pts',(-1.95319573152308,0.405924604148637,92.8431340104945));
#9649=CARTESIAN_POINT('Ctrl Pts',(-1.95848189088488,0.379601004188181,92.8448103274703));
#9650=CARTESIAN_POINT('Ctrl Pts',(-1.96737471167752,0.330168104992137,92.8479786594319));
#9651=CARTESIAN_POINT('Ctrl Pts',(-1.97110936606265,0.307086346196896,92.849466277822));
#9652=CARTESIAN_POINT('Ctrl Pts',(-1.97870700001022,0.25425551998164,92.8528923046844));
#9653=CARTESIAN_POINT('Ctrl Pts',(-1.98230626294191,0.224474893553132,92.8548387461944));
#9654=CARTESIAN_POINT('Ctrl Pts',(-1.99162693376925,0.129401653965325,92.8611047927957));
#9655=CARTESIAN_POINT('Ctrl Pts',(-1.9948024372975,0.0639086640660525,92.8655008761481));
#9656=CARTESIAN_POINT('Ctrl Pts',(-1.99465511719842,-0.117910358781764,
92.8779097976458));
#9657=CARTESIAN_POINT('Ctrl Pts',(-1.98439094668236,-0.233967639382531,
92.8860753729621));
#9658=CARTESIAN_POINT('Ctrl Pts',(-1.95114650175334,-0.421349275226169,
92.8993075156381));
#9659=CARTESIAN_POINT('Ctrl Pts',(-1.93416554738107,-0.49347093512938,92.904407391848));
#9660=CARTESIAN_POINT('Ctrl Pts',(-1.90735651027819,-0.584334586802061,
92.9107165915922));
#9661=CARTESIAN_POINT('Ctrl Pts',(-1.90119187458933,-0.604090477603018,
92.9120810164205));
#9662=CARTESIAN_POINT('Ctrl Pts',(-1.89050642106548,-0.636549028649673,
92.9143065213592));
#9663=CARTESIAN_POINT('Ctrl Pts',(-1.88616239214241,-0.64930783777143,92.9151770858983));
#9664=CARTESIAN_POINT('Ctrl Pts',(-1.87662478957617,-0.676416886776717,
92.9170165874034));
#9665=CARTESIAN_POINT('Ctrl Pts',(-1.87139533360319,-0.690753173554557,
92.9179834829762));
#9666=CARTESIAN_POINT('Ctrl Pts',(-1.85567909982095,-0.732349385696667,
92.920775534039));
#9667=CARTESIAN_POINT('Ctrl Pts',(-1.84475712448675,-0.759441834062847,
92.9225771968203));
#9668=CARTESIAN_POINT('Ctrl Pts',(-1.77954035833619,-0.911496147107613,
92.9326454919777));
#9669=CARTESIAN_POINT('Ctrl Pts',(-1.7131456271791,-1.03088743015271,92.9404025854022));
#9670=CARTESIAN_POINT('Ctrl Pts',(-1.57907898295936,-1.22274258367096,92.9540254115825));
#9671=CARTESIAN_POINT('Ctrl Pts',(-1.51725463547167,-1.298662873535,92.9597840613694));
#9672=CARTESIAN_POINT('Ctrl Pts',(-1.4278060820309,-1.39336035696389,92.9677486377447));
#9673=CARTESIAN_POINT('Ctrl Pts',(-1.40492200481048,-1.41643117198373,92.9697573357295));
#9674=CARTESIAN_POINT('Ctrl Pts',(-1.36440978718365,-1.45532602882664,92.9732724667747));
#9675=CARTESIAN_POINT('Ctrl Pts',(-1.34704405377998,-1.47141433876481,92.9747669439829));
#9676=CARTESIAN_POINT('Ctrl Pts',(-1.31030835442004,-1.50425233687816,92.9779058305046));
#9677=CARTESIAN_POINT('Ctrl Pts',(-1.29089402889713,-1.52094562068431,92.9795522255363));
#9678=CARTESIAN_POINT('Ctrl Pts',(-1.23765428873952,-1.56496970824304,92.9840368599456));
#9679=CARTESIAN_POINT('Ctrl Pts',(-1.20324931729963,-1.59157435313095,92.9869033836938));
#9680=CARTESIAN_POINT('Ctrl Pts',(-1.10404073383569,-1.66323408925702,92.9950861571707));
#9681=CARTESIAN_POINT('Ctrl Pts',(-1.03739809873881,-1.70559565083309,93.00049103467));
#9682=CARTESIAN_POINT('Ctrl Pts',(-0.843682912417196,-1.81317043202614,
93.0158621023904));
#9683=CARTESIAN_POINT('Ctrl Pts',(-0.711862417101707,-1.86886134718499,
93.0259635940504));
#9684=CARTESIAN_POINT('Ctrl Pts',(-0.552778315810356,-1.91677156248625,
93.0370843163391));
#9685=CARTESIAN_POINT('Ctrl Pts',(-0.53021353876527,-1.92313567073269,93.0386368570876));
#9686=CARTESIAN_POINT('Ctrl Pts',(-0.493888036648513,-1.93269280185331,
93.0410909391426));
#9687=CARTESIAN_POINT('Ctrl Pts',(-0.480197033226998,-1.93613989811209,
93.042005679616));
#9688=CARTESIAN_POINT('Ctrl Pts',(-0.45240942402555,-1.9428233091784,93.0438400739522));
#9689=CARTESIAN_POINT('Ctrl Pts',(-0.438312009033998,-1.94605223762001,
93.0447593108979));
#9690=CARTESIAN_POINT('Ctrl Pts',(-0.399612655355769,-1.95447421009414,
93.0472547239346));
#9691=CARTESIAN_POINT('Ctrl Pts',(-0.374944884625538,-1.95935606310019,
93.0488145089472));
#9692=CARTESIAN_POINT('Ctrl Pts',(-0.263505088602613,-1.97922860658991,
93.0557496110934));
#9693=CARTESIAN_POINT('Ctrl Pts',(-0.175882639845324,-1.98893166625432,
93.0609026963323));
#9694=CARTESIAN_POINT('Ctrl Pts',(0.0583901544985113,-1.99926488571686,
93.0745295959856));
#9695=CARTESIAN_POINT('Ctrl Pts',(0.204930305133938,-1.98959019038703,93.0829300454182));
#9696=CARTESIAN_POINT('Ctrl Pts',(0.383868432653864,-1.95778458687587,93.0939929498025));
#9697=CARTESIAN_POINT('Ctrl Pts',(0.418476757048317,-1.95067999160903,93.0961686434896));
#9698=CARTESIAN_POINT('Ctrl Pts',(0.47613270818206,-1.93723912907946,93.0998641340636));
#9699=CARTESIAN_POINT('Ctrl Pts',(0.499288670728882,-1.9314006685248,93.1013677328839));
#9700=CARTESIAN_POINT('Ctrl Pts',(0.546167865218077,-1.91868135019056,93.1044541587557));
#9701=CARTESIAN_POINT('Ctrl Pts',(0.569879179439027,-1.91177276114,93.1060376638746));
#9702=CARTESIAN_POINT('Ctrl Pts',(0.630276283468075,-1.89295187777978,93.1101314104183));
#9703=CARTESIAN_POINT('Ctrl Pts',(0.666754488391153,-1.88041301714173,93.1126617806849));
#9704=CARTESIAN_POINT('Ctrl Pts',(0.746929001184873,-1.85022797569027,93.1183560252242));
#9705=CARTESIAN_POINT('Ctrl Pts',(0.790408924064606,-1.83207523838219,93.1215344480049));
#9706=CARTESIAN_POINT('Ctrl Pts',(0.941881898457166,-1.76243960428723,93.1329189886566));
#9707=CARTESIAN_POINT('Ctrl Pts',(1.04584163009959,-1.70280546550533,93.1413272902403));
#9708=CARTESIAN_POINT('Ctrl Pts',(1.20108839945414,-1.59414551522322,93.154487457048));
#9709=CARTESIAN_POINT('Ctrl Pts',(1.25621242893426,-1.55107878721968,93.159293162197));
#9710=CARTESIAN_POINT('Ctrl Pts',(1.32444456969645,-1.49174224578306,93.1653129767044));
#9711=CARTESIAN_POINT('Ctrl Pts',(1.33971552051755,-1.47804287850864,93.1666650940437));
#9712=CARTESIAN_POINT('Ctrl Pts',(1.36464422671566,-1.45497579511731,93.1688764918592));
#9713=CARTESIAN_POINT('Ctrl Pts',(1.37442314417884,-1.44574184910487,93.1697450091712));
#9714=CARTESIAN_POINT('Ctrl Pts',(1.3951503083557,-1.42576937111761,93.1715870444625));
#9715=CARTESIAN_POINT('Ctrl Pts',(1.4060693497814,-1.41500236834655,93.1725583994572));
#9716=CARTESIAN_POINT('Ctrl Pts',(1.43769908609697,-1.3830853409288,93.1753790473706));
#9717=CARTESIAN_POINT('Ctrl Pts',(1.45806531681313,-1.36159812910831,93.1772041029978));
#9718=CARTESIAN_POINT('Ctrl Pts',(1.50562211867457,-1.30913242663865,93.1815106887642));
#9719=CARTESIAN_POINT('Ctrl Pts',(1.53234614423503,-1.2777485455341,93.1839680951894));
#9720=CARTESIAN_POINT('Ctrl Pts',(1.65186787372459,-1.12823766174791,93.1952561620992));
#9721=CARTESIAN_POINT('Ctrl Pts',(1.73210444863872,-1.00070173857716,93.2037554202385));
#9722=CARTESIAN_POINT('Ctrl Pts',(1.82127914161318,-0.815495775363631,93.2159951782602));
#9723=CARTESIAN_POINT('Ctrl Pts',(1.84320294362894,-0.764652333486747,93.219340771976));
#9724=CARTESIAN_POINT('Ctrl Pts',(1.87287077963935,-0.687130167819476,93.2244639515179));
#9725=CARTESIAN_POINT('Ctrl Pts',(1.88221933293004,-0.661092344034207,93.2261881381217));
#9726=CARTESIAN_POINT('Ctrl Pts',(1.89837164012252,-0.612981063845531,93.2293848103148));
#9727=CARTESIAN_POINT('Ctrl Pts',(1.90533935371217,-0.590967462871391,93.230851530997));
#9728=CARTESIAN_POINT('Ctrl Pts',(1.92012849492411,-0.541259688248745,93.2341748520179));
#9729=CARTESIAN_POINT('Ctrl Pts',(1.92773575762002,-0.513507732691427,93.2360381351656));
#9730=CARTESIAN_POINT('Ctrl Pts',(1.94999968326752,-0.424803623022148,93.2420223367544));
#9731=CARTESIAN_POINT('Ctrl Pts',(1.96238375849129,-0.363325595392939,93.2462135762827));
#9732=CARTESIAN_POINT('Ctrl Pts',(1.98711090575525,-0.201537723390736,93.2573481716866));
#9733=CARTESIAN_POINT('Ctrl Pts',(1.99476427900868,-0.100696007704139,93.2643982695156));
#9734=CARTESIAN_POINT('Ctrl Pts',(1.99473755778325,0.0880071858877521,93.2775631558897));
#9735=CARTESIAN_POINT('Ctrl Pts',(1.98893822119425,0.175642896268484,93.2836625484435));
#9736=CARTESIAN_POINT('Ctrl Pts',(1.97412291727871,0.287194964745106,93.291211463674));
#9737=CARTESIAN_POINT('Ctrl Pts',(1.97040074623101,0.311710240298752,93.2928566253757));
#9738=CARTESIAN_POINT('Ctrl Pts',(1.96379719620553,0.350335875008289,93.2954202251518));
#9739=CARTESIAN_POINT('Ctrl Pts',(1.96121859472815,0.364494592427848,93.2963538532427));
#9740=CARTESIAN_POINT('Ctrl Pts',(1.95579550137601,0.392546269099557,93.2981897951889));
#9741=CARTESIAN_POINT('Ctrl Pts',(1.95295566424722,0.406439189911222,93.2990922670959));
#9742=CARTESIAN_POINT('Ctrl Pts',(1.94496335750908,0.443519135267231,93.3014855898408));
#9743=CARTESIAN_POINT('Ctrl Pts',(1.93954433362855,0.466647168918481,93.302962250298));
#9744=CARTESIAN_POINT('Ctrl Pts',(1.92627135661989,0.519061893116134,93.3062833751774));
#9745=CARTESIAN_POINT('Ctrl Pts',(1.91816013344389,0.548277733178115,93.3081163180706));
#9746=CARTESIAN_POINT('Ctrl Pts',(1.88770524171498,0.649005716514939,93.314407754467));
#9747=CARTESIAN_POINT('Ctrl Pts',(1.86200128263339,0.719438665912472,93.3187589550081));
#9748=CARTESIAN_POINT('Ctrl Pts',(1.78179817005032,0.905878896388542,93.3305297870666));
#9749=CARTESIAN_POINT('Ctrl Pts',(1.72000033107232,1.01834003963853,93.3379279308839));
#9750=CARTESIAN_POINT('Ctrl Pts',(1.62696477649855,1.15472396604202,93.3479524974945));
#9751=CARTESIAN_POINT('Ctrl Pts',(1.60522567776207,1.18475823499143,93.3502309239898));
#9752=CARTESIAN_POINT('Ctrl Pts',(1.56779625578206,1.23354734594667,93.3540638853263));
#9753=CARTESIAN_POINT('Ctrl Pts',(1.55257493746703,1.2526512414243,93.3555998956789));
#9754=CARTESIAN_POINT('Ctrl Pts',(1.52145663340575,1.29026837036096,93.3586986964883));
#9755=CARTESIAN_POINT('Ctrl Pts',(1.50556311268616,1.30877896559753,93.3602611868543));
#9756=CARTESIAN_POINT('Ctrl Pts',(1.46478020192573,1.35455118446636,93.3642234014067));
#9757=CARTESIAN_POINT('Ctrl Pts',(1.43946702593971,1.38142112748593,93.366640725911));
#9758=CARTESIAN_POINT('Ctrl Pts',(1.33964565784226,1.48165753098581,93.3760227910914));
#9759=CARTESIAN_POINT('Ctrl Pts',(1.260166109322,1.54981792109557,93.3831981195032));
#9760=CARTESIAN_POINT('Ctrl Pts',(1.06896078215935,1.68932416319989,93.399667610501));
#9761=CARTESIAN_POINT('Ctrl Pts',(0.954716970738655,1.7564204682159,93.4089878084472));
#9762=CARTESIAN_POINT('Ctrl Pts',(0.814555674194009,1.82099344276447,93.4192938217076));
#9763=CARTESIAN_POINT('Ctrl Pts',(0.794286479735627,1.82992544989915,93.4207577010488));
#9764=CARTESIAN_POINT('Ctrl Pts',(0.762349176348671,1.84336854386684,93.4230184418628));
#9765=CARTESIAN_POINT('Ctrl Pts',(0.750780871540235,1.84811037550477,93.4238280564819));
#9766=CARTESIAN_POINT('Ctrl Pts',(0.725867578271714,1.85804975453646,93.4255506309008));
#9767=CARTESIAN_POINT('Ctrl Pts',(0.712509558042411,1.86321302904902,93.4264614650853));
#9768=CARTESIAN_POINT('Ctrl Pts',(0.676200921556376,1.87679980078664,93.4289057746728));
#9769=CARTESIAN_POINT('Ctrl Pts',(0.653148461228603,1.88494625719749,93.4304239720942));
#9770=CARTESIAN_POINT('Ctrl Pts',(0.552247099320134,1.91853002619811,93.4369474337038));
#9771=CARTESIAN_POINT('Ctrl Pts',(0.473016428015961,1.9395856219531,93.4417596454754));
#9772=CARTESIAN_POINT('Ctrl Pts',(0.238685200471375,1.98663956043353,93.4556722611848));
#9773=CARTESIAN_POINT('Ctrl Pts',(0.0815621009566453,1.99926265710679,93.4646488341483));
#9774=CARTESIAN_POINT('Ctrl Pts',(-0.109266383595662,1.99204322542493,93.4762986420151));
#9775=CARTESIAN_POINT('Ctrl Pts',(-0.143081436923691,1.9899002101402,93.4783891117578));
#9776=CARTESIAN_POINT('Ctrl Pts',(-0.200375541292755,1.98480131772284,93.4819843642072));
#9777=CARTESIAN_POINT('Ctrl Pts',(-0.223887039877736,1.98228684702796,93.4834750179601));
#9778=CARTESIAN_POINT('Ctrl Pts',(-0.272225280677243,1.97624632266604,93.4865739106634));
#9779=CARTESIAN_POINT('Ctrl Pts',(-0.297041241904327,1.97266888666929,93.4881835342224));
#9780=CARTESIAN_POINT('Ctrl Pts',(-0.361855275781671,1.96207468546193,93.4924393277618));
#9781=CARTESIAN_POINT('Ctrl Pts',(-0.401716301027536,1.95430292631391,93.4951088854404));
#9782=CARTESIAN_POINT('Ctrl Pts',(-0.549132303021071,1.92086053543104,93.5051820519882));
#9783=CARTESIAN_POINT('Ctrl Pts',(-0.654720647077651,1.88748152761864,93.5128132189124));
#9784=CARTESIAN_POINT('Ctrl Pts',(-0.863927386426982,1.80167066632472,93.5285798127436));
#9785=CARTESIAN_POINT('Ctrl Pts',(-0.966859360471028,1.74859211228761,93.5366918853279));
#9786=CARTESIAN_POINT('Ctrl Pts',(-1.08477530747532,1.6741738636361,93.5460311202479));
#9787=CARTESIAN_POINT('Ctrl Pts',(-1.10470192726965,1.66109282284214,93.5476104878353));
#9788=CARTESIAN_POINT('Ctrl Pts',(-1.13611597003732,1.63965532483181,93.5500962643702));
#9789=CARTESIAN_POINT('Ctrl Pts',(-1.14775635218576,1.63152826256372,93.5510164402055));
#9790=CARTESIAN_POINT('Ctrl Pts',(-1.17100542302791,1.61492427992367,93.5528507947463));
#9791=CARTESIAN_POINT('Ctrl Pts',(-1.1826111999242,1.60644480488654,93.5537647347169));
#9792=CARTESIAN_POINT('Ctrl Pts',(-1.21391256493022,1.58305214544875,93.5562279100334));
#9793=CARTESIAN_POINT('Ctrl Pts',(-1.23342503802517,1.56789687672873,93.5577614601002));
#9794=CARTESIAN_POINT('Ctrl Pts',(-1.3181141946708,1.49955930223707,93.5644338091069));
#9795=CARTESIAN_POINT('Ctrl Pts',(-1.38017637517835,1.4426430857935,93.5693692382941));
#9796=CARTESIAN_POINT('Ctrl Pts',(-1.52332772341475,1.29364010344176,93.5813887261374));
#9797=CARTESIAN_POINT('Ctrl Pts',(-1.59982355324681,1.19773213210311,93.5884097664221));
#9798=CARTESIAN_POINT('Ctrl Pts',(-1.66701733785596,1.09548197510851,93.5957235785224));
#9799=CARTESIAN_POINT('Origin',(0.,0.,89.2710285354474));
#9800=CARTESIAN_POINT('',(-1.66701720848889,1.09548217196899,94.5531952825684));
#9801=CARTESIAN_POINT('',(-1.66701746607046,1.09548178000185,94.3957559446131));
#9802=CARTESIAN_POINT('',(-1.66701720851066,1.09548217193587,89.2710285354474));
#9803=CARTESIAN_POINT('',(-1.99474905761762,0.00184918920886758,93.8294109563595));
#9804=CARTESIAN_POINT('Ctrl Pts',(-1.66701720848889,1.09548217196899,94.5531952825684));
#9805=CARTESIAN_POINT('Ctrl Pts',(-1.65877814536531,1.10801971969024,94.5522588550472));
#9806=CARTESIAN_POINT('Ctrl Pts',(-1.65039747779998,1.12046456721701,94.5513305262315));
#9807=CARTESIAN_POINT('Ctrl Pts',(-1.62450307492538,1.15799535947798,94.5485306443866));
#9808=CARTESIAN_POINT('Ctrl Pts',(-1.60655150988994,1.18277467219681,94.5466816763493));
#9809=CARTESIAN_POINT('Ctrl Pts',(-1.54192739585364,1.26779055836618,94.5402998219996));
#9810=CARTESIAN_POINT('Ctrl Pts',(-1.49237836509429,1.32576058053032,94.5358774212361));
#9811=CARTESIAN_POINT('Ctrl Pts',(-1.35242075810157,1.47168597577157,94.5241523801242));
#9812=CARTESIAN_POINT('Ctrl Pts',(-1.25679984611073,1.55414027442987,94.5168661992516));
#9813=CARTESIAN_POINT('Ctrl Pts',(-1.12373179260989,1.64852531373329,94.5069613783697));
#9814=CARTESIAN_POINT('Ctrl Pts',(-1.09282411206984,1.6691746583652,94.5046773719786));
#9815=CARTESIAN_POINT('Ctrl Pts',(-1.04065981086558,1.70195545906256,94.5008374096396));
#9816=CARTESIAN_POINT('Ctrl Pts',(-1.01972388302515,1.71458109855253,94.4993001165723));
#9817=CARTESIAN_POINT('Ctrl Pts',(-0.977448590663658,1.73902750166448,94.4962005553139));
#9818=CARTESIAN_POINT('Ctrl Pts',(-0.956113931721415,1.75084792622617,94.4946386213168));
#9819=CARTESIAN_POINT('Ctrl Pts',(-0.902020836293087,1.77953456532363,94.4906815735246));
#9820=CARTESIAN_POINT('Ctrl Pts',(-0.869002998235498,1.79588929166821,94.4882689682843));
#9821=CARTESIAN_POINT('Ctrl Pts',(-0.741125540299473,1.85487854702981,94.4789299417245));
#9822=CARTESIAN_POINT('Ctrl Pts',(-0.643448962027013,1.89098114233389,94.4717953999255));
#9823=CARTESIAN_POINT('Ctrl Pts',(-0.415370962582188,1.95555733245835,94.4553035478323));
#9824=CARTESIAN_POINT('Ctrl Pts',(-0.284012913178147,1.97890835156229,94.4459159151652));
#9825=CARTESIAN_POINT('Ctrl Pts',(-0.129319918189096,1.99067574956653,94.4355571500884));
#9826=CARTESIAN_POINT('Ctrl Pts',(-0.107310257357126,1.99198348078666,94.434100220218));
#9827=CARTESIAN_POINT('Ctrl Pts',(-0.0728068789317379,1.99345996790867,
94.431847340437));
#9828=CARTESIAN_POINT('Ctrl Pts',(-0.0603261957933327,1.99387669081826,
94.4310387813376));
#9829=CARTESIAN_POINT('Ctrl Pts',(-0.0334924276918565,1.9945204555676,94.4293152109124));
#9830=CARTESIAN_POINT('Ctrl Pts',(-0.0191390545645032,1.9947098329248,94.4284023736306));
#9831=CARTESIAN_POINT('Ctrl Pts',(0.0198136761772904,1.99480326035947,94.4259467423169));
#9832=CARTESIAN_POINT('Ctrl Pts',(0.0444120141936166,1.9944072630241,94.4244194641022));
#9833=CARTESIAN_POINT('Ctrl Pts',(0.152124506610376,1.99067927822345,94.4178099068501));
#9834=CARTESIAN_POINT('Ctrl Pts',(0.234998195084644,1.9826054578836,94.4129265939112));
#9835=CARTESIAN_POINT('Ctrl Pts',(0.46996000404195,1.94476914667243,94.399078874414));
#9836=CARTESIAN_POINT('Ctrl Pts',(0.619389079980499,1.9024570274418,94.3902262158612));
#9837=CARTESIAN_POINT('Ctrl Pts',(0.794031674106413,1.83022169896995,94.3787026051903));
#9838=CARTESIAN_POINT('Ctrl Pts',(0.825299480243103,1.81633651024285,94.3765927251096));
#9839=CARTESIAN_POINT('Ctrl Pts',(0.877600802071935,1.79148155605093,94.3729744300148));
#9840=CARTESIAN_POINT('Ctrl Pts',(0.898824337046323,1.78092786665713,94.3714806032605));
#9841=CARTESIAN_POINT('Ctrl Pts',(0.942026555636191,1.75847602375361,94.3683841977219));
#9842=CARTESIAN_POINT('Ctrl Pts',(0.96397967403659,1.74653801882003,94.3667803973395));
#9843=CARTESIAN_POINT('Ctrl Pts',(1.0205878962206,1.71436230817635,94.3625622762207));
#9844=CARTESIAN_POINT('Ctrl Pts',(1.05486530273371,1.69348651795838,94.3599253520937));
#9845=CARTESIAN_POINT('Ctrl Pts',(1.19618300106117,1.60146492012662,94.3486942095417));
#9846=CARTESIAN_POINT('Ctrl Pts',(1.29683478037455,1.52110303558176,94.3397730302349));
#9847=CARTESIAN_POINT('Ctrl Pts',(1.45783728687042,1.36489017899323,94.3241170658233));
#9848=CARTESIAN_POINT('Ctrl Pts',(1.52173401535396,1.29326839804365,94.3174307016422));
#9849=CARTESIAN_POINT('Ctrl Pts',(1.59569138049773,1.19726267587847,94.309294325021));
#9850=CARTESIAN_POINT('Ctrl Pts',(1.61076349197795,1.17690696828544,94.3076126603283));
#9851=CARTESIAN_POINT('Ctrl Pts',(1.63385013665638,1.14445251828961,94.3050057927724));
#9852=CARTESIAN_POINT('Ctrl Pts',(1.64212683511803,1.13254462373975,94.3040645895399));
#9853=CARTESIAN_POINT('Ctrl Pts',(1.65818987186635,1.10888796523642,94.3022263715666));
#9854=CARTESIAN_POINT('Ctrl Pts',(1.66598291995116,1.09714497764926,94.3013289986563));
#9855=CARTESIAN_POINT('Ctrl Pts',(1.68633087466789,1.06576679047973,94.2989681730435));
#9856=CARTESIAN_POINT('Ctrl Pts',(1.69866769458293,1.04599179972339,94.2975182207548));
#9857=CARTESIAN_POINT('Ctrl Pts',(1.72584954932471,1.0006715194403,94.2942693609485));
#9858=CARTESIAN_POINT('Ctrl Pts',(1.740479529708,0.975003248315662,94.292481236487));
#9859=CARTESIAN_POINT('Ctrl Pts',(1.78850253994539,0.886218830395893,94.2864389506135));
#9860=CARTESIAN_POINT('Ctrl Pts',(1.81907630182492,0.821637224234635,94.2822834492804));
#9861=CARTESIAN_POINT('Ctrl Pts',(1.89688761394112,0.631512362308087,94.2703635230671));
#9862=CARTESIAN_POINT('Ctrl Pts',(1.93501811058044,0.502684357809222,94.2626381646091));
#9863=CARTESIAN_POINT('Ctrl Pts',(1.96676344618634,0.334983058620699,94.2522686357913));
#9864=CARTESIAN_POINT('Ctrl Pts',(1.97258839314024,0.298775621890827,94.2500139112907));
#9865=CARTESIAN_POINT('Ctrl Pts',(1.98061657781982,0.238283168243984,94.2462089969451));
#9866=CARTESIAN_POINT('Ctrl Pts',(1.98337850050852,0.214080675691126,94.2446767185164));
#9867=CARTESIAN_POINT('Ctrl Pts',(1.98802608555792,0.165466263185176,94.2415760371739));
#9868=CARTESIAN_POINT('Ctrl Pts',(1.98990685970579,0.141058151383069,94.2400077613994));
#9869=CARTESIAN_POINT('Ctrl Pts',(1.99352130748105,0.0793411754075412,94.236010774918));
#9870=CARTESIAN_POINT('Ctrl Pts',(1.99465717066892,0.0420081592897301,94.2335638165659));
#9871=CARTESIAN_POINT('Ctrl Pts',(1.99499708561107,-0.103268839732908,94.2239230815013));
#9872=CARTESIAN_POINT('Ctrl Pts',(1.98648864865558,-0.211032967510561,94.2165037350097));
#9873=CARTESIAN_POINT('Ctrl Pts',(1.94914056120583,-0.44263787315862,94.2001670206954));
#9874=CARTESIAN_POINT('Ctrl Pts',(1.91710175250023,-0.565510451063959,94.1912467239069));
#9875=CARTESIAN_POINT('Ctrl Pts',(1.86581140866124,-0.705899029901706,94.1812540631847));
#9876=CARTESIAN_POINT('Ctrl Pts',(1.85763475115789,-0.727144339953264,94.1797481352418));
#9877=CARTESIAN_POINT('Ctrl Pts',(1.84436548688519,-0.759935879159465,94.1774386268102));
#9878=CARTESIAN_POINT('Ctrl Pts',(1.83952425092934,-0.771580936092235,94.1766214206556));
#9879=CARTESIAN_POINT('Ctrl Pts',(1.82900684205424,-0.79621762195198,94.1749000183802));
#9880=CARTESIAN_POINT('Ctrl Pts',(1.82330194091378,-0.809196259719386,94.1739977111454));
#9881=CARTESIAN_POINT('Ctrl Pts',(1.80768173545641,-0.8437280939436,94.1716062715789));
#9882=CARTESIAN_POINT('Ctrl Pts',(1.79751916363818,-0.8651678023182,94.1701312835946));
#9883=CARTESIAN_POINT('Ctrl Pts',(1.77352717224698,-0.913534272911786,94.1668148256097));
#9884=CARTESIAN_POINT('Ctrl Pts',(1.75946238013835,-0.940338137389606,94.1649848262875));
#9885=CARTESIAN_POINT('Ctrl Pts',(1.70860206065416,-1.0321249826431,94.1587105323954));
#9886=CARTESIAN_POINT('Ctrl Pts',(1.66877093169261,-1.0953573949966,94.1543729171989));
#9887=CARTESIAN_POINT('Ctrl Pts',(1.55104574932368,-1.26086414296275,94.1425933259141));
#9888=CARTESIAN_POINT('Ctrl Pts',(1.46668027507267,-1.35807457368512,94.1351738647117));
#9889=CARTESIAN_POINT('Ctrl Pts',(1.34669021923759,-1.47201430151598,94.1251263210794));
#9890=CARTESIAN_POINT('Ctrl Pts',(1.31911521311274,-1.49677501165304,94.1228488146139));
#9891=CARTESIAN_POINT('Ctrl Pts',(1.27224504856193,-1.53656005292961,94.1190166395278));
#9892=CARTESIAN_POINT('Ctrl Pts',(1.25333406638924,-1.55202380542538,94.1174804661503));
#9893=CARTESIAN_POINT('Ctrl Pts',(1.21496836525932,-1.58223740835474,94.1143807034539));
#9894=CARTESIAN_POINT('Ctrl Pts',(1.19551736795742,-1.59698512201632,94.1128174029695));
#9895=CARTESIAN_POINT('Ctrl Pts',(1.14595262606596,-1.63315200455973,94.1088517277386));
#9896=CARTESIAN_POINT('Ctrl Pts',(1.11550626593893,-1.65409744568524,94.1064316989168));
#9897=CARTESIAN_POINT('Ctrl Pts',(0.996514443340254,-1.73117756850181,94.0970283746854));
#9898=CARTESIAN_POINT('Ctrl Pts',(0.904187332282916,-1.78113916536057,94.0898333081222));
#9899=CARTESIAN_POINT('Ctrl Pts',(0.687968751104798,-1.87698507490708,94.073375125702));
#9900=CARTESIAN_POINT('Ctrl Pts',(0.562566625708487,-1.91830571956047,94.0640880254416));
#9901=CARTESIAN_POINT('Ctrl Pts',(0.412331946076651,-1.95179476441778,94.0538076723575));
#9902=CARTESIAN_POINT('Ctrl Pts',(0.390582774671034,-1.95626318067689,94.0523401398014));
#9903=CARTESIAN_POINT('Ctrl Pts',(0.356464878494291,-1.9626810578659,94.050075027217));
#9904=CARTESIAN_POINT('Ctrl Pts',(0.344145366749343,-1.96487865595286,94.0492646208273));
#9905=CARTESIAN_POINT('Ctrl Pts',(0.317692205954323,-1.96934102683323,94.0475417005943));
#9906=CARTESIAN_POINT('Ctrl Pts',(0.30355310205298,-1.97156992325673,94.0466312944225));
#9907=CARTESIAN_POINT('Ctrl Pts',(0.265251805654981,-1.97718594380987,94.0441904253263));
#9908=CARTESIAN_POINT('Ctrl Pts',(0.241048713215539,-1.98028240924477,94.0426751605065));
#9909=CARTESIAN_POINT('Ctrl Pts',(0.135824066286911,-1.99178659100132,94.0361812612194));
#9910=CARTESIAN_POINT('Ctrl Pts',(0.0543800288674653,-1.9956721643413,94.0313936434756));
#9911=CARTESIAN_POINT('Ctrl Pts',(-0.184960421726489,-1.99242262696403,
94.0174584547268));
#9912=CARTESIAN_POINT('Ctrl Pts',(-0.342012742189479,-1.97154299114936,
94.0084390653217));
#9913=CARTESIAN_POINT('Ctrl Pts',(-0.527671360217766,-1.92398827556405,
93.9967452621222));
#9914=CARTESIAN_POINT('Ctrl Pts',(-0.560165202110039,-1.91478006216783,
93.9946612325277));
#9915=CARTESIAN_POINT('Ctrl Pts',(-0.614974763371199,-1.89773341383098,
93.9910731646538));
#9916=CARTESIAN_POINT('Ctrl Pts',(-0.63741392819908,-1.89031464998026,93.9895830961079));
#9917=CARTESIAN_POINT('Ctrl Pts',(-0.683416273752857,-1.87419328963735,
93.9864819012364));
#9918=CARTESIAN_POINT('Ctrl Pts',(-0.706957379123901,-1.86544082143876,
93.9848693262261));
#9919=CARTESIAN_POINT('Ctrl Pts',(-0.768303628899785,-1.84130460565617,
93.9805968106557));
#9920=CARTESIAN_POINT('Ctrl Pts',(-0.805811151358889,-1.82520166058388,
93.9779131484791));
#9921=CARTESIAN_POINT('Ctrl Pts',(-0.889028745586847,-1.78640906990593,
93.9717932221061));
#9922=CARTESIAN_POINT('Ctrl Pts',(-0.934414251957977,-1.76309353312745,
93.9683385408809));
#9923=CARTESIAN_POINT('Ctrl Pts',(-1.10837674595844,-1.66512036997281,93.9546522514962));
#9924=CARTESIAN_POINT('Ctrl Pts',(-1.22933022848395,-1.57793164990642,93.9441092151829));
#9925=CARTESIAN_POINT('Ctrl Pts',(-1.36862307789195,-1.45170451731197,93.9312687216011));
#9926=CARTESIAN_POINT('Ctrl Pts',(-1.39698799277902,-1.42442975580955,93.9286144656591));
#9927=CARTESIAN_POINT('Ctrl Pts',(-1.43672904898935,-1.38388616941381,93.9248600329928));
#9928=CARTESIAN_POINT('Ctrl Pts',(-1.44876545415989,-1.37128042375902,93.9237179558235));
#9929=CARTESIAN_POINT('Ctrl Pts',(-1.46968834420685,-1.34878479429032,93.9217264015465));
#9930=CARTESIAN_POINT('Ctrl Pts',(-1.47864345874466,-1.338961463559,93.9208720849971));
#9931=CARTESIAN_POINT('Ctrl Pts',(-1.49891346599327,-1.31627482064861,93.9189338255884));
#9932=CARTESIAN_POINT('Ctrl Pts',(-1.51016185228887,-1.30335421531302,93.9178545837748));
#9933=CARTESIAN_POINT('Ctrl Pts',(-1.54730230578337,-1.25956587370218,93.9142723223722));
#9934=CARTESIAN_POINT('Ctrl Pts',(-1.57242694269054,-1.2280572468943,93.9118175118612));
#9935=CARTESIAN_POINT('Ctrl Pts',(-1.63609156501138,-1.14305542888454,93.9054468966782));
#9936=CARTESIAN_POINT('Ctrl Pts',(-1.67296514493075,-1.08837491582328,93.9015976883592));
#9937=CARTESIAN_POINT('Ctrl Pts',(-1.78201946006359,-0.907978650159301,
93.8893512695102));
#9938=CARTESIAN_POINT('Ctrl Pts',(-1.84323582364829,-0.776206364462101,
93.8810340427052));
#9939=CARTESIAN_POINT('Ctrl Pts',(-1.90099129240392,-0.605404954737159,
93.8700605206674));
#9940=CARTESIAN_POINT('Ctrl Pts',(-1.91144443599477,-0.57154438392123,93.8678784987383));
#9941=CARTESIAN_POINT('Ctrl Pts',(-1.92742971719943,-0.514406053835909,
93.864175195573));
#9942=CARTESIAN_POINT('Ctrl Pts',(-1.93345507876547,-0.491274140584253,
93.8626702634296));
#9943=CARTESIAN_POINT('Ctrl Pts',(-1.94485432327511,-0.444047751229549,
93.8595835123776));
#9944=CARTESIAN_POINT('Ctrl Pts',(-1.95019949184321,-0.419950705610756,
93.858001058756));
#9945=CARTESIAN_POINT('Ctrl Pts',(-1.96008624682162,-0.371109289120179,
93.8547766195633));
#9946=CARTESIAN_POINT('Ctrl Pts',(-1.96460958394189,-0.346365827303723,
93.8531343674238));
#9947=CARTESIAN_POINT('Ctrl Pts',(-1.97499847301754,-0.282759583788984,
93.8488891054048));
#9948=CARTESIAN_POINT('Ctrl Pts',(-1.9801853328603,-0.243798393516646,93.84626611072));
#9949=CARTESIAN_POINT('Ctrl Pts',(-1.99129863967524,-0.136079862540772,
93.838953796603));
#9950=CARTESIAN_POINT('Ctrl Pts',(-1.99481311978167,-0.067133567392285,
93.8342045185029));
#9951=CARTESIAN_POINT('Ctrl Pts',(-1.99474914212584,0.00184999681506738,
93.8294110481131));
#9952=CARTESIAN_POINT('Ctrl Pts',(-1.99474914286513,0.00184919951270623,
93.8294111035154));
#9953=CARTESIAN_POINT('Ctrl Pts',(-1.99462397475624,0.136869231801161,93.8200289485989));
#9954=CARTESIAN_POINT('Ctrl Pts',(-1.98079066454154,0.271536840527291,93.8104912318438));
#9955=CARTESIAN_POINT('Ctrl Pts',(-1.94859746654462,0.427283678473688,93.7998361128864));
#9956=CARTESIAN_POINT('Ctrl Pts',(-1.94331593803251,0.450695813799839,93.7982455201724));
#9957=CARTESIAN_POINT('Ctrl Pts',(-1.93423114022538,0.48783193030372,93.795746305063));
#9958=CARTESIAN_POINT('Ctrl Pts',(-1.93070137826948,0.501619693313766,93.7948236788762));
#9959=CARTESIAN_POINT('Ctrl Pts',(-1.9237767885384,0.527511531704006,93.7931025842245));
#9960=CARTESIAN_POINT('Ctrl Pts',(-1.92041456497507,0.539623449765512,93.7923022311904));
#9961=CARTESIAN_POINT('Ctrl Pts',(-1.91070800480892,0.573349690034312,93.7900848293567));
#9962=CARTESIAN_POINT('Ctrl Pts',(-1.90411151867594,0.594890218949912,93.7886815402064));
#9963=CARTESIAN_POINT('Ctrl Pts',(-1.85735859713285,0.738805748324284,93.7793644012841));
#9964=CARTESIAN_POINT('Ctrl Pts',(-1.80579145843149,0.857169984270223,93.7719734846332));
#9965=CARTESIAN_POINT('Ctrl Pts',(-1.71932457295764,1.01259823602324,93.7616551244413));
#9966=CARTESIAN_POINT('Ctrl Pts',(-1.69392384772003,1.0545378050329,93.7588051545207));
#9967=CARTESIAN_POINT('Ctrl Pts',(-1.66701713450993,1.09548228454426,93.7559248887299));
#9968=CARTESIAN_POINT('',(-1.99475046548998,-0.00047329462618507,93.6728333695482));
#9969=CARTESIAN_POINT('Ctrl Pts',(-1.66701733785596,1.09548197510851,93.5957235785224));
#9970=CARTESIAN_POINT('Ctrl Pts',(-1.68382990952458,1.06989794077261,93.5975535690613));
#9971=CARTESIAN_POINT('Ctrl Pts',(-1.70006015033342,1.04391678375076,93.5994006921208));
#9972=CARTESIAN_POINT('Ctrl Pts',(-1.73325899504351,0.987940554734956,93.6033675317161));
#9973=CARTESIAN_POINT('Ctrl Pts',(-1.75005382536845,0.957875081423901,93.6054907201682));
#9974=CARTESIAN_POINT('Ctrl Pts',(-1.77709515091515,0.906379408478577,93.6091243008571));
#9975=CARTESIAN_POINT('Ctrl Pts',(-1.78775263093988,0.885173011029849,93.6106197782722));
#9976=CARTESIAN_POINT('Ctrl Pts',(-1.80881826746923,0.841323275402433,93.6137130011928));
#9977=CARTESIAN_POINT('Ctrl Pts',(-1.81918549136577,0.818665030883475,93.6153118489053));
#9978=CARTESIAN_POINT('Ctrl Pts',(-1.84498983427763,0.759355876062686,93.6195008497259));
#9979=CARTESIAN_POINT('Ctrl Pts',(-1.85975953843096,0.722428487904385,93.6221130272067));
#9980=CARTESIAN_POINT('Ctrl Pts',(-1.91791393370979,0.563401383673303,93.6333850330902));
#9981=CARTESIAN_POINT('Ctrl Pts',(-1.950445242861,0.437686318157782,93.6423796064582));
#9982=CARTESIAN_POINT('Ctrl Pts',(-1.98232649146809,0.234849380821766,93.656709282206));
#9983=CARTESIAN_POINT('Ctrl Pts',(-1.98981866226028,0.159359265007278,93.6619961768541));
#9984=CARTESIAN_POINT('Ctrl Pts',(-1.99417188367383,0.0556081062775789,
93.6690725907853));
#9985=CARTESIAN_POINT('Ctrl Pts',(-1.99475656749687,0.0275705606384254,
93.6709656878819));
#9986=CARTESIAN_POINT('Ctrl Pts',(-1.99474994436128,-0.000471137632967747,
93.6728341296312));
#9987=CARTESIAN_POINT('Ctrl Pts',(-1.99474994386491,-0.000473234538596436,
93.6728342693498));
#9988=CARTESIAN_POINT('Ctrl Pts',(-1.99474660187362,-0.0145601965145745,
93.6737728947528));
#9989=CARTESIAN_POINT('Ctrl Pts',(-1.99459403618466,-0.0286472457323476,
93.6747052266267));
#9990=CARTESIAN_POINT('Ctrl Pts',(-1.99399045765822,-0.0568161117758029,
93.6765554132599));
#9991=CARTESIAN_POINT('Ctrl Pts',(-1.99353947529967,-0.0708971409524056,
93.6774732166138));
#9992=CARTESIAN_POINT('Ctrl Pts',(-1.99237775670518,-0.0981439454589759,
93.6792339620626));
#9993=CARTESIAN_POINT('Ctrl Pts',(-1.99168566144922,-0.111308559768748,
93.6800775829642));
#9994=CARTESIAN_POINT('Ctrl Pts',(-1.98965922496718,-0.143721770119643,
93.6821385238247));
#9995=CARTESIAN_POINT('Ctrl Pts',(-1.9881760626398,-0.162959472154204,93.6833478528335));
#9996=CARTESIAN_POINT('Ctrl Pts',(-1.98139508284564,-0.236899064765848,
93.6879528673883));
#9997=CARTESIAN_POINT('Ctrl Pts',(-1.97411636760926,-0.291398798271338,
93.6912566358625));
#9998=CARTESIAN_POINT('Ctrl Pts',(-1.95472287231988,-0.401664396129385,
93.6978798064567));
#9999=CARTESIAN_POINT('Ctrl Pts',(-1.94244894939685,-0.457349248172171,
93.7011923668612));
#10000=CARTESIAN_POINT('Ctrl Pts',(-1.90711040483513,-0.590294996565072,
93.7091719511386));
#10001=CARTESIAN_POINT('Ctrl Pts',(-1.88171632705291,-0.666829332174217,
93.713827281217));
#10002=CARTESIAN_POINT('Ctrl Pts',(-1.8265594919523,-0.804552214992443,
93.7225803402644));
#10003=CARTESIAN_POINT('Ctrl Pts',(-1.79816414114437,-0.866157173060337,
93.7266430927624));
#10004=CARTESIAN_POINT('Ctrl Pts',(-1.75300775377003,-0.952291820612311,
93.7326222817654));
#10005=CARTESIAN_POINT('Ctrl Pts',(-1.73874950995876,-0.978082764812323,
93.7344526506466));
#10006=CARTESIAN_POINT('Ctrl Pts',(-1.71218258699017,-1.02372027363406,
93.737769787191));
#10007=CARTESIAN_POINT('Ctrl Pts',(-1.7000866277015,-1.04368471887101,93.7392486309641));
#10008=CARTESIAN_POINT('Ctrl Pts',(-1.67313813526597,-1.08645140661088,
93.7424796561735));
#10009=CARTESIAN_POINT('Ctrl Pts',(-1.65816390074364,-1.1091709672942,93.7442361861689));
#10010=CARTESIAN_POINT('Ctrl Pts',(-1.61384334494729,-1.17351194140583,
93.7493303283768));
#10011=CARTESIAN_POINT('Ctrl Pts',(-1.58336357099285,-1.21432271588118,
93.7527101165153));
#10012=CARTESIAN_POINT('Ctrl Pts',(-1.45369037090604,-1.37475525703491,
93.7666160268956));
#10013=CARTESIAN_POINT('Ctrl Pts',(-1.34224499953218,-1.48375711668785,
93.7775856899134));
#10014=CARTESIAN_POINT('Ctrl Pts',(-1.18633764710202,-1.60417142408417,
93.7912155777713));
#10015=CARTESIAN_POINT('Ctrl Pts',(-1.15257655720715,-1.62859774914347,
93.7940748744114));
#10016=CARTESIAN_POINT('Ctrl Pts',(-1.09337412027603,-1.66866716884381,
93.7989043867696));
#10017=CARTESIAN_POINT('Ctrl Pts',(-1.06830127082955,-1.68482927983789,
93.8008957614767));
#10018=CARTESIAN_POINT('Ctrl Pts',(-1.02976676801425,-1.70846257858821,
93.8038649023371));
#10019=CARTESIAN_POINT('Ctrl Pts',(-1.01656661326717,-1.71634971283828,
93.8048661821745));
#10020=CARTESIAN_POINT('Ctrl Pts',(-0.991664843150677,-1.7308405114638,
93.8067237339182));
#10021=CARTESIAN_POINT('Ctrl Pts',(-0.97998571558448,-1.73747979637569,
93.8075820481971));
#10022=CARTESIAN_POINT('Ctrl Pts',(-0.950392146728589,-1.75390965119886,
93.8097264586801));
#10023=CARTESIAN_POINT('Ctrl Pts',(-0.93239231513687,-1.76354442690906,
93.811003139794));
#10024=CARTESIAN_POINT('Ctrl Pts',(-0.857933612010118,-1.80194116537811,
93.8161850359675));
#10025=CARTESIAN_POINT('Ctrl Pts',(-0.800263237426656,-1.82828397384793,
93.8199679620237));
#10026=CARTESIAN_POINT('Ctrl Pts',(-0.625710072406765,-1.898170864491,93.8310241635355));
#10027=CARTESIAN_POINT('Ctrl Pts',(-0.505900350255956,-1.93355417388032,
93.8381256182141));
#10028=CARTESIAN_POINT('Ctrl Pts',(-0.336565421072765,-1.96673473501722,
93.8482963851583));
#10029=CARTESIAN_POINT('Ctrl Pts',(-0.289247102256536,-1.97424858662186,
93.8511500261183));
#10030=CARTESIAN_POINT('Ctrl Pts',(-0.202964388590369,-1.98478117734626,
93.8564142697464));
#10031=CARTESIAN_POINT('Ctrl Pts',(-0.164094179975455,-1.98837211168075,
93.858807824392));
#10032=CARTESIAN_POINT('Ctrl Pts',(-0.100413548997051,-1.99237515783081,
93.8627792051893));
#10033=CARTESIAN_POINT('Ctrl Pts',(-0.0756556915753041,-1.99346878029904,
93.864335463143));
#10034=CARTESIAN_POINT('Ctrl Pts',(-0.027072715856891,-1.99470850317478,
93.8674164682595));
#10035=CARTESIAN_POINT('Ctrl Pts',(-0.00325261441307909,-1.99488954166603,
93.868939845437));
#10036=CARTESIAN_POINT('Ctrl Pts',(0.0555289642162972,-1.99428352097563,
93.8727330196911));
#10037=CARTESIAN_POINT('Ctrl Pts',(0.0904762358002397,-1.99300376862146,
93.8750178563666));
#10038=CARTESIAN_POINT('Ctrl Pts',(0.274301034826361,-1.981427490311,93.8871999151269));
#10039=CARTESIAN_POINT('Ctrl Pts',(0.421687035470673,-1.95536741019804,
93.8975850246593));
#10040=CARTESIAN_POINT('Ctrl Pts',(0.625894879735792,-1.89508473915859,
93.9124382178875));
#10041=CARTESIAN_POINT('Ctrl Pts',(0.686131356732233,-1.87411715377668,
93.9168725362948));
#10042=CARTESIAN_POINT('Ctrl Pts',(0.781875085440731,-1.83555354916185,
93.9239168798862));
#10043=CARTESIAN_POINT('Ctrl Pts',(0.818044345055888,-1.81972233848153,
93.9265767369699));
#10044=CARTESIAN_POINT('Ctrl Pts',(0.869091152501267,-1.79554930150296,
93.9303057495643));
#10045=CARTESIAN_POINT('Ctrl Pts',(0.884366808824619,-1.78807497646299,
93.9314183497518));
#10046=CARTESIAN_POINT('Ctrl Pts',(0.911410338073204,-1.77441130083946,
93.9333796991753));
#10047=CARTESIAN_POINT('Ctrl Pts',(0.923214409355658,-1.76829846017705,
93.9342326977994));
#10048=CARTESIAN_POINT('Ctrl Pts',(0.950462070276944,-1.75384078038997,
93.9361949943438));
#10049=CARTESIAN_POINT('Ctrl Pts',(0.965857939541601,-1.74540944260488,
93.9372989989004));
#10050=CARTESIAN_POINT('Ctrl Pts',(1.01608580483633,-1.71703466314968,93.9408916778265));
#10051=CARTESIAN_POINT('Ctrl Pts',(1.05042926877709,-1.69624208518923,93.943333733786));
#10052=CARTESIAN_POINT('Ctrl Pts',(1.20812630889072,-1.59413951647265,93.954590641622));
#10053=CARTESIAN_POINT('Ctrl Pts',(1.32283277100802,-1.50032314931616,93.9629388629905));
#10054=CARTESIAN_POINT('Ctrl Pts',(1.46172589069291,-1.35829908370278,93.9746151731138));
#10055=CARTESIAN_POINT('Ctrl Pts',(1.49591027729057,-1.32055705196346,93.9776389794543));
#10056=CARTESIAN_POINT('Ctrl Pts',(1.55479330926606,-1.25032235008209,93.9831776506486));
#10057=CARTESIAN_POINT('Ctrl Pts',(1.58000971394817,-1.21830093498907,93.9856722626986));
#10058=CARTESIAN_POINT('Ctrl Pts',(1.61914318833425,-1.16534665467781,93.9897657485668));
#10059=CARTESIAN_POINT('Ctrl Pts',(1.63367693174514,-1.14488299872273,93.9913402502351));
#10060=CARTESIAN_POINT('Ctrl Pts',(1.66113717488308,-1.10463081599153,93.9944264234733));
#10061=CARTESIAN_POINT('Ctrl Pts',(1.67410572826589,-1.08487597650066,93.9959361358999));
#10062=CARTESIAN_POINT('Ctrl Pts',(1.7047572779801,-1.0363260972633,93.9996370081963));
#10063=CARTESIAN_POINT('Ctrl Pts',(1.72206492551498,-1.00730398427055,94.0018415459047));
#10064=CARTESIAN_POINT('Ctrl Pts',(1.81596340937894,-0.84035293288418,94.0144875508056));
#10065=CARTESIAN_POINT('Ctrl Pts',(1.87670291423943,-0.694179647501685,
94.0254885712474));
#10066=CARTESIAN_POINT('Ctrl Pts',(1.94175888886326,-0.463948780345325,
94.0421682492272));
#10067=CARTESIAN_POINT('Ctrl Pts',(1.95910079833111,-0.384190465057437,
94.0478226945815));
#10068=CARTESIAN_POINT('Ctrl Pts',(1.97522663671268,-0.279468885810256,
94.0549261084285));
#10069=CARTESIAN_POINT('Ctrl Pts',(1.97849805899632,-0.255281577539669,
94.0565446128269));
#10070=CARTESIAN_POINT('Ctrl Pts',(1.98298256808391,-0.216823709869348,
94.059076691998));
#10071=CARTESIAN_POINT('Ctrl Pts',(1.98448722595458,-0.20259039251445,94.0600048729891));
#10072=CARTESIAN_POINT('Ctrl Pts',(1.987019541698,-0.175890127427713,94.0617277494856));
#10073=CARTESIAN_POINT('Ctrl Pts',(1.98808336972325,-0.163427447081837,
94.0625244646784));
#10074=CARTESIAN_POINT('Ctrl Pts',(1.99070843843327,-0.128838772818492,
94.0647170305938));
#10075=CARTESIAN_POINT('Ctrl Pts',(1.99201803098366,-0.10669478803277,94.0660996362109));
#10076=CARTESIAN_POINT('Ctrl Pts',(1.99854585342463,0.0472067020327452,
94.0755909836437));
#10077=CARTESIAN_POINT('Ctrl Pts',(1.99105823810366,0.179192468372397,94.0831471717682));
#10078=CARTESIAN_POINT('Ctrl Pts',(1.95434646639441,0.412947503039959,94.096877911222));
#10079=CARTESIAN_POINT('Ctrl Pts',(1.92997687187872,0.514958318723832,94.1029937156257));
#10080=CARTESIAN_POINT('Ctrl Pts',(1.88633522565453,0.649716131997069,94.1115962649241));
#10081=CARTESIAN_POINT('Ctrl Pts',(1.87398307316575,0.684528166074212,94.1138665942333));
#10082=CARTESIAN_POINT('Ctrl Pts',(1.85187751695145,0.741736217348781,94.1176898594097));
#10083=CARTESIAN_POINT('Ctrl Pts',(1.84266614439187,0.764332616874433,94.1192244790452));
#10084=CARTESIAN_POINT('Ctrl Pts',(1.82341094472551,0.80919495744426,94.1223235603189));
#10085=CARTESIAN_POINT('Ctrl Pts',(1.8133680430868,0.831456676394288,94.12388777873));
#10086=CARTESIAN_POINT('Ctrl Pts',(1.78706699842629,0.887012772082696,94.1278608872834));
#10087=CARTESIAN_POINT('Ctrl Pts',(1.77028581895735,0.92004778655433,94.1302875834516));
#10088=CARTESIAN_POINT('Ctrl Pts',(1.69124175549195,1.06547403385005,94.141267226823));
#10089=CARTESIAN_POINT('Ctrl Pts',(1.61913500289807,1.17214597465599,94.1501594368165));
#10090=CARTESIAN_POINT('Ctrl Pts',(1.48971703785157,1.32866236186849,94.164331767512));
#10091=CARTESIAN_POINT('Ctrl Pts',(1.43895183055248,1.38348075864037,94.1695474173394));
#10092=CARTESIAN_POINT('Ctrl Pts',(1.36345894261606,1.45633885224281,94.176730939166));
#10093=CARTESIAN_POINT('Ctrl Pts',(1.34120993733703,1.4768545049761,94.1787844058516));
#10094=CARTESIAN_POINT('Ctrl Pts',(1.30070335310181,1.51253460099505,94.1823992458531));
#10095=CARTESIAN_POINT('Ctrl Pts',(1.2826258261464,1.5278943816045,94.1839707406079));
#10096=CARTESIAN_POINT('Ctrl Pts',(1.25331526857232,1.55191148680318,94.1864472110057));
#10097=CARTESIAN_POINT('Ctrl Pts',(1.24225693369214,1.56077742511963,94.1873657864092));
#10098=CARTESIAN_POINT('Ctrl Pts',(1.22118572201773,1.5773052681468,94.1890850701671));
#10099=CARTESIAN_POINT('Ctrl Pts',(1.21119302545486,1.58499146765078,94.1898875683919));
#10100=CARTESIAN_POINT('Ctrl Pts',(1.18296475799256,1.60628126169809,94.1921208930795));
#10101=CARTESIAN_POINT('Ctrl Pts',(1.16456777383121,1.61966882870458,94.1935376195694));
#10102=CARTESIAN_POINT('Ctrl Pts',(1.04219267490347,1.7055582964341,94.2027390201555));
#10103=CARTESIAN_POINT('Ctrl Pts',(0.931722647487114,1.76833127626115,94.2100198962002));
#10104=CARTESIAN_POINT('Ctrl Pts',(0.717582925363837,1.86433421530465,94.2236322613004));
#10105=CARTESIAN_POINT('Ctrl Pts',(0.615727053153437,1.90040639267756,94.2299212430756));
#10106=CARTESIAN_POINT('Ctrl Pts',(0.475372728777888,1.93763831568532,94.2387351459183));
#10107=CARTESIAN_POINT('Ctrl Pts',(0.43902602604148,1.94619560862729,94.2410291078333));
#10108=CARTESIAN_POINT('Ctrl Pts',(0.378493014018842,1.95866523641376,94.2448806889106));
#10109=CARTESIAN_POINT('Ctrl Pts',(0.354435782124617,1.96316113975725,94.2464193819229));
#10110=CARTESIAN_POINT('Ctrl Pts',(0.306287980925508,1.97124534322307,94.2495177548893));
#10111=CARTESIAN_POINT('Ctrl Pts',(0.282202317599193,1.97483728318786,94.2510770270853));
#10112=CARTESIAN_POINT('Ctrl Pts',(0.221711923730755,1.98272915266453,94.2550189041925));
#10113=CARTESIAN_POINT('Ctrl Pts',(0.185244417643904,1.98646804170269,94.2574187271263));
#10114=CARTESIAN_POINT('Ctrl Pts',(0.0537425722199683,1.99629805712961,
94.2661614256868));
#10115=CARTESIAN_POINT('Ctrl Pts',(-0.0415858162103165,1.99658726086145,
94.2726734217836));
#10116=CARTESIAN_POINT('Ctrl Pts',(-0.265009734361744,1.98125579170285,
94.2882217314387));
#10117=CARTESIAN_POINT('Ctrl Pts',(-0.392306789321386,1.96002603095119,
94.2973125324171));
#10118=CARTESIAN_POINT('Ctrl Pts',(-0.545321495904473,1.91899239750081,
94.3080128319002));
#10119=CARTESIAN_POINT('Ctrl Pts',(-0.573797441173737,1.91067110436594,
94.3099929229632));
#10120=CARTESIAN_POINT('Ctrl Pts',(-0.616708338418779,1.89708562312931,
94.3129489716658));
#10121=CARTESIAN_POINT('Ctrl Pts',(-0.631284456391861,1.89228512864927,
94.3139481499711));
#10122=CARTESIAN_POINT('Ctrl Pts',(-0.6585252827618,1.88296383021898,94.3158042671725));
#10123=CARTESIAN_POINT('Ctrl Pts',(-0.671201892513914,1.87848246245331,
94.3166632005401));
#10124=CARTESIAN_POINT('Ctrl Pts',(-0.703076964403794,1.86685029177569,
94.3188126363815));
#10125=CARTESIAN_POINT('Ctrl Pts',(-0.722212937587476,1.85953106485829,
94.3200936224265));
#10126=CARTESIAN_POINT('Ctrl Pts',(-0.805697204827674,1.82611633087875,
94.3256548311249));
#10127=CARTESIAN_POINT('Ctrl Pts',(-0.868776220092474,1.79696372066087,
94.3297856004103));
#10128=CARTESIAN_POINT('Ctrl Pts',(-1.03635689587212,1.70862218497011,94.3408921083088));
#10129=CARTESIAN_POINT('Ctrl Pts',(-1.13723611467703,1.64320418712213,94.3477399635334));
#10130=CARTESIAN_POINT('Ctrl Pts',(-1.268728526189,1.53999358369181,94.3575999267126));
#10131=CARTESIAN_POINT('Ctrl Pts',(-1.304784793124,1.50956567819077,94.3604121429735));
#10132=CARTESIAN_POINT('Ctrl Pts',(-1.36832824530758,1.45196267621233,94.3656092001478));
#10133=CARTESIAN_POINT('Ctrl Pts',(-1.39616900729853,1.42521212514782,94.3679777324168));
#10134=CARTESIAN_POINT('Ctrl Pts',(-1.44052346478258,1.38004707743838,94.3719189529604));
#10135=CARTESIAN_POINT('Ctrl Pts',(-1.45750252326476,1.36210282112052,94.3734707479523));
#10136=CARTESIAN_POINT('Ctrl Pts',(-1.49022765095059,1.32620477895533,94.3765510681031));
#10137=CARTESIAN_POINT('Ctrl Pts',(-1.5059932432108,1.30827437357928,94.3780783771192));
#10138=CARTESIAN_POINT('Ctrl Pts',(-1.54426016921174,1.26314447034638,94.3818974987313));
#10139=CARTESIAN_POINT('Ctrl Pts',(-1.56636778168429,1.23562337772486,94.3842048245139));
#10140=CARTESIAN_POINT('Ctrl Pts',(-1.61545779480429,1.17107698714966,94.3895708216905));
#10141=CARTESIAN_POINT('Ctrl Pts',(-1.64189998476113,1.13370357502457,94.3926453687346));
#10142=CARTESIAN_POINT('Ctrl Pts',(-1.66701746607045,1.09548178000186,94.3957559446131));
#10143=CARTESIAN_POINT('Origin',(0.,0.,89.2710285354474));
#10144=CARTESIAN_POINT('',(-1.66701714412027,1.09548226992002,95.3554060137221));
#10145=CARTESIAN_POINT('',(-1.66701720893993,1.09548217128264,95.1987207124569));
#10146=CARTESIAN_POINT('',(-1.66701720851066,1.09548217193587,89.2710285354474));
#10147=CARTESIAN_POINT('Ctrl Pts',(-1.66701714412024,1.09548226992006,95.3554060137221));
#10148=CARTESIAN_POINT('Ctrl Pts',(-1.64000640050892,1.13658505534331,95.3519840620999));
#10149=CARTESIAN_POINT('Ctrl Pts',(-1.61146537971087,1.17670425752475,95.3485433737237));
#10150=CARTESIAN_POINT('Ctrl Pts',(-1.53292208075897,1.27887297180187,95.3395615817572));
#10151=CARTESIAN_POINT('Ctrl Pts',(-1.48065870255216,1.3390362592318,95.3340455315168));
#10152=CARTESIAN_POINT('Ctrl Pts',(-1.40801552310433,1.41318944202132,95.3270887724191));
#10153=CARTESIAN_POINT('Ctrl Pts',(-1.39078269325614,1.43015234785357,95.3254858138427));
#10154=CARTESIAN_POINT('Ctrl Pts',(-1.36289667472665,1.45662066896006,95.322972014917));
#10155=CARTESIAN_POINT('Ctrl Pts',(-1.35244305211034,1.46633179783612,95.3220469045316));
#10156=CARTESIAN_POINT('Ctrl Pts',(-1.33260507548917,1.48436808178,95.3203249220826));
#10157=CARTESIAN_POINT('Ctrl Pts',(-1.32324473203996,1.49271842259496,95.3195261043901));
#10158=CARTESIAN_POINT('Ctrl Pts',(-1.29697036202853,1.51571634336574,95.3173195269075));
#10159=CARTESIAN_POINT('Ctrl Pts',(-1.2798872036958,1.53016894458555,95.3159253000714));
#10160=CARTESIAN_POINT('Ctrl Pts',(-1.16180158695774,1.62670947545258,95.3065309272179));
#10161=CARTESIAN_POINT('Ctrl Pts',(-1.05320615018574,1.69903854536474,95.2990667087308));
#10162=CARTESIAN_POINT('Ctrl Pts',(-0.844981353867737,1.81003398973017,
95.285376251291));
#10163=CARTESIAN_POINT('Ctrl Pts',(-0.747836220846204,1.85228359813868,
95.2792028864927));
#10164=CARTESIAN_POINT('Ctrl Pts',(-0.61274129340497,1.89867061105845,95.2705297819906));
#10165=CARTESIAN_POINT('Ctrl Pts',(-0.577350616843583,1.90972981788722,
95.2682512161602));
#10166=CARTESIAN_POINT('Ctrl Pts',(-0.518160901684755,1.92643030548239,
95.2644177399511));
#10167=CARTESIAN_POINT('Ctrl Pts',(-0.494528792083287,1.93263178862709,
95.2628813510899));
#10168=CARTESIAN_POINT('Ctrl Pts',(-0.44707260379844,1.94415774161554,95.2597815261279));
#10169=CARTESIAN_POINT('Ctrl Pts',(-0.423252849652262,1.94948202728075,
95.2582183857543));
#10170=CARTESIAN_POINT('Ctrl Pts',(-0.363154823951822,1.96176205030644,
95.2542538868453));
#10171=CARTESIAN_POINT('Ctrl Pts',(-0.32677116801332,1.96814940243149,95.2518348981535));
#10172=CARTESIAN_POINT('Ctrl Pts',(-0.161170245646818,1.99250324752168,
95.2407334857278));
#10173=CARTESIAN_POINT('Ctrl Pts',(-0.0305751668670882,1.99877476163169,
95.2316992618598));
#10174=CARTESIAN_POINT('Ctrl Pts',(0.173037175092029,1.98858769896971,95.2174721654136));
#10175=CARTESIAN_POINT('Ctrl Pts',(0.246142544232215,1.98086789116589,95.2123424697461));
#10176=CARTESIAN_POINT('Ctrl Pts',(0.348270769375714,1.96434083538861,95.2052611590111));
#10177=CARTESIAN_POINT('Ctrl Pts',(0.377773255114963,1.95888105674249,95.2032260225623));
#10178=CARTESIAN_POINT('Ctrl Pts',(0.430216521192827,1.94794682925256,95.1996394916636));
#10179=CARTESIAN_POINT('Ctrl Pts',(0.453204446764953,1.94272719427836,95.1980781915435));
#10180=CARTESIAN_POINT('Ctrl Pts',(0.489832563574475,1.93372483165117,95.1956135761548));
#10181=CARTESIAN_POINT('Ctrl Pts',(0.503533813988761,1.93020242434779,95.1946968800585));
#10182=CARTESIAN_POINT('Ctrl Pts',(0.531141981485651,1.92279074114548,95.192861926143));
#10183=CARTESIAN_POINT('Ctrl Pts',(0.5450463802842,1.9188956493574,95.1919440307082));
#10184=CARTESIAN_POINT('Ctrl Pts',(0.582922552044203,1.90784032425974,95.1894576664844));
#10185=CARTESIAN_POINT('Ctrl Pts',(0.606804644935765,1.90037934683931,95.1879053828174));
#10186=CARTESIAN_POINT('Ctrl Pts',(0.718287091064494,1.86323515807974,95.1807045866458));
#10187=CARTESIAN_POINT('Ctrl Pts',(0.80390269635338,1.82792930098886,95.1753039603777));
#10188=CARTESIAN_POINT('Ctrl Pts',(0.974086549453968,1.7434694797139,95.16427192238));
#10189=CARTESIAN_POINT('Ctrl Pts',(1.0581113476354,1.69379157978336,95.158655870719));
#10190=CARTESIAN_POINT('Ctrl Pts',(1.18868792745926,1.60306998733783,95.1492343798801));
#10191=CARTESIAN_POINT('Ctrl Pts',(1.23755643119603,1.56565175523927,95.1455322257767));
#10192=CARTESIAN_POINT('Ctrl Pts',(1.30650373206005,1.50761207985663,95.1399814498158));
#10193=CARTESIAN_POINT('Ctrl Pts',(1.32799246049851,1.48871826687761,95.1382014755914));
#10194=CARTESIAN_POINT('Ctrl Pts',(1.36623771251457,1.45360430197288,95.1349360262293));
#10195=CARTESIAN_POINT('Ctrl Pts',(1.38313054452707,1.43753983422498,95.1334573380849));
#10196=CARTESIAN_POINT('Ctrl Pts',(1.41962970835688,1.40159145536372,95.1301788495971));
#10197=CARTESIAN_POINT('Ctrl Pts',(1.43910756775304,1.38158473972121,95.1283737462407));
#10198=CARTESIAN_POINT('Ctrl Pts',(1.49701301251369,1.31955362327645,95.1228316039774));
#10199=CARTESIAN_POINT('Ctrl Pts',(1.53406420810023,1.27628980992534,95.1190385783563));
#10200=CARTESIAN_POINT('Ctrl Pts',(1.66067064850778,1.11496487680025,95.1051490975733));
#10201=CARTESIAN_POINT('Ctrl Pts',(1.73885720476997,0.988605557061351,95.0946895564644));
#10202=CARTESIAN_POINT('Ctrl Pts',(1.81990456802142,0.817714924312398,95.0816091433359));
#10203=CARTESIAN_POINT('Ctrl Pts',(1.83633639577286,0.780114954124258,95.0787950208599));
#10204=CARTESIAN_POINT('Ctrl Pts',(1.86257450586625,0.714642906436793,95.074031853511));
#10205=CARTESIAN_POINT('Ctrl Pts',(1.87294278370813,0.687010783473413,95.0720623495546));
#10206=CARTESIAN_POINT('Ctrl Pts',(1.88775676664163,0.644698859152281,95.0691184266652));
#10207=CARTESIAN_POINT('Ctrl Pts',(1.89265229374907,0.63018216463559,95.0681210629457));
#10208=CARTESIAN_POINT('Ctrl Pts',(1.90153441752246,0.602806443425458,95.0662658162068));
#10209=CARTESIAN_POINT('Ctrl Pts',(1.90555883430308,0.589961258570713,95.0654059860135));
#10210=CARTESIAN_POINT('Ctrl Pts',(1.91540290507772,0.557388787449253,95.0632506806532));
#10211=CARTESIAN_POINT('Ctrl Pts',(1.92104823126789,0.537609822967386,95.0619648335877));
#10212=CARTESIAN_POINT('Ctrl Pts',(1.94477135643207,0.449342791310319,95.0563133417703));
#10213=CARTESIAN_POINT('Ctrl Pts',(1.95950129187206,0.3800016458441,95.052103461659));
#10214=CARTESIAN_POINT('Ctrl Pts',(1.98898019562982,0.192629922334281,95.0409907313784));
#10215=CARTESIAN_POINT('Ctrl Pts',(1.99692223099103,0.0738280114103413,
95.034206047352));
#10216=CARTESIAN_POINT('Ctrl Pts',(1.99318363263276,-0.091944548102242,
95.0244236391947));
#10217=CARTESIAN_POINT('Ctrl Pts',(1.99046539747487,-0.138859211699801,
95.0216219725172));
#10218=CARTESIAN_POINT('Ctrl Pts',(1.98251119776994,-0.223961864711707,
95.0164419218809));
#10219=CARTESIAN_POINT('Ctrl Pts',(1.97782003657836,-0.262177744840459,
95.0140796578135));
#10220=CARTESIAN_POINT('Ctrl Pts',(1.96831060242317,-0.324638926262241,
95.0101456856472));
#10221=CARTESIAN_POINT('Ctrl Pts',(1.96414213997096,-0.348973675619511,
95.0085946977961));
#10222=CARTESIAN_POINT('Ctrl Pts',(1.95505195471309,-0.39669952366313,95.0055136460254));
#10223=CARTESIAN_POINT('Ctrl Pts',(1.95015930732267,-0.420091955768283,
95.0039847553345));
#10224=CARTESIAN_POINT('Ctrl Pts',(1.93697836674742,-0.477907696068513,
95.0001569487279));
#10225=CARTESIAN_POINT('Ctrl Pts',(1.92819187305794,-0.512207763929782,
94.9978423713254));
#10226=CARTESIAN_POINT('Ctrl Pts',(1.87855338009975,-0.68654299343533,94.9858461317687));
#10227=CARTESIAN_POINT('Ctrl Pts',(1.82334749995286,-0.822006467192766,
94.9757031394992));
#10228=CARTESIAN_POINT('Ctrl Pts',(1.71177446885238,-1.0279448039999,94.9593612284853));
#10229=CARTESIAN_POINT('Ctrl Pts',(1.66453984848377,-1.10279278426571,94.9532115513421));
#10230=CARTESIAN_POINT('Ctrl Pts',(1.59766696571887,-1.19462212411728,94.9455864470728));
#10231=CARTESIAN_POINT('Ctrl Pts',(1.58245720008408,-1.21469794714771,94.9439144924345));
#10232=CARTESIAN_POINT('Ctrl Pts',(1.55791419072324,-1.24584926073553,94.9413190890251));
#10233=CARTESIAN_POINT('Ctrl Pts',(1.54883408112337,-1.25711973448196,94.9403798573355));
#10234=CARTESIAN_POINT('Ctrl Pts',(1.5306563100003,-1.27918649865755,94.9385421608716));
#10235=CARTESIAN_POINT('Ctrl Pts',(1.52156519604381,-1.28998690452822,94.9376433913933));
#10236=CARTESIAN_POINT('Ctrl Pts',(1.49708626919025,-1.31844944579232,94.9352738577021));
#10237=CARTESIAN_POINT('Ctrl Pts',(1.48150018175619,-1.33593920619831,94.9338167763371));
#10238=CARTESIAN_POINT('Ctrl Pts',(1.38381720636386,-1.44174041191605,94.92496617921));
#10239=CARTESIAN_POINT('Ctrl Pts',(1.29415178834417,-1.52274210553938,94.9180209318477));
#10240=CARTESIAN_POINT('Ctrl Pts',(1.11212782056348,-1.6594133209955,94.9048220050446));
#10241=CARTESIAN_POINT('Ctrl Pts',(1.02152152690275,-1.71667466565261,94.8985988335062));
#10242=CARTESIAN_POINT('Ctrl Pts',(0.891124553348857,-1.78508947791917,
94.8896944792892));
#10243=CARTESIAN_POINT('Ctrl Pts',(0.854928997228063,-1.80270449208195,
94.8872294129879));
#10244=CARTESIAN_POINT('Ctrl Pts',(0.795417981461111,-1.82947077154647,
94.8831713582245));
#10245=CARTESIAN_POINT('Ctrl Pts',(0.772418700767902,-1.83929941253145,
94.8816019034032));
#10246=CARTESIAN_POINT('Ctrl Pts',(0.72728685582231,-1.85759052815895,94.8785167332748));
#10247=CARTESIAN_POINT('Ctrl Pts',(0.705176261857091,-1.86609621950026,
94.8770028063069));
#10248=CARTESIAN_POINT('Ctrl Pts',(0.650853481422376,-1.88589026949441,
94.873274938858));
#10249=CARTESIAN_POINT('Ctrl Pts',(0.618493943138326,-1.89674915734738,
94.8710471496236));
#10250=CARTESIAN_POINT('Ctrl Pts',(0.437347017908791,-1.95240822628186,
94.8585293213655));
#10251=CARTESIAN_POINT('Ctrl Pts',(0.28401948116203,-1.98052696612134,94.8477003508948));
#10252=CARTESIAN_POINT('Ctrl Pts',(0.0463333531054047,-1.99593240325661,
94.8310914956814));
#10253=CARTESIAN_POINT('Ctrl Pts',(-0.0366113899861371,-1.9961349651935,
94.8253419842448));
#10254=CARTESIAN_POINT('Ctrl Pts',(-0.143851229570361,-1.98970792664064,
94.81813780822));
#10255=CARTESIAN_POINT('Ctrl Pts',(-0.168340459620043,-1.98778581095932,
94.8165085430132));
#10256=CARTESIAN_POINT('Ctrl Pts',(-0.207068256653312,-1.98402522990132,
94.8139635693902));
#10257=CARTESIAN_POINT('Ctrl Pts',(-0.221332457634056,-1.98248464050104,
94.81303302242));
#10258=CARTESIAN_POINT('Ctrl Pts',(-0.247983695250929,-1.97931495582176,
94.8113087157904));
#10259=CARTESIAN_POINT('Ctrl Pts',(-0.260374301620065,-1.97772314767735,
94.8105128894812));
#10260=CARTESIAN_POINT('Ctrl Pts',(-0.29461631657724,-1.97299671976163,
94.8083277114931));
#10261=CARTESIAN_POINT('Ctrl Pts',(-0.316432610203252,-1.96961552833803,
94.8069514447082));
#10262=CARTESIAN_POINT('Ctrl Pts',(-0.469086759411744,-1.94335441541403,
94.7974051694603));
#10263=CARTESIAN_POINT('Ctrl Pts',(-0.597424957286881,-1.90781582519287,
94.7897972057455));
#10264=CARTESIAN_POINT('Ctrl Pts',(-0.818379850211406,-1.82212139989698,
94.7760437422254));
#10265=CARTESIAN_POINT('Ctrl Pts',(-0.912363128409627,-1.77692503036384,
94.7699604989349));
#10266=CARTESIAN_POINT('Ctrl Pts',(-1.03425322739517,-1.70607929316196,
94.7613974419449));
#10267=CARTESIAN_POINT('Ctrl Pts',(-1.06560088140683,-1.6866774406634,94.7591313624949));
#10268=CARTESIAN_POINT('Ctrl Pts',(-1.11676936485749,-1.65301202469281,
94.7553128672792));
#10269=CARTESIAN_POINT('Ctrl Pts',(-1.13689871103542,-1.63923268756043,
94.7537786531774));
#10270=CARTESIAN_POINT('Ctrl Pts',(-1.17668338959991,-1.61091317322565,
94.7506784710887));
#10271=CARTESIAN_POINT('Ctrl Pts',(-1.19633413918716,-1.59637388794437,
94.749112711366));
#10272=CARTESIAN_POINT('Ctrl Pts',(-1.24516197761499,-1.55883899763492,
94.7451315420696));
#10273=CARTESIAN_POINT('Ctrl Pts',(-1.27397201865552,-1.53538345699506,
94.7426981853701));
#10274=CARTESIAN_POINT('Ctrl Pts',(-1.39792537087027,-1.42857606464283,
94.731842998691));
#10275=CARTESIAN_POINT('Ctrl Pts',(-1.4856585814445,-1.33709933737728,94.7230942628763));
#10276=CARTESIAN_POINT('Ctrl Pts',(-1.61122987556561,-1.17844192674678,
94.7089757223603));
#10277=CARTESIAN_POINT('Ctrl Pts',(-1.65489577017786,-1.11629204553124,
94.7036712708942));
#10278=CARTESIAN_POINT('Ctrl Pts',(-1.71101225266918,-1.02586382855634,
94.696382108899));
#10279=CARTESIAN_POINT('Ctrl Pts',(-1.72651249531619,-0.999557059447308,
94.6943096803854));
#10280=CARTESIAN_POINT('Ctrl Pts',(-1.75304784994849,-0.952061336780932,
94.6906654158869));
#10281=CARTESIAN_POINT('Ctrl Pts',(-1.76431771260774,-0.931010571136016,
94.6890832373839));
#10282=CARTESIAN_POINT('Ctrl Pts',(-1.78168680844721,-0.897118446140278,
94.6865939734653));
#10283=CARTESIAN_POINT('Ctrl Pts',(-1.78803114405685,-0.88440604439966,
94.685673063538));
#10284=CARTESIAN_POINT('Ctrl Pts',(-1.80051842169671,-0.858701035039137,
94.6838381313032));
#10285=CARTESIAN_POINT('Ctrl Pts',(-1.80665784649302,-0.845707698218548,
94.6829243335641));
#10286=CARTESIAN_POINT('Ctrl Pts',(-1.82295750055046,-0.810223735175114,
94.6804628630978));
#10287=CARTESIAN_POINT('Ctrl Pts',(-1.83284198127424,-0.787608374228948,
94.6789308326135));
#10288=CARTESIAN_POINT('Ctrl Pts',(-1.8741878208184,-0.688013422227519,
94.6723186152871));
#10289=CARTESIAN_POINT('Ctrl Pts',(-1.9012405036474,-0.60928621840954,94.6674368873436));
#10290=CARTESIAN_POINT('Ctrl Pts',(-1.94315050863123,-0.456939609295913,
94.6582433561534));
#10291=CARTESIAN_POINT('Ctrl Pts',(-1.95892355149556,-0.383726693627432,
94.6539306291679));
#10292=CARTESIAN_POINT('Ctrl Pts',(-1.97965101114832,-0.251885878741675,
94.6461314979659));
#10293=CARTESIAN_POINT('Ctrl Pts',(-1.98619806998029,-0.193600586003824,
94.6426728484757));
#10294=CARTESIAN_POINT('Ctrl Pts',(-1.99321318099655,-0.0902714636182581,
94.6364442687785));
#10295=CARTESIAN_POINT('Ctrl Pts',(-1.99474094538159,-0.0453412368257697,
94.6337039991689));
#10296=CARTESIAN_POINT('Ctrl Pts',(-1.99475515014938,0.0254756584597319,
94.6293124195342));
#10297=CARTESIAN_POINT('Ctrl Pts',(-1.99425685285608,0.0513480592313933,
94.6276928372794));
#10298=CARTESIAN_POINT('Ctrl Pts',(-1.9923424517438,0.100775079815879,94.6245661517782));
#10299=CARTESIAN_POINT('Ctrl Pts',(-1.99101139003775,0.124328707273745,
94.6230619980674));
#10300=CARTESIAN_POINT('Ctrl Pts',(-1.98690200403548,0.179617971685833,
94.619495442874));
#10301=CARTESIAN_POINT('Ctrl Pts',(-1.98378060979329,0.211320813876593,
94.6174225667285));
#10302=CARTESIAN_POINT('Ctrl Pts',(-1.9688021423382,0.333394744469055,94.6093282535835));
#10303=CARTESIAN_POINT('Ctrl Pts',(-1.95151755653796,0.422976674579823,
94.6031422473714));
#10304=CARTESIAN_POINT('Ctrl Pts',(-1.91010256459144,0.57923288766905,94.5919691421925));
#10305=CARTESIAN_POINT('Ctrl Pts',(-1.88842884801342,0.646404293885178,
94.5870365336252));
#10306=CARTESIAN_POINT('Ctrl Pts',(-1.83407770900289,0.788579857640487,
94.5764240467774));
#10307=CARTESIAN_POINT('Ctrl Pts',(-1.80025018444409,0.863018362847558,
94.5707583942592));
#10308=CARTESIAN_POINT('Ctrl Pts',(-1.75039987305223,0.956940369494432,
94.5636271569895));
#10309=CARTESIAN_POINT('Ctrl Pts',(-1.73844631861725,0.97848817864638,94.561992624652));
#10310=CARTESIAN_POINT('Ctrl Pts',(-1.71889756798875,1.01223760692697,94.5594414265673));
#10311=CARTESIAN_POINT('Ctrl Pts',(-1.71156488974823,1.02458746879418,94.5585098067686));
#10312=CARTESIAN_POINT('Ctrl Pts',(-1.69671073008836,1.04900062224592,94.5566737249281));
#10313=CARTESIAN_POINT('Ctrl Pts',(-1.68919244049364,1.06106481073259,94.5557691690028));
#10314=CARTESIAN_POINT('Ctrl Pts',(-1.67675295115384,1.08055841072364,94.5543103505775));
#10315=CARTESIAN_POINT('Ctrl Pts',(-1.67191004952877,1.08803663755448,94.5537513883947));
#10316=CARTESIAN_POINT('Ctrl Pts',(-1.66701720848889,1.09548217196899,94.5531952825684));
#10317=CARTESIAN_POINT('Ctrl Pts',(-1.66701746607045,1.09548178000186,94.3957559446131));
#10318=CARTESIAN_POINT('Ctrl Pts',(-1.72234085055941,1.0112950322998,94.4026072520028));
#10319=CARTESIAN_POINT('Ctrl Pts',(-1.77123728885008,0.922992974446591,
94.4096419874811));
#10320=CARTESIAN_POINT('Ctrl Pts',(-1.84990319857548,0.751408149615364,
94.4228114350097));
#10321=CARTESIAN_POINT('Ctrl Pts',(-1.88122093678841,0.66915342018724,94.4289257276447));
#10322=CARTESIAN_POINT('Ctrl Pts',(-1.91438130181607,0.561073221213647,
94.4365135640341));
#10323=CARTESIAN_POINT('Ctrl Pts',(-1.92129735696453,0.536912966604122,
94.438181669056));
#10324=CARTESIAN_POINT('Ctrl Pts',(-1.93147103579295,0.498654433812127,
94.4407723694985));
#10325=CARTESIAN_POINT('Ctrl Pts',(-1.93503477698584,0.48464115568311,94.4417106638947));
#10326=CARTESIAN_POINT('Ctrl Pts',(-1.94177710867641,0.456868253884788,
94.4435476402762));
#10327=CARTESIAN_POINT('Ctrl Pts',(-1.94496255449358,0.443111301035664,
94.4444466090214));
#10328=CARTESIAN_POINT('Ctrl Pts',(-1.95304993685363,0.406415625350268,
94.4468182731131));
#10329=CARTESIAN_POINT('Ctrl Pts',(-1.95769399326869,0.383421515032688,
94.4482772346208));
#10330=CARTESIAN_POINT('Ctrl Pts',(-1.98365164534925,0.242094518024507,
94.4571082998858));
#10331=CARTESIAN_POINT('Ctrl Pts',(-1.9946381206811,0.122103299536532,94.464035045935));
#10332=CARTESIAN_POINT('Ctrl Pts',(-1.99485382532739,-0.111537975921789,
94.4775828400643));
#10333=CARTESIAN_POINT('Ctrl Pts',(-1.9852921665754,-0.224709168571586,
94.4841770799989));
#10334=CARTESIAN_POINT('Ctrl Pts',(-1.95989974512443,-0.373099245030639,
94.49331692478));
#10335=CARTESIAN_POINT('Ctrl Pts',(-1.95260521739944,-0.409563976140234,
94.4956018757191));
#10336=CARTESIAN_POINT('Ctrl Pts',(-1.93883316378939,-0.469628670061659,
94.4994426540661));
#10337=CARTESIAN_POINT('Ctrl Pts',(-1.93293267397357,-0.493352122937258,
94.5009797886316));
#10338=CARTESIAN_POINT('Ctrl Pts',(-1.92028032840084,-0.540504643114598,
94.5040783918586));
#10339=CARTESIAN_POINT('Ctrl Pts',(-1.91353191742561,-0.563930245920264,
94.5056395149832));
#10340=CARTESIAN_POINT('Ctrl Pts',(-1.89552229117753,-0.622396310368928,
94.5095930982492));
#10341=CARTESIAN_POINT('Ctrl Pts',(-1.88371783338206,-0.657258510208223,
94.512002996197));
#10342=CARTESIAN_POINT('Ctrl Pts',(-1.83498734577181,-0.789054196339219,
94.5213208978034));
#10343=CARTESIAN_POINT('Ctrl Pts',(-1.79149044277126,-0.883369610399564,
94.5284358580718));
#10344=CARTESIAN_POINT('Ctrl Pts',(-1.67567408528248,-1.09040106452989,
94.5449391366079));
#10345=CARTESIAN_POINT('Ctrl Pts',(-1.5989425966499,-1.20010198722774,94.5543599074582));
#10346=CARTESIAN_POINT('Ctrl Pts',(-1.49747402565541,-1.31798434826651,
94.5647442706119));
#10347=CARTESIAN_POINT('Ctrl Pts',(-1.48285185569662,-1.33441435510216,
94.5661975063757));
#10348=CARTESIAN_POINT('Ctrl Pts',(-1.45951349449258,-1.35978070111148,
94.568445970764));
#10349=CARTESIAN_POINT('Ctrl Pts',(-1.45098049411716,-1.36888232677686,
94.5692537347906));
#10350=CARTESIAN_POINT('Ctrl Pts',(-1.43244180215702,-1.38828826393017,
94.5709769893516));
#10351=CARTESIAN_POINT('Ctrl Pts',(-1.42240902672103,-1.39856584101785,
94.5718902871724));
#10352=CARTESIAN_POINT('Ctrl Pts',(-1.39485738025176,-1.42618654997126,
94.5743495602532));
#10353=CARTESIAN_POINT('Ctrl Pts',(-1.37712607675265,-1.44331531015171,
94.5758799348214));
#10354=CARTESIAN_POINT('Ctrl Pts',(-1.29784945597035,-1.51710646432063,
94.582521202334));
#10355=CARTESIAN_POINT('Ctrl Pts',(-1.23308714688521,-1.57019873161565,
94.5874309014939));
#10356=CARTESIAN_POINT('Ctrl Pts',(-1.04021287089503,-1.70900209521139,
94.6012556493916));
#10357=CARTESIAN_POINT('Ctrl Pts',(-0.905270696982442,-1.78415584065899,
94.6100631946339));
#10358=CARTESIAN_POINT('Ctrl Pts',(-0.731321434214433,-1.85617198949191,
94.6215405815396));
#10359=CARTESIAN_POINT('Ctrl Pts',(-0.69927868039424,-1.86847922213847,
94.6236570949731));
#10360=CARTESIAN_POINT('Ctrl Pts',(-0.64458601544131,-1.88788209684428,
94.6272828391324));
#10361=CARTESIAN_POINT('Ctrl Pts',(-0.622097422547269,-1.89541147545236,
94.628777316197));
#10362=CARTESIAN_POINT('Ctrl Pts',(-0.575687301915362,-1.91003508518783,
94.6318715994443));
#10363=CARTESIAN_POINT('Ctrl Pts',(-0.551756304930712,-1.9170849699942,
94.6334725642319));
#10364=CARTESIAN_POINT('Ctrl Pts',(-0.489192642572395,-1.93424728039212,
94.6376746892442));
#10365=CARTESIAN_POINT('Ctrl Pts',(-0.450379009383618,-1.94365129394204,
94.6402981394614));
#10366=CARTESIAN_POINT('Ctrl Pts',(-0.298048564977516,-1.97575119060712,
94.6506635346371));
#10367=CARTESIAN_POINT('Ctrl Pts',(-0.182937796229097,-1.9897117387946,
94.658661872608));
#10368=CARTESIAN_POINT('Ctrl Pts',(0.0440314465671003,-1.9973716754297,
94.6745026431037));
#10369=CARTESIAN_POINT('Ctrl Pts',(0.155471852321721,-1.99179929765975,
94.682308631613));
#10370=CARTESIAN_POINT('Ctrl Pts',(0.289658813082551,-1.97375313436064,
94.6913797609719));
#10371=CARTESIAN_POINT('Ctrl Pts',(0.313388380668226,-1.97012474462161,
94.6929706944434));
#10372=CARTESIAN_POINT('Ctrl Pts',(0.351073161289664,-1.96366435191211,
94.6954701488235));
#10373=CARTESIAN_POINT('Ctrl Pts',(0.365072862796352,-1.96110986152983,
94.6963926829507));
#10374=CARTESIAN_POINT('Ctrl Pts',(0.393119375069116,-1.95568152830216,
94.6982271523147));
#10375=CARTESIAN_POINT('Ctrl Pts',(0.407164912396803,-1.95280563492537,
94.6991389232492));
#10376=CARTESIAN_POINT('Ctrl Pts',(0.445149487690522,-1.94460044857614,
94.70158891864));
#10377=CARTESIAN_POINT('Ctrl Pts',(0.469023988048549,-1.93898055613956,
94.7031117428312));
#10378=CARTESIAN_POINT('Ctrl Pts',(0.572789215257659,-1.91252605846039,
94.7096797066495));
#10379=CARTESIAN_POINT('Ctrl Pts',(0.651453257493272,-1.88718168619305,
94.7145287383811));
#10380=CARTESIAN_POINT('Ctrl Pts',(0.873467432677757,-1.80010789860049,
94.7284076062172));
#10381=CARTESIAN_POINT('Ctrl Pts',(1.0114211788061,-1.72637109465251,94.7373199644767));
#10382=CARTESIAN_POINT('Ctrl Pts',(1.16732780025472,-1.61787905999709,94.748904218046));
#10383=CARTESIAN_POINT('Ctrl Pts',(1.19477131620079,-1.59771966704374,94.7510046580032));
#10384=CARTESIAN_POINT('Ctrl Pts',(1.24039657803675,-1.56237134365112,94.754611567818));
#10385=CARTESIAN_POINT('Ctrl Pts',(1.2588486276319,-1.54754254897465,94.7561036703488));
#10386=CARTESIAN_POINT('Ctrl Pts',(1.29625432672046,-1.51637014120827,94.7592007090007));
#10387=CARTESIAN_POINT('Ctrl Pts',(1.31517294847959,-1.49999123509994,94.7608069420687));
#10388=CARTESIAN_POINT('Ctrl Pts',(1.3637743533284,-1.45628789726547,94.7650417173248));
#10389=CARTESIAN_POINT('Ctrl Pts',(1.39294382588228,-1.42841241744161,94.7676932150616));
#10390=CARTESIAN_POINT('Ctrl Pts',(1.50100631575798,-1.31868436363296,94.7779525906848));
#10391=CARTESIAN_POINT('Ctrl Pts',(1.57368729988192,-1.231036302203,94.7858046002336));
#10392=CARTESIAN_POINT('Ctrl Pts',(1.70283212427025,-1.04504177996186,94.8015971935676));
#10393=CARTESIAN_POINT('Ctrl Pts',(1.75919253802137,-0.947098086779131,
94.809505951235));
#10394=CARTESIAN_POINT('Ctrl Pts',(1.8171125464336,-0.823226867615654,94.8186664337049));
#10395=CARTESIAN_POINT('Ctrl Pts',(1.82686038939481,-0.80136241604765,94.8202528170724));
#10396=CARTESIAN_POINT('Ctrl Pts',(1.84176701244387,-0.766240132792765,
94.8227468897498));
#10397=CARTESIAN_POINT('Ctrl Pts',(1.84718138185248,-0.753094047832167,
94.8236684952487));
#10398=CARTESIAN_POINT('Ctrl Pts',(1.85777771673606,-0.7265641374833,94.8255029093264));
#10399=CARTESIAN_POINT('Ctrl Pts',(1.86295671400261,-0.713180063514287,
94.8264155245002));
#10400=CARTESIAN_POINT('Ctrl Pts',(1.87661821622744,-0.676710038575338,
94.8288706521999));
#10401=CARTESIAN_POINT('Ctrl Pts',(1.88481922127824,-0.653520494951424,
94.8303976536703));
#10402=CARTESIAN_POINT('Ctrl Pts',(1.91886223526572,-0.551281377037774,
94.8370060744766));
#10403=CARTESIAN_POINT('Ctrl Pts',(1.94017753753412,-0.4708049017683,94.8418885866826));
#10404=CARTESIAN_POINT('Ctrl Pts',(1.98661843337307,-0.23737400045742,94.8557373631577));
#10405=CARTESIAN_POINT('Ctrl Pts',(1.99904556621664,-0.0825358998770869,
94.8645917287909));
#10406=CARTESIAN_POINT('Ctrl Pts',(1.99220624355518,0.106355378428988,94.8761168360027));
#10407=CARTESIAN_POINT('Ctrl Pts',(1.99009008337187,0.140493513254606,94.8782262017423));
#10408=CARTESIAN_POINT('Ctrl Pts',(1.98502402816594,0.198163141345853,94.8818435629053));
#10409=CARTESIAN_POINT('Ctrl Pts',(1.98253014310789,0.221727707678418,94.883336976731));
#10410=CARTESIAN_POINT('Ctrl Pts',(1.9765460726311,0.270031809412018,94.8864324457461));
#10411=CARTESIAN_POINT('Ctrl Pts',(1.97300969222284,0.294761285302761,94.8880357205874));
#10412=CARTESIAN_POINT('Ctrl Pts',(1.96258719464009,0.359009607645426,94.8922521687871));
#10413=CARTESIAN_POINT('Ctrl Pts',(1.9549720846786,0.398396987146023,94.8948879233356));
#10414=CARTESIAN_POINT('Ctrl Pts',(1.92244444056224,0.543084443519314,94.9047643240906));
#10415=CARTESIAN_POINT('Ctrl Pts',(1.89016782667402,0.646524069356427,94.9122226308457));
#10416=CARTESIAN_POINT('Ctrl Pts',(1.80494395005695,0.857599197321721,94.928088048193));
#10417=CARTESIAN_POINT('Ctrl Pts',(1.75035397216493,0.964138895694782,94.9364821087725));
#10418=CARTESIAN_POINT('Ctrl Pts',(1.67398858491842,1.08505462977537,94.9460560530447));
#10419=CARTESIAN_POINT('Ctrl Pts',(1.66107100996395,1.10472826914306,94.9476147835699));
#10420=CARTESIAN_POINT('Ctrl Pts',(1.63984152028889,1.13584644927539,94.950076173487));
#10421=CARTESIAN_POINT('Ctrl Pts',(1.63175114562176,1.14743871419964,94.9509921626206));
#10422=CARTESIAN_POINT('Ctrl Pts',(1.61514803684204,1.17069761510358,94.9528265059667));
#10423=CARTESIAN_POINT('Ctrl Pts',(1.60663052750775,1.18235970248587,94.9537444850996));
#10424=CARTESIAN_POINT('Ctrl Pts',(1.58300058105899,1.21398666885885,94.9562322375093));
#10425=CARTESIAN_POINT('Ctrl Pts',(1.5676372191505,1.23376179049795,94.9577857885204));
#10426=CARTESIAN_POINT('Ctrl Pts',(1.49718196231678,1.32100729039596,94.964657468642));
#10427=CARTESIAN_POINT('Ctrl Pts',(1.43807383832485,1.3851211928176,94.9697579947416));
#10428=CARTESIAN_POINT('Ctrl Pts',(1.26772136879738,1.54719722538085,94.9834249292052));
#10429=CARTESIAN_POINT('Ctrl Pts',(1.14947278465562,1.63696215773694,94.9919113685094));
#10430=CARTESIAN_POINT('Ctrl Pts',(0.992228677138516,1.73082159466148,95.0030618471947));
#10431=CARTESIAN_POINT('Ctrl Pts',(0.961601768133306,1.74802258200071,95.0052255674762));
#10432=CARTESIAN_POINT('Ctrl Pts',(0.909446087625864,1.77552921420515,95.008906900898));
#10433=CARTESIAN_POINT('Ctrl Pts',(0.888157049798099,1.78627353785805,95.0104086110769));
#10434=CARTESIAN_POINT('Ctrl Pts',(0.844395305354261,1.80738384643756,95.0134963594836));
#10435=CARTESIAN_POINT('Ctrl Pts',(0.82191214831249,1.81771838545395,95.0150831696287));
#10436=CARTESIAN_POINT('Ctrl Pts',(0.763670283496213,1.84318819218763,95.0191974678284));
#10437=CARTESIAN_POINT('Ctrl Pts',(0.727652804076258,1.85770182253066,95.0217454889645));
#10438=CARTESIAN_POINT('Ctrl Pts',(0.646634499047044,1.8876313827665,95.0274882628434));
#10439=CARTESIAN_POINT('Ctrl Pts',(0.601460371254185,1.9025071017558,95.0306979817946));
#10440=CARTESIAN_POINT('Ctrl Pts',(0.438258094034412,1.94985552764731,95.0423076705302));
#10441=CARTESIAN_POINT('Ctrl Pts',(0.31783104822713,1.97306522650949,95.0509192155384));
#10442=CARTESIAN_POINT('Ctrl Pts',(0.184560515937871,1.9862271427577,95.0602094352488));
#10443=CARTESIAN_POINT('Ctrl Pts',(0.173061783772749,1.98726205392293,95.061008880912));
#10444=CARTESIAN_POINT('Ctrl Pts',(0.104965202839168,1.99279536662306,95.0657287028701));
#10445=CARTESIAN_POINT('Ctrl Pts',(0.0482001199276148,1.99497592331722,
95.0696043153805));
#10446=CARTESIAN_POINT('Ctrl Pts',(-0.0281025192915678,1.99464752442088,
95.0746734183335));
#10447=CARTESIAN_POINT('Ctrl Pts',(-0.0476185473319972,1.99427707268691,
95.0759575354909));
#10448=CARTESIAN_POINT('Ctrl Pts',(-0.0805583133211505,1.99316796301811,
95.0781004659385));
#10449=CARTESIAN_POINT('Ctrl Pts',(-0.0939852496088416,1.99257998218247,
95.0789670061351));
#10450=CARTESIAN_POINT('Ctrl Pts',(-0.123255387817326,1.9910016559093,95.0808400429614));
#10451=CARTESIAN_POINT('Ctrl Pts',(-0.139094273582351,1.98995786570135,
95.0818436976671));
#10452=CARTESIAN_POINT('Ctrl Pts',(-0.187370481802562,1.98619719890168,
95.0848771788734));
#10453=CARTESIAN_POINT('Ctrl Pts',(-0.219756705741729,1.98287525378018,
95.0868768824646));
#10454=CARTESIAN_POINT('Ctrl Pts',(-0.298986281507957,1.97278321373854,
95.0917137533449));
#10455=CARTESIAN_POINT('Ctrl Pts',(-0.345698646081356,1.96513596588499,
95.0945179806292));
#10456=CARTESIAN_POINT('Ctrl Pts',(-0.550676055505781,1.92404297133538,
95.1067796885204));
#10457=CARTESIAN_POINT('Ctrl Pts',(-0.704792316380372,1.87308655043888,
95.1159372905321));
#10458=CARTESIAN_POINT('Ctrl Pts',(-0.889040091783791,1.78616856279797,
95.1282301844786));
#10459=CARTESIAN_POINT('Ctrl Pts',(-0.926435920998179,1.76706155101298,
95.1307972231268));
#10460=CARTESIAN_POINT('Ctrl Pts',(-0.9853778621583,1.73456031524067,95.1349784261133));
#10461=CARTESIAN_POINT('Ctrl Pts',(-1.00732074902634,1.72190993750723,95.1365661299273));
#10462=CARTESIAN_POINT('Ctrl Pts',(-1.04939238985302,1.69657564603989,95.1396746518579));
#10463=CARTESIAN_POINT('Ctrl Pts',(-1.06954685533006,1.68394262186445,95.1411934068288));
#10464=CARTESIAN_POINT('Ctrl Pts',(-1.11733484843794,1.65278459955141,95.1448687162549));
#10465=CARTESIAN_POINT('Ctrl Pts',(-1.14473946256447,1.63392332654914,95.1470376584428));
#10466=CARTESIAN_POINT('Ctrl Pts',(-1.26955969096458,1.54333370795849,95.1572116389215));
#10467=CARTESIAN_POINT('Ctrl Pts',(-1.36077988903793,1.46353355744171,95.1655256470115));
#10468=CARTESIAN_POINT('Ctrl Pts',(-1.5267316245529,1.28935386566257,95.182289761695));
#10469=CARTESIAN_POINT('Ctrl Pts',(-1.60130511782977,1.19547757932092,95.1907000296954));
#10470=CARTESIAN_POINT('Ctrl Pts',(-1.66701720893993,1.09548217128264,95.1987207124569));
#10471=CARTESIAN_POINT('Origin',(0.,0.,89.2710285354474));
#10472=CARTESIAN_POINT('',(-1.66701720827332,1.09548217229703,96.1569262941178));
#10473=CARTESIAN_POINT('',(-1.66701720851842,1.09548217192407,95.9972028497351));
#10474=CARTESIAN_POINT('',(-1.66701720851066,1.09548217193587,89.2710285354474));
#10475=CARTESIAN_POINT('',(-1.99474928355678,-0.00169063588936904,95.428322530593));
#10476=CARTESIAN_POINT('Ctrl Pts',(-1.66701720827332,1.09548217229703,96.1569262941178));
#10477=CARTESIAN_POINT('Ctrl Pts',(-1.65718555120821,1.11044320217762,96.155810481867));
#10478=CARTESIAN_POINT('Ctrl Pts',(-1.64715299206609,1.12527110996234,96.1546873293238));
#10479=CARTESIAN_POINT('Ctrl Pts',(-1.62356010618087,1.15914918914147,96.1520796164126));
#10480=CARTESIAN_POINT('Ctrl Pts',(-1.60986214623897,1.17809933957545,96.1505898928457));
#10481=CARTESIAN_POINT('Ctrl Pts',(-1.57753446881027,1.22120551531339,96.1471263981644));
#10482=CARTESIAN_POINT('Ctrl Pts',(-1.55867783592543,1.24518317611485,96.1451438338539));
#10483=CARTESIAN_POINT('Ctrl Pts',(-1.4921193017721,1.32593571544113,96.1382672384479));
#10484=CARTESIAN_POINT('Ctrl Pts',(-1.44181061195347,1.38047292060104,96.1332697996111));
#10485=CARTESIAN_POINT('Ctrl Pts',(-1.38203403040671,1.43843416697403,96.1275555004801));
#10486=CARTESIAN_POINT('Ctrl Pts',(-1.37543610621948,1.44474441636437,96.1269276819358));
#10487=CARTESIAN_POINT('Ctrl Pts',(-1.28157730318415,1.53328519495493,96.1180383372285));
#10488=CARTESIAN_POINT('Ctrl Pts',(-1.1871238639983,1.60752573190601,96.1095775453159));
#10489=CARTESIAN_POINT('Ctrl Pts',(-1.04037214602199,1.70284738486894,96.0974967694941));
#10490=CARTESIAN_POINT('Ctrl Pts',(-0.992937490984979,1.73093605376192,
96.0937401661729));
#10491=CARTESIAN_POINT('Ctrl Pts',(-0.927753039315384,1.76597250905472,
96.0888288798244));
#10492=CARTESIAN_POINT('Ctrl Pts',(-0.910982307948996,1.77468191635101,
96.0875868367289));
#10493=CARTESIAN_POINT('Ctrl Pts',(-0.882177375235394,1.78912498667104,
96.0854932014088));
#10494=CARTESIAN_POINT('Ctrl Pts',(-0.870205448786078,1.79497845475207,
96.0846346607371));
#10495=CARTESIAN_POINT('Ctrl Pts',(-0.843600057448697,1.80765792400793,
96.0827527240333));
#10496=CARTESIAN_POINT('Ctrl Pts',(-0.828941076879176,1.81442689569141,
96.0817326583937));
#10497=CARTESIAN_POINT('Ctrl Pts',(-0.783067525646691,1.83493756667492,
96.078587656144));
#10498=CARTESIAN_POINT('Ctrl Pts',(-0.751580153335586,1.84805795459866,
96.0764961673729));
#10499=CARTESIAN_POINT('Ctrl Pts',(-0.672463065625395,1.87866812138816,
96.0713694873987));
#10500=CARTESIAN_POINT('Ctrl Pts',(-0.624472549307504,1.89516097391315,
96.0683726624658));
#10501=CARTESIAN_POINT('Ctrl Pts',(-0.410838420465918,1.95958240964507,
96.0553176215227));
#10502=CARTESIAN_POINT('Ctrl Pts',(-0.240030758218407,1.98774617780153,
96.045548388951));
#10503=CARTESIAN_POINT('Ctrl Pts',(-0.0337182590463221,1.99475530458375,
96.0329572928333));
#10504=CARTESIAN_POINT('Ctrl Pts',(0.000315049989103523,1.99504018350141,
96.0308577792975));
#10505=CARTESIAN_POINT('Ctrl Pts',(0.0580354930702617,1.99404644006744,
96.0272498697896));
#10506=CARTESIAN_POINT('Ctrl Pts',(0.0817234549550927,1.99321612531343,
96.0257557667319));
#10507=CARTESIAN_POINT('Ctrl Pts',(0.130450312191673,1.99063810011081,96.022651994938));
#10508=CARTESIAN_POINT('Ctrl Pts',(0.155482164603916,1.98883949339408,96.0210409808045));
#10509=CARTESIAN_POINT('Ctrl Pts',(0.220879619033977,1.98289837510018,96.0167860760089));
#10510=CARTESIAN_POINT('Ctrl Pts',(0.261162682853044,1.97799581126181,96.0141189298242));
#10511=CARTESIAN_POINT('Ctrl Pts',(0.404687675438619,1.95606778243425,96.0044453799975));
#10512=CARTESIAN_POINT('Ctrl Pts',(0.506693356665096,1.93215685501721,95.9972403429969));
#10513=CARTESIAN_POINT('Ctrl Pts',(0.722599765512278,1.86326836870318,95.9814565039718));
#10514=CARTESIAN_POINT('Ctrl Pts',(0.835215392179229,1.81558214297996,95.9728788030905));
#10515=CARTESIAN_POINT('Ctrl Pts',(0.9632559709393,1.74691321743989,95.9631589077026));
#10516=CARTESIAN_POINT('Ctrl Pts',(0.983547713442134,1.73556960758609,95.9616201818055));
#10517=CARTESIAN_POINT('Ctrl Pts',(1.01582550046536,1.7167775079078,95.9591807824589));
#10518=CARTESIAN_POINT('Ctrl Pts',(1.02793842142351,1.7095523093668,95.9582672578376));
#10519=CARTESIAN_POINT('Ctrl Pts',(1.05239437531223,1.69461071663575,95.9564283527891));
#10520=CARTESIAN_POINT('Ctrl Pts',(1.06473152646805,1.6868865434114,95.9555035117789));
#10521=CARTESIAN_POINT('Ctrl Pts',(1.09848804373676,1.66523400559506,95.9529776110545));
#10522=CARTESIAN_POINT('Ctrl Pts',(1.11972679971511,1.65102765322497,95.9513935735834));
#10523=CARTESIAN_POINT('Ctrl Pts',(1.16816686839282,1.61726179827986,95.9477784856478));
#10524=CARTESIAN_POINT('Ctrl Pts',(1.19516046813669,1.59741705369019,95.9457621795953));
#10525=CARTESIAN_POINT('Ctrl Pts',(1.2935353372021,1.52120494122501,95.9383561048706));
#10526=CARTESIAN_POINT('Ctrl Pts',(1.36153853727005,1.46065487294374,95.9331154899632));
#10527=CARTESIAN_POINT('Ctrl Pts',(1.49906087726493,1.32022552824929,95.9217098969715));
#10528=CARTESIAN_POINT('Ctrl Pts',(1.56683185762389,1.23903749061577,95.9155455065653));
#10529=CARTESIAN_POINT('Ctrl Pts',(1.64924950321509,1.12266373824548,95.9068854237849));
#10530=CARTESIAN_POINT('Ctrl Pts',(1.66979722993901,1.09186754478085,95.9046100654212));
#10531=CARTESIAN_POINT('Ctrl Pts',(1.70246339748899,1.03982822558492,95.9007798802223));
#10532=CARTESIAN_POINT('Ctrl Pts',(1.71506973619169,1.01890140506983,95.8992434705017));
#10533=CARTESIAN_POINT('Ctrl Pts',(1.73950888353016,0.976592721752463,95.8961418698856));
#10534=CARTESIAN_POINT('Ctrl Pts',(1.75133941670121,0.955214457279873,95.8945769432028));
#10535=CARTESIAN_POINT('Ctrl Pts',(1.78010632376555,0.900899770357549,95.8906041722798));
#10536=CARTESIAN_POINT('Ctrl Pts',(1.79652305659613,0.867700134478513,95.8881785693077));
#10537=CARTESIAN_POINT('Ctrl Pts',(1.85606519862452,0.738344823156949,95.8787326821863));
#10538=CARTESIAN_POINT('Ctrl Pts',(1.89246530539454,0.639297071433817,95.8714983211058));
#10539=CARTESIAN_POINT('Ctrl Pts',(1.95617953598975,0.411749413906618,95.8550521539249));
#10540=CARTESIAN_POINT('Ctrl Pts',(1.97898718761388,0.282470764603638,95.8458199947951));
#10541=CARTESIAN_POINT('Ctrl Pts',(1.99065701722765,0.129650966286144,95.8355816179709));
#10542=CARTESIAN_POINT('Ctrl Pts',(1.99198196647591,0.107390313759802,95.83410745844));
#10543=CARTESIAN_POINT('Ctrl Pts',(1.9934680891285,0.0725917276628886,95.8318346279011));
#10544=CARTESIAN_POINT('Ctrl Pts',(1.99388478295424,0.0600672482854625,
95.8310229961583));
#10545=CARTESIAN_POINT('Ctrl Pts',(1.99452376804397,0.0332630174499008,
95.8293008450244));
#10546=CARTESIAN_POINT('Ctrl Pts',(1.99471079723741,0.0189830075776515,
95.8283923890133));
#10547=CARTESIAN_POINT('Ctrl Pts',(1.99480164228288,-0.019558881247296,
95.8259618387166));
#10548=CARTESIAN_POINT('Ctrl Pts',(1.99441622854976,-0.0438197796222868,
95.8244547415938));
#10549=CARTESIAN_POINT('Ctrl Pts',(1.99084652767614,-0.148368527168874,
95.8180355355985));
#10550=CARTESIAN_POINT('Ctrl Pts',(1.98325540178347,-0.228437354466921,
95.8133095507038));
#10551=CARTESIAN_POINT('Ctrl Pts',(1.94617349370064,-0.465845780593805,
95.7993160740881));
#10552=CARTESIAN_POINT('Ctrl Pts',(1.90258484034827,-0.620298912835385,
95.7901882687197));
#10553=CARTESIAN_POINT('Ctrl Pts',(1.82814183536849,-0.798777248527106,
95.778383870874));
#10554=CARTESIAN_POINT('Ctrl Pts',(1.81448350939313,-0.829335308167921,
95.7763177076403));
#10555=CARTESIAN_POINT('Ctrl Pts',(1.78980391512241,-0.881020102060512,
95.7727364949512));
#10556=CARTESIAN_POINT('Ctrl Pts',(1.77916077291047,-0.902319976130327,
95.7712347582729));
#10557=CARTESIAN_POINT('Ctrl Pts',(1.75645196863676,-0.945802005943015,
95.7681126166698));
#10558=CARTESIAN_POINT('Ctrl Pts',(1.74434132155344,-0.967955685412192,
95.7664908081088));
#10559=CARTESIAN_POINT('Ctrl Pts',(1.71117845658708,-1.02597517580799,95.7621574830059));
#10560=CARTESIAN_POINT('Ctrl Pts',(1.68942049399444,-1.06142109442833,95.7594209284971));
#10561=CARTESIAN_POINT('Ctrl Pts',(1.61290398940453,-1.17775481282689,95.7501309443903));
#10562=CARTESIAN_POINT('Ctrl Pts',(1.55332227062096,-1.25528939990836,95.7434123740196));
#10563=CARTESIAN_POINT('Ctrl Pts',(1.40219170503602,-1.42464572957135,95.7276101657699));
#10564=CARTESIAN_POINT('Ctrl Pts',(1.30688670246067,-1.51255023759461,95.7184951895744));
#10565=CARTESIAN_POINT('Ctrl Pts',(1.18582176102637,-1.60416927630132,95.708349622307));
#10566=CARTESIAN_POINT('Ctrl Pts',(1.16767811949116,-1.61742394823665,95.7068638345312));
#10567=CARTESIAN_POINT('Ctrl Pts',(1.1390529759052,-1.63760296665094,95.7045779821658));
#10568=CARTESIAN_POINT('Ctrl Pts',(1.12872404715159,-1.64473925122031,95.7037647002753));
#10569=CARTESIAN_POINT('Ctrl Pts',(1.10653584936109,-1.65976166244187,95.7020432894067));
#10570=CARTESIAN_POINT('Ctrl Pts',(1.09465802692806,-1.66761931947711,95.7011371574348));
#10571=CARTESIAN_POINT('Ctrl Pts',(1.06250457039156,-1.68839853153055,95.6987223567505));
#10572=CARTESIAN_POINT('Ctrl Pts',(1.04207716071228,-1.70108226589601,95.6972283281254));
#10573=CARTESIAN_POINT('Ctrl Pts',(0.932835099552581,-1.7662059267947,95.6894207061942));
#10574=CARTESIAN_POINT('Ctrl Pts',(0.840273193861112,-1.81207348534812,
95.6834267565779));
#10575=CARTESIAN_POINT('Ctrl Pts',(0.624109702688555,-1.89904563305184,
95.6699117573346));
#10576=CARTESIAN_POINT('Ctrl Pts',(0.499216766717564,-1.93563067270597,
95.662414772899));
#10577=CARTESIAN_POINT('Ctrl Pts',(0.335327690412879,-1.9667105531926,95.6522846342544));
#10578=CARTESIAN_POINT('Ctrl Pts',(0.298812915084599,-1.97258856171814,
95.6500115522083));
#10579=CARTESIAN_POINT('Ctrl Pts',(0.237951651615745,-1.98065716329069,
95.6461844374645));
#10580=CARTESIAN_POINT('Ctrl Pts',(0.213689767485512,-1.98342138364617,
95.6446487788926));
#10581=CARTESIAN_POINT('Ctrl Pts',(0.165065138562273,-1.98805881538828,
95.6415481479632));
#10582=CARTESIAN_POINT('Ctrl Pts',(0.140706578795773,-1.98993113547655,
95.6399834294939));
#10583=CARTESIAN_POINT('Ctrl Pts',(0.0793384714745956,-1.99351581817488,
95.6360100296403));
#10584=CARTESIAN_POINT('Ctrl Pts',(0.0423055125903197,-1.9946452942262,
95.6335835610386));
#10585=CARTESIAN_POINT('Ctrl Pts',(-0.100292991783385,-1.99502164075874,
95.6241245703117));
#10586=CARTESIAN_POINT('Ctrl Pts',(-0.205692103694485,-1.98692107220505,
95.6168771600717));
#10587=CARTESIAN_POINT('Ctrl Pts',(-0.438786193166679,-1.95025783748678,
95.6004550758324));
#10588=CARTESIAN_POINT('Ctrl Pts',(-0.565338239443567,-1.91740336876445,
95.5912619438001));
#10589=CARTESIAN_POINT('Ctrl Pts',(-0.70875251942594,-1.86472424447827,
95.5810553193265));
#10590=CARTESIAN_POINT('Ctrl Pts',(-0.729592858535322,-1.85666933080406,
95.5795782814347));
#10591=CARTESIAN_POINT('Ctrl Pts',(-0.761913460968846,-1.84354893822585,
95.5773020214592));
#10592=CARTESIAN_POINT('Ctrl Pts',(-0.773488073689845,-1.83872266267815,
95.5764897838792));
#10593=CARTESIAN_POINT('Ctrl Pts',(-0.798145916596024,-1.82816701133072,
95.574766936133));
#10594=CARTESIAN_POINT('Ctrl Pts',(-0.811214793022019,-1.82240558457939,
95.5738583794762));
#10595=CARTESIAN_POINT('Ctrl Pts',(-0.846294315449824,-1.80648859104071,
95.5714290414359));
#10596=CARTESIAN_POINT('Ctrl Pts',(-0.868184277564329,-1.79607106809063,
95.5699232070324));
#10597=CARTESIAN_POINT('Ctrl Pts',(-0.96158028868379,-1.74951683809526,
95.5635191710709));
#10598=CARTESIAN_POINT('Ctrl Pts',(-1.03106959325041,-1.70948641136204,
95.5588058907052));
#10599=CARTESIAN_POINT('Ctrl Pts',(-1.23182815515036,-1.57712837923862,
95.544800178572));
#10600=CARTESIAN_POINT('Ctrl Pts',(-1.35454787343886,-1.47306851679111,
95.5356497288283));
#10601=CARTESIAN_POINT('Ctrl Pts',(-1.48619548145103,-1.33092723532978,
95.5238218625293));
#10602=CARTESIAN_POINT('Ctrl Pts',(-1.50828230089145,-1.30584402316266,
95.5217585561656));
#10603=CARTESIAN_POINT('Ctrl Pts',(-1.54501198392521,-1.26195589485126,
95.5181798524091));
#10604=CARTESIAN_POINT('Ctrl Pts',(-1.55996738582723,-1.24342124259173,
95.5166776770877));
#10605=CARTESIAN_POINT('Ctrl Pts',(-1.5901123428049,-1.20466170759963,95.5135522762242));
#10606=CARTESIAN_POINT('Ctrl Pts',(-1.60525616557102,-1.1844068715559,95.5119276036378));
#10607=CARTESIAN_POINT('Ctrl Pts',(-1.64437077414544,-1.12996260534527,
95.5075802533079));
#10608=CARTESIAN_POINT('Ctrl Pts',(-1.66765905954146,-1.09530067211596,
95.5048322861038));
#10609=CARTESIAN_POINT('Ctrl Pts',(-1.74232462677389,-0.976262348631661,
95.4954556278635));
#10610=CARTESIAN_POINT('Ctrl Pts',(-1.78851463349696,-0.88881631802061,
95.4886576921736));
#10611=CARTESIAN_POINT('Ctrl Pts',(-1.87821173646035,-0.683423136798174,
95.4730516775108));
#10612=CARTESIAN_POINT('Ctrl Pts',(-1.91744688388269,-0.564045799662935,
95.4642237314289));
#10613=CARTESIAN_POINT('Ctrl Pts',(-1.95048069896177,-0.418590018862053,
95.4542342277323));
#10614=CARTESIAN_POINT('Ctrl Pts',(-1.95533043058807,-0.395317072854785,
95.4526592277267));
#10615=CARTESIAN_POINT('Ctrl Pts',(-1.96240840658594,-0.358025186918168,
95.4501784518105));
#10616=CARTESIAN_POINT('Ctrl Pts',(-1.96490494315641,-0.344060150975849,
95.4492590037126));
#10617=CARTESIAN_POINT('Ctrl Pts',(-1.96963377948949,-0.315875703541852,
95.447424185483));
#10618=CARTESIAN_POINT('Ctrl Pts',(-1.97186158370587,-0.301656445141128,
95.4465090857984));
#10619=CARTESIAN_POINT('Ctrl Pts',(-1.97614996123957,-0.272204204994292,
95.4446331605963));
#10620=CARTESIAN_POINT('Ctrl Pts',(-1.97818875876497,-0.256968998038571,
95.4436735154417));
#10621=CARTESIAN_POINT('Ctrl Pts',(-1.98346971106087,-0.213708464554809,
95.4409751280481));
#10622=CARTESIAN_POINT('Ctrl Pts',(-1.98629384811802,-0.185634892351318,
95.4392554960969));
#10623=CARTESIAN_POINT('Ctrl Pts',(-1.99262757669528,-0.105672998812069,
95.4344229864603));
#10624=CARTESIAN_POINT('Ctrl Pts',(-1.99470520880076,-0.0536936062182133,
95.4313594480369));
#10625=CARTESIAN_POINT('Ctrl Pts',(-1.99474928355678,-0.00169063588936904,
95.428322530593));
#10626=CARTESIAN_POINT('Ctrl Pts',(-1.99474928174581,-0.00169277126666055,
95.4283226552967));
#10627=CARTESIAN_POINT('Ctrl Pts',(-1.99487747865361,0.149373527398597,
95.4195005439435));
#10628=CARTESIAN_POINT('Ctrl Pts',(-1.9778456373477,0.299964032517438,95.4109013801887));
#10629=CARTESIAN_POINT('Ctrl Pts',(-1.93456535897058,0.488105111933841,
95.399251979848));
#10630=CARTESIAN_POINT('Ctrl Pts',(-1.92386597454785,0.528705080201953,
95.3966854295853));
#10631=CARTESIAN_POINT('Ctrl Pts',(-1.90467016788025,0.593212163409328,
95.3925045977965));
#10632=CARTESIAN_POINT('Ctrl Pts',(-1.89698447461586,0.617348303740286,
95.3909167606056));
#10633=CARTESIAN_POINT('Ctrl Pts',(-1.88119219618946,0.663859583565867,
95.3878076720259));
#10634=CARTESIAN_POINT('Ctrl Pts',(-1.87314065820016,0.686248948327138,
95.3862884790016));
#10635=CARTESIAN_POINT('Ctrl Pts',(-1.85286969062847,0.7396007044466,95.3826115369586));
#10636=CARTESIAN_POINT('Ctrl Pts',(-1.84027232339096,0.770410829364629,
95.3804413789972));
#10637=CARTESIAN_POINT('Ctrl Pts',(-1.78193221943771,0.903490492294931,
95.3708557820111));
#10638=CARTESIAN_POINT('Ctrl Pts',(-1.72842993999459,1.00202919778739,95.3631863110547));
#10639=CARTESIAN_POINT('Ctrl Pts',(-1.66701714412024,1.09548226992006,95.3554060137221));
#10640=CARTESIAN_POINT('',(-1.99474996431002,-0.000377339601584004,95.2691777234731));
#10641=CARTESIAN_POINT('Ctrl Pts',(-1.66701720893993,1.09548217128264,95.1987207124569));
#10642=CARTESIAN_POINT('Ctrl Pts',(-1.66802828759705,1.09394359259538,95.1988441226394));
#10643=CARTESIAN_POINT('Ctrl Pts',(-1.66903726848786,1.09240356500824,95.1989674367045));
#10644=CARTESIAN_POINT('Ctrl Pts',(-1.68280203943216,1.07133052990688,95.2006518868572));
#10645=CARTESIAN_POINT('Ctrl Pts',(-1.69521699123801,1.05157561539804,95.2021966907627));
#10646=CARTESIAN_POINT('Ctrl Pts',(-1.71457241109769,1.01954287441436,95.2046416413902));
#10647=CARTESIAN_POINT('Ctrl Pts',(-1.72173395913149,1.00740182503062,95.2055548244644));
#10648=CARTESIAN_POINT('Ctrl Pts',(-1.73599476179255,0.982628952685094,
95.20738930547));
#10649=CARTESIAN_POINT('Ctrl Pts',(-1.74308623460031,0.969993753431862,
95.2083101336997));
#10650=CARTESIAN_POINT('Ctrl Pts',(-1.76216931572772,0.935107323861602,
95.210815275299));
#10651=CARTESIAN_POINT('Ctrl Pts',(-1.77387706730868,0.91270295973959,95.2123829817895));
#10652=CARTESIAN_POINT('Ctrl Pts',(-1.82499346896941,0.81018332385509,95.2193996423362));
#10653=CARTESIAN_POINT('Ctrl Pts',(-1.85942576560974,0.72769304324409,95.2246203371528));
#10654=CARTESIAN_POINT('Ctrl Pts',(-1.93427802862944,0.507940526652045,
95.2381069057587));
#10655=CARTESIAN_POINT('Ctrl Pts',(-1.96567577102525,0.368171235952138,
95.2463088270924));
#10656=CARTESIAN_POINT('Ctrl Pts',(-1.98591952037962,0.190843582955943,
95.2571576814379));
#10657=CARTESIAN_POINT('Ctrl Pts',(-1.98901186887296,0.155335634415854,
95.2593495024733));
#10658=CARTESIAN_POINT('Ctrl Pts',(-1.99250218417579,0.0973076913499925,
95.2629734686202));
#10659=CARTESIAN_POINT('Ctrl Pts',(-1.9934729078245,0.0748294058175734,
95.2643874976281));
#10660=CARTESIAN_POINT('Ctrl Pts',(-1.99452436434611,0.0347709085144968,
95.2669276932659));
#10661=CARTESIAN_POINT('Ctrl Pts',(-1.99475328875839,0.0171968647529458,
95.2680490325194));
#10662=CARTESIAN_POINT('Ctrl Pts',(-1.99474996431002,-0.000377339601584004,
95.2691777234731));
#10663=CARTESIAN_POINT('Ctrl Pts',(-1.66701720851842,1.09548217192407,95.9972028497351));
#10664=CARTESIAN_POINT('Ctrl Pts',(-1.6668804849266,1.09569022695793,95.9971884173542));
#10665=CARTESIAN_POINT('Ctrl Pts',(-1.66674372178711,1.09589825730506,95.9971739849087));
#10666=CARTESIAN_POINT('Ctrl Pts',(-1.60429633353987,1.19084822050707,95.9905858626106));
#10667=CARTESIAN_POINT('Ctrl Pts',(-1.53402745914654,1.2800937819193,95.9840334802001));
#10668=CARTESIAN_POINT('Ctrl Pts',(-1.44022506551533,1.38034473607148,95.9756036167107));
#10669=CARTESIAN_POINT('Ctrl Pts',(-1.42356866007336,1.39751636144373,95.974116948274));
#10670=CARTESIAN_POINT('Ctrl Pts',(-1.39653426673596,1.42440214384986,95.9717117554366));
#10671=CARTESIAN_POINT('Ctrl Pts',(-1.38635372287017,1.43431264182164,95.9708076996927));
#10672=CARTESIAN_POINT('Ctrl Pts',(-1.36567984616665,1.45401239274738,95.9689729904776));
#10673=CARTESIAN_POINT('Ctrl Pts',(-1.3551850454292,1.46379880526544,95.9680422534304));
#10674=CARTESIAN_POINT('Ctrl Pts',(-1.32642392666607,1.49004418302365,95.9654955061654));
#10675=CARTESIAN_POINT('Ctrl Pts',(-1.30795796645712,1.50627949837785,95.9638646203654));
#10676=CARTESIAN_POINT('Ctrl Pts',(-1.22578862674561,1.57587266525385,95.9566435479395));
#10677=CARTESIAN_POINT('Ctrl Pts',(-1.15909077817714,1.6255579711623,95.9508778893337));
#10678=CARTESIAN_POINT('Ctrl Pts',(-0.959697853330762,1.75556762473521,
95.9342790910101));
#10679=CARTESIAN_POINT('Ctrl Pts',(-0.820455885106113,1.82480295950729,
95.9234773012427));
#10680=CARTESIAN_POINT('Ctrl Pts',(-0.642417649259808,1.88878147799821,
95.9109795939836));
#10681=CARTESIAN_POINT('Ctrl Pts',(-0.609957156241353,1.89951267845743,
95.9087480327944));
#10682=CARTESIAN_POINT('Ctrl Pts',(-0.554553930603341,1.91626171340789,
95.9050159099953));
#10683=CARTESIAN_POINT('Ctrl Pts',(-0.53175156304769,1.92271406395186,95.9035014232127));
#10684=CARTESIAN_POINT('Ctrl Pts',(-0.484675213996757,1.93513359119853,
95.9004167556999));
#10685=CARTESIAN_POINT('Ctrl Pts',(-0.460393142552787,1.94105392090838,
95.8988483331189));
#10686=CARTESIAN_POINT('Ctrl Pts',(-0.396823108916739,1.95529313799269,
95.894796715629));
#10687=CARTESIAN_POINT('Ctrl Pts',(-0.357383000908921,1.96288500973171,
95.892336901338));
#10688=CARTESIAN_POINT('Ctrl Pts',(-0.204445405882167,1.98756109035315,
95.8829680732485));
#10689=CARTESIAN_POINT('Ctrl Pts',(-0.089783335550865,1.99603079495289,
95.8763155700666));
#10690=CARTESIAN_POINT('Ctrl Pts',(0.136881162197166,1.99319221518432,95.8631720438534));
#10691=CARTESIAN_POINT('Ctrl Pts',(0.248454710518279,1.98237641249894,95.8566996018982));
#10692=CARTESIAN_POINT('Ctrl Pts',(0.382100773166669,1.95795843928683,95.8483579931264));
#10693=CARTESIAN_POINT('Ctrl Pts',(0.40560224615661,1.9532252683376,95.8468682222481));
#10694=CARTESIAN_POINT('Ctrl Pts',(0.442905949010768,1.94501010341849,95.8444586424363));
#10695=CARTESIAN_POINT('Ctrl Pts',(0.456766826120236,1.94180174614435,95.8435533564393));
#10696=CARTESIAN_POINT('Ctrl Pts',(0.484535045439318,1.93506052268165,95.8417175132417));
#10697=CARTESIAN_POINT('Ctrl Pts',(0.498440916820015,1.93152531909679,95.840786887517));
#10698=CARTESIAN_POINT('Ctrl Pts',(0.536059543298598,1.92152849524061,95.8382409518977));
#10699=CARTESIAN_POINT('Ctrl Pts',(0.559692227728055,1.91477833469492,95.8366107833347));
#10700=CARTESIAN_POINT('Ctrl Pts',(0.662568301886348,1.88332688303307,95.8293968235987));
#10701=CARTESIAN_POINT('Ctrl Pts',(0.740345460910375,1.85413139794827,95.8236379340896));
#10702=CARTESIAN_POINT('Ctrl Pts',(0.957588248540831,1.75673137430935,95.8070363844033));
#10703=CARTESIAN_POINT('Ctrl Pts',(1.09124951906365,1.67698269264066,95.7962246606123));
#10704=CARTESIAN_POINT('Ctrl Pts',(1.24142742211929,1.56174646183854,95.7837200819162));
#10705=CARTESIAN_POINT('Ctrl Pts',(1.26798635304312,1.54026131022483,95.7814903549566));
#10706=CARTESIAN_POINT('Ctrl Pts',(1.31200921584522,1.50273766044407,95.7777605469953));
#10707=CARTESIAN_POINT('Ctrl Pts',(1.32976202831772,1.48705133968567,95.7762465732006));
#10708=CARTESIAN_POINT('Ctrl Pts',(1.36566198371057,1.45417312316325,95.77316238363));
#10709=CARTESIAN_POINT('Ctrl Pts',(1.38377389160839,1.43694886253776,95.7715939357578));
#10710=CARTESIAN_POINT('Ctrl Pts',(1.43014409775887,1.3911611513272,95.7675410770411));
#10711=CARTESIAN_POINT('Ctrl Pts',(1.45787227569515,1.36207571491972,95.7650800899108));
#10712=CARTESIAN_POINT('Ctrl Pts',(1.59088092058869,1.21383758313938,95.7530358693994));
#10713=CARTESIAN_POINT('Ctrl Pts',(1.68252649186866,1.08324029997221,95.744010236509));
#10714=CARTESIAN_POINT('Ctrl Pts',(1.79279399776592,0.877739634866055,95.7303674974415));
#10715=CARTESIAN_POINT('Ctrl Pts',(1.82420794422698,0.810432182841149,95.7259661528869));
#10716=CARTESIAN_POINT('Ctrl Pts',(1.85949243853509,0.722318552123517,95.7200990614011));
#10717=CARTESIAN_POINT('Ctrl Pts',(1.86688899986503,0.702980512553152,95.7188050892396));
#10718=CARTESIAN_POINT('Ctrl Pts',(1.87860176379632,0.670868590711476,95.7166404547415));
#10719=CARTESIAN_POINT('Ctrl Pts',(1.88309205089432,0.658159230235376,95.7157796159247));
#10720=CARTESIAN_POINT('Ctrl Pts',(1.89238911763242,0.630970457586125,95.7139276723563));
#10721=CARTESIAN_POINT('Ctrl Pts',(1.89715909993132,0.616480011172265,95.712934715081));
#10722=CARTESIAN_POINT('Ctrl Pts',(1.9105695639407,0.574110926068069,95.7100170163937));
#10723=CARTESIAN_POINT('Ctrl Pts',(1.91876460274693,0.54609669977558,95.7080699005966));
#10724=CARTESIAN_POINT('Ctrl Pts',(1.96162978023872,0.386663116313515,95.6969255419223));
#10725=CARTESIAN_POINT('Ctrl Pts',(1.98341032242802,0.252154077736425,95.6873117790037));
#10726=CARTESIAN_POINT('Ctrl Pts',(1.99707619038273,0.0185205112697676,
95.6710916348758));
#10727=CARTESIAN_POINT('Ctrl Pts',(1.9955708102381,-0.0797383823695557,
95.664407174551));
#10728=CARTESIAN_POINT('Ctrl Pts',(1.98394530854109,-0.209868232954295,
95.6557993807004));
#10729=CARTESIAN_POINT('Ctrl Pts',(1.98026285094011,-0.242162984086466,
95.6536824128717));
#10730=CARTESIAN_POINT('Ctrl Pts',(1.97253719478053,-0.297800008652776,
95.6500664284491));
#10731=CARTESIAN_POINT('Ctrl Pts',(1.96886450855976,-0.321186015878491,
95.6485560597808));
#10732=CARTESIAN_POINT('Ctrl Pts',(1.96035599414429,-0.369712087492614,
95.645439858646));
#10733=CARTESIAN_POINT('Ctrl Pts',(1.95545072718728,-0.394835664403702,
95.6438365433885));
#10734=CARTESIAN_POINT('Ctrl Pts',(1.94091771332892,-0.462335241306044,
95.6395511921536));
#10735=CARTESIAN_POINT('Ctrl Pts',(1.93038648945833,-0.504503579980473,
95.6368981879895));
#10736=CARTESIAN_POINT('Ctrl Pts',(1.89676002257848,-0.622593052559095,
95.629501754739));
#10737=CARTESIAN_POINT('Ctrl Pts',(1.8705012297357,-0.697529392975611,95.6248502118933));
#10738=CARTESIAN_POINT('Ctrl Pts',(1.78492443945544,-0.90182018466734,95.6119704544728));
#10739=CARTESIAN_POINT('Ctrl Pts',(1.71615061848828,-1.02667026181237,95.6038794510283));
#10740=CARTESIAN_POINT('Ctrl Pts',(1.62121697230445,-1.16242730818389,95.5937000511406));
#10741=CARTESIAN_POINT('Ctrl Pts',(1.60738681205321,-1.18147756659049,95.5922361474023));
#10742=CARTESIAN_POINT('Ctrl Pts',(1.58471715602143,-1.21156879558851,95.589858482816));
#10743=CARTESIAN_POINT('Ctrl Pts',(1.57609125577559,-1.22276888311434,95.5889585847402));
#10744=CARTESIAN_POINT('Ctrl Pts',(1.55841546156062,-1.24522179377426,95.5871220052268));
#10745=CARTESIAN_POINT('Ctrl Pts',(1.54936103552292,-1.25646982326632,95.586185073764));
#10746=CARTESIAN_POINT('Ctrl Pts',(1.5242786393232,-1.28694552053004,95.5836023242514));
#10747=CARTESIAN_POINT('Ctrl Pts',(1.50801009620147,-1.30597073284255,95.5819409575158));
#10748=CARTESIAN_POINT('Ctrl Pts',(1.4335927114004,-1.38975318888101,95.5744209048966));
#10749=CARTESIAN_POINT('Ctrl Pts',(1.37160457042969,-1.45096535589064,95.5683712483666));
#10750=CARTESIAN_POINT('Ctrl Pts',(1.19384786551966,-1.60489759793944,95.551966785172));
#10751=CARTESIAN_POINT('Ctrl Pts',(1.07139945953297,-1.68910811201298,95.5416575085761));
#10752=CARTESIAN_POINT('Ctrl Pts',(0.909785653747475,-1.77554210064671,
95.529533410311));
#10753=CARTESIAN_POINT('Ctrl Pts',(0.878399661951723,-1.79127719260074,
95.5272391271243));
#10754=CARTESIAN_POINT('Ctrl Pts',(0.825025261387033,-1.81629548886062,
95.5234350237021));
#10755=CARTESIAN_POINT('Ctrl Pts',(0.803257102718503,-1.82602686004232,
95.5219099663663));
#10756=CARTESIAN_POINT('Ctrl Pts',(0.758549468498303,-1.84505898753218,
95.5188291870527));
#10757=CARTESIAN_POINT('Ctrl Pts',(0.735600859048451,-1.85432775639869,
95.5172747705094));
#10758=CARTESIAN_POINT('Ctrl Pts',(0.676200430981533,-1.87704278709469,
95.5133160036981));
#10759=CARTESIAN_POINT('Ctrl Pts',(0.639516758065794,-1.88985588611785,
95.5109329363723));
#10760=CARTESIAN_POINT('Ctrl Pts',(0.557116277702242,-1.91596280864444,
95.5056968943315));
#10761=CARTESIAN_POINT('Ctrl Pts',(0.511250611400254,-1.92870818676769,
95.50286065405));
#10762=CARTESIAN_POINT('Ctrl Pts',(0.34568589476606,-1.96839407045617,95.4928223941057));
#10763=CARTESIAN_POINT('Ctrl Pts',(0.224022178038709,-1.98592222931546,
95.485829206451));
#10764=CARTESIAN_POINT('Ctrl Pts',(0.0353405790285169,-1.99553748330494,
95.4747343014208));
#10765=CARTESIAN_POINT('Ctrl Pts',(-0.0309608271509282,-1.99560981837558,
95.4707843446693));
#10766=CARTESIAN_POINT('Ctrl Pts',(-0.117408298304569,-1.99139518890504,
95.4654293578231));
#10767=CARTESIAN_POINT('Ctrl Pts',(-0.137663428620152,-1.99009753797934,
95.4641598526853));
#10768=CARTESIAN_POINT('Ctrl Pts',(-0.171401369062353,-1.98741860840557,
95.4620153507443));
#10769=CARTESIAN_POINT('Ctrl Pts',(-0.184896767081178,-1.98620853165765,
95.4611494532922));
#10770=CARTESIAN_POINT('Ctrl Pts',(-0.213792624288833,-1.98332050686113,
95.4592765458064));
#10771=CARTESIAN_POINT('Ctrl Pts',(-0.229187296533426,-1.9816005310061,
95.4582674983234));
#10772=CARTESIAN_POINT('Ctrl Pts',(-0.27476792319316,-1.97596978970285,
95.4552496695103));
#10773=CARTESIAN_POINT('Ctrl Pts',(-0.304884874318545,-1.97154736248637,
95.4532162706466));
#10774=CARTESIAN_POINT('Ctrl Pts',(-0.377172120157074,-1.95923675261806,
95.4482586963375));
#10775=CARTESIAN_POINT('Ctrl Pts',(-0.419211859057176,-1.95067385198253,
95.4453119885369));
#10776=CARTESIAN_POINT('Ctrl Pts',(-0.627629794158019,-1.9011736045099,
95.4304785449886));
#10777=CARTESIAN_POINT('Ctrl Pts',(-0.788559727426716,-1.84026406201591,
95.418385180547));
#10778=CARTESIAN_POINT('Ctrl Pts',(-0.975880102200488,-1.7402198818578,
95.4042271508111));
#10779=CARTESIAN_POINT('Ctrl Pts',(-1.01142920599408,-1.7198019016725,95.4015313578321));
#10780=CARTESIAN_POINT('Ctrl Pts',(-1.06773039546024,-1.68511465598701,
95.3972450359742));
#10781=CARTESIAN_POINT('Ctrl Pts',(-1.08888411246433,-1.67152358258132,
95.3956304868089));
#10782=CARTESIAN_POINT('Ctrl Pts',(-1.12961460845479,-1.6442531412768,95.3925117133335));
#10783=CARTESIAN_POINT('Ctrl Pts',(-1.14921373532863,-1.63061504560477,
95.3910062857853));
#10784=CARTESIAN_POINT('Ctrl Pts',(-1.19599410254259,-1.59680030433749,
95.3873983322278));
#10785=CARTESIAN_POINT('Ctrl Pts',(-1.22291627140408,-1.57627697709067,
95.3853096366637));
#10786=CARTESIAN_POINT('Ctrl Pts',(-1.34576153555728,-1.47758663335609,
95.3756961624452));
#10787=CARTESIAN_POINT('Ctrl Pts',(-1.43480305972305,-1.39128744985625,
95.3685066037472));
#10788=CARTESIAN_POINT('Ctrl Pts',(-1.59106580722298,-1.2087663827373,95.354575622804));
#10789=CARTESIAN_POINT('Ctrl Pts',(-1.6589394085242,-1.11378647911449,95.3478521061144));
#10790=CARTESIAN_POINT('Ctrl Pts',(-1.73021015981792,-0.992958130028485,
95.3392359144624));
#10791=CARTESIAN_POINT('Ctrl Pts',(-1.74192376921246,-0.972262572592298,
95.3377576908817));
#10792=CARTESIAN_POINT('Ctrl Pts',(-1.76002954836182,-0.938895510076941,
95.3353624551874));
#10793=CARTESIAN_POINT('Ctrl Pts',(-1.76666167076963,-0.926355928195318,
95.3344596740909));
#10794=CARTESIAN_POINT('Ctrl Pts',(-1.77974904771161,-0.900959399357691,
95.3326238232502));
#10795=CARTESIAN_POINT('Ctrl Pts',(-1.78620004066283,-0.888101286913282,
95.3316906067212));
#10796=CARTESIAN_POINT('Ctrl Pts',(-1.80337709674544,-0.852919678675461,
95.3291293717002));
#10797=CARTESIAN_POINT('Ctrl Pts',(-1.81382703857817,-0.830465093503172,
95.3274862070553));
#10798=CARTESIAN_POINT('Ctrl Pts',(-1.85814204097891,-0.730413272875547,
95.3201459128128));
#10799=CARTESIAN_POINT('Ctrl Pts',(-1.88746268593931,-0.650905271121404,
95.314267189847));
#10800=CARTESIAN_POINT('Ctrl Pts',(-1.95408120416242,-0.427397707683001,
95.2980005412358));
#10801=CARTESIAN_POINT('Ctrl Pts',(-1.98048680204003,-0.280691985162438,
95.2876463359679));
#10802=CARTESIAN_POINT('Ctrl Pts',(-1.99206761974544,-0.106596547266537,
95.2760856043113));
#10803=CARTESIAN_POINT('Ctrl Pts',(-1.99328212697559,-0.0807631774867131,
95.2743871290724));
#10804=CARTESIAN_POINT('Ctrl Pts',(-1.99449450571052,-0.0367390039569643,
95.2715208843643));
#10805=CARTESIAN_POINT('Ctrl Pts',(-1.99474651892921,-0.0185591628008082,
95.2703454385103));
#10806=CARTESIAN_POINT('Ctrl Pts',(-1.99474996418557,-0.000377996936292165,
95.26917776569));
#10807=CARTESIAN_POINT('Origin',(0.,0.,93.6863092095721));
#10808=CARTESIAN_POINT('',(-2.45049957974585,0.00143515344103661,91.0079011502938));
#10809=CARTESIAN_POINT('',(1.07552003335881,2.20186441631719,90.7500985735148));
#10810=CARTESIAN_POINT('Ctrl Pts',(-2.45049957974552,0.00143515400488855,
91.0079011502643));
#10811=CARTESIAN_POINT('Ctrl Pts',(-2.45045513469659,0.0773242734643422,
91.0039383691107));
#10812=CARTESIAN_POINT('Ctrl Pts',(-2.44688570781849,0.153113617481004,
90.9999755879572));
#10813=CARTESIAN_POINT('Ctrl Pts',(-2.43981706709049,0.228567121725641,
90.9960128068037));
#10814=CARTESIAN_POINT('Ctrl Pts',(-2.43225809680979,0.309254600140117,
90.9917751398856));
#10815=CARTESIAN_POINT('Ctrl Pts',(-2.42067817110913,0.389716438532518,
90.9875374729676));
#10816=CARTESIAN_POINT('Ctrl Pts',(-2.40509883718744,0.469520855084889,
90.9832998060496));
#10817=CARTESIAN_POINT('Ctrl Pts',(-2.38954194646292,0.549210307399057,
90.9790682438081));
#10818=CARTESIAN_POINT('Ctrl Pts',(-2.36999717910937,0.628243767924927,
90.9748366815665));
#10819=CARTESIAN_POINT('Ctrl Pts',(-2.3465378718612,0.706194212608052,90.970605119325));
#10820=CARTESIAN_POINT('Ctrl Pts',(-2.32300893032839,0.784376037672345,
90.9663609965332));
#10821=CARTESIAN_POINT('Ctrl Pts',(-2.29554222219168,0.861467938715433,
90.9621168737413));
#10822=CARTESIAN_POINT('Ctrl Pts',(-2.26426354690845,0.93704900626465,90.9578727509494));
#10823=CARTESIAN_POINT('Ctrl Pts',(-2.23313447742932,1.01226856980888,90.9536489277833));
#10824=CARTESIAN_POINT('Ctrl Pts',(-2.198229996004,1.08599128588063,90.9494251046172));
#10825=CARTESIAN_POINT('Ctrl Pts',(-2.15972356100008,1.15781880709425,90.9452012814511));
#10826=CARTESIAN_POINT('Ctrl Pts',(-2.1212303860275,1.22962159386587,90.9409789127959));
#10827=CARTESIAN_POINT('Ctrl Pts',(-2.07913793966161,1.29953007383443,90.9367565441406));
#10828=CARTESIAN_POINT('Ctrl Pts',(-2.03366625515513,1.36716926993086,90.9325341754853));
#10829=CARTESIAN_POINT('Ctrl Pts',(-1.98819640912799,1.43480573128665,90.9283119775459));
#10830=CARTESIAN_POINT('Ctrl Pts',(-1.93934785597698,1.50017270716457,90.9240897796065));
#10831=CARTESIAN_POINT('Ctrl Pts',(-1.88738391238524,1.5629242519295,90.9198675816671));
#10832=CARTESIAN_POINT('Ctrl Pts',(-1.83495328127442,1.62623936752298,90.9156074642215));
#10833=CARTESIAN_POINT('Ctrl Pts',(-1.77935131023484,1.68689145526741,90.9113473467759));
#10834=CARTESIAN_POINT('Ctrl Pts',(-1.72088874892593,1.74456073663836,90.9070872293303));
#10835=CARTESIAN_POINT('Ctrl Pts',(-1.6628652686989,1.80179689482945,90.9028591073521));
#10836=CARTESIAN_POINT('Ctrl Pts',(-1.60202441132498,1.8560946328778,90.8986309853739));
#10837=CARTESIAN_POINT('Ctrl Pts',(-1.5387043079605,1.90718098319582,90.8944028633957));
#10838=CARTESIAN_POINT('Ctrl Pts',(-1.4746654612688,1.95884721212195,90.8901267482164));
#10839=CARTESIAN_POINT('Ctrl Pts',(-1.40809112214727,2.00722839985949,90.8858506330371));
#10840=CARTESIAN_POINT('Ctrl Pts',(-1.33936071827131,2.0520875021187,90.8815745178577));
#10841=CARTESIAN_POINT('Ctrl Pts',(-1.27063031439535,2.09694660437791,90.8772984026784));
#10842=CARTESIAN_POINT('Ctrl Pts',(-1.19974429486011,2.13828343119256,90.8730222874991));
#10843=CARTESIAN_POINT('Ctrl Pts',(-1.12710540617508,2.17590984495473,90.8687461723198));
#10844=CARTESIAN_POINT('Ctrl Pts',(-1.05595631550261,2.21276455422834,90.8645577587561));
#10845=CARTESIAN_POINT('Ctrl Pts',(-0.982852107750259,2.24620109854361,
90.8603693451924));
#10846=CARTESIAN_POINT('Ctrl Pts',(-0.90815856879314,2.27600489101575,90.8561809316287));
#10847=CARTESIAN_POINT('Ctrl Pts',(-0.83357144946631,2.3057662205303,90.8519984855079));
#10848=CARTESIAN_POINT('Ctrl Pts',(-0.757399931236271,2.33190489769667,
90.847816039387));
#10849=CARTESIAN_POINT('Ctrl Pts',(-0.680034221161387,2.35425226092053,
90.8436335932661));
#10850=CARTESIAN_POINT('Ctrl Pts',(-0.602755438791394,2.37657451476461,
90.8394558465198));
#10851=CARTESIAN_POINT('Ctrl Pts',(-0.524285584084021,2.39511378547164,
90.8352780997734));
#10852=CARTESIAN_POINT('Ctrl Pts',(-0.445033163404528,2.40975013921986,
90.831100353027));
#10853=CARTESIAN_POINT('Ctrl Pts',(-0.365828226585273,2.42437772363878,
90.8269251093656));
#10854=CARTESIAN_POINT('Ctrl Pts',(-0.285842120195265,2.43510694459348,
90.8227498657042));
#10855=CARTESIAN_POINT('Ctrl Pts',(-0.205495493448251,2.44186851656113,
90.8185746220427));
#10856=CARTESIAN_POINT('Ctrl Pts',(-0.125171178618621,2.44862821086894,
90.8144005378288));
#10857=CARTESIAN_POINT('Ctrl Pts',(-0.0444870154651063,2.45142240394326,
90.8102264536148));
#10858=CARTESIAN_POINT('Ctrl Pts',(0.036130810748099,2.45023362447639,90.8060523694009));
#10859=CARTESIAN_POINT('Ctrl Pts',(0.11675216395715,2.44904479300091,90.8018781025725));
#10860=CARTESIAN_POINT('Ctrl Pts',(0.197306699372924,2.44387265252368,90.7977038357441));
#10861=CARTESIAN_POINT('Ctrl Pts',(0.277369399422697,2.43475182847532,90.7935295689157));
#10862=CARTESIAN_POINT('Ctrl Pts',(0.357510268542577,2.42562209932714,90.7893512265496));
#10863=CARTESIAN_POINT('Ctrl Pts',(0.437157871055443,2.41253604661732,90.7851728841834));
#10864=CARTESIAN_POINT('Ctrl Pts',(0.51589427676123,2.39557996009422,90.7809945418173));
#10865=CARTESIAN_POINT('Ctrl Pts',(0.594674132214892,2.37861451655668,90.7768138936827));
#10866=CARTESIAN_POINT('Ctrl Pts',(0.672541331726469,2.3577749134305,90.7726332455481));
#10867=CARTESIAN_POINT('Ctrl Pts',(0.749092534027391,2.33319751102739,90.7684525974135));
#10868=CARTESIAN_POINT('Ctrl Pts',(0.825765885523192,2.3085808916058,90.764265278413));
#10869=CARTESIAN_POINT('Ctrl Pts',(0.901118605741132,2.2802147391212,90.7600779594125));
#10870=CARTESIAN_POINT('Ctrl Pts',(0.974767401018496,2.24828351502021,90.755890640412));
#10871=CARTESIAN_POINT('Ctrl Pts',(1.00872538615526,2.23356066681426,90.7539599514462));
#10872=CARTESIAN_POINT('Ctrl Pts',(1.0423214721646,2.21808054542054,90.7520292624805));
#10873=CARTESIAN_POINT('Ctrl Pts',(1.07552003335881,2.20186441631719,90.7500985735148));
#10874=CARTESIAN_POINT('',(-1.07508846035167,2.2020751695659,90.7500736540522));
#10875=CARTESIAN_POINT('Origin',(0.,0.,90.7500736540522));
#10876=CARTESIAN_POINT('',(-2.45072924584278,0.0021129184388593,90.8922461578402));
#10877=CARTESIAN_POINT('Ctrl Pts',(-1.07508846035167,2.2020751695659,90.7500736540522));
#10878=CARTESIAN_POINT('Ctrl Pts',(-1.8087830660249,1.84387368085965,90.7924958655468));
#10879=CARTESIAN_POINT('Ctrl Pts',(-2.40530016291556,1.0047114134998,90.8398867001428));
#10880=CARTESIAN_POINT('Ctrl Pts',(-2.45341561407347,0.0973545315146867,
90.8872775347387));
#10881=CARTESIAN_POINT('Ctrl Pts',(-2.45268413588137,0.00211460386502969,
90.8922461578402));
#10882=CARTESIAN_POINT('',(-2.45049967807228,0.00125609221652004,91.6922461578137));
#10883=CARTESIAN_POINT('Ctrl Pts',(-2.45049908924981,0.002112720007266,
90.8922461578402));
#10884=CARTESIAN_POINT('Ctrl Pts',(-2.45056743907129,-0.0771647870499678,
90.8963857471584));
#10885=CARTESIAN_POINT('Ctrl Pts',(-2.4467845025604,-0.156615417674207,
90.9005253364765));
#10886=CARTESIAN_POINT('Ctrl Pts',(-2.43912640173371,-0.235823337194504,
90.9046649257947));
#10887=CARTESIAN_POINT('Ctrl Pts',(-2.43142267969008,-0.315503118049918,
90.9088291756791));
#10888=CARTESIAN_POINT('Ctrl Pts',(-2.41979738988535,-0.394936793730064,
90.9129934255634));
#10889=CARTESIAN_POINT('Ctrl Pts',(-2.40427949190856,-0.473698611764804,
90.9171576754478));
#10890=CARTESIAN_POINT('Ctrl Pts',(-2.38888912154466,-0.551813157426998,
90.9212877031168));
#10891=CARTESIAN_POINT('Ctrl Pts',(-2.36966996403225,-0.629266359954761,
90.9254177307857));
#10892=CARTESIAN_POINT('Ctrl Pts',(-2.34670224663734,-0.705647798570415,
90.9295477584547));
#10893=CARTESIAN_POINT('Ctrl Pts',(-2.32374575456158,-0.781991906265813,
90.9336757676001));
#10894=CARTESIAN_POINT('Ctrl Pts',(-2.29704447515276,-0.857264824312452,
90.9378037767455));
#10895=CARTESIAN_POINT('Ctrl Pts',(-2.26672915922954,-0.931068831343059,
90.9419317858909));
#10896=CARTESIAN_POINT('Ctrl Pts',(-2.23641852515404,-1.00486144020376,
90.9460591575133));
#10897=CARTESIAN_POINT('Ctrl Pts',(-2.20249514766258,-1.07718513927766,
90.9501865291357));
#10898=CARTESIAN_POINT('Ctrl Pts',(-2.16513821012427,-1.14766144008583,
90.9543139007582));
#10899=CARTESIAN_POINT('Ctrl Pts',(-2.12720459960284,-1.21922567211385,
90.9585049859466));
#10900=CARTESIAN_POINT('Ctrl Pts',(-2.08573073865029,-1.28888451711404,
90.9626960711351));
#10901=CARTESIAN_POINT('Ctrl Pts',(-2.04095207066785,-1.35626874004993,
90.9668871563235));
#10902=CARTESIAN_POINT('Ctrl Pts',(-1.99679743076912,-1.42271390764082,
90.9710198352445));
#10903=CARTESIAN_POINT('Ctrl Pts',(-1.94942986193507,-1.48694709560799,
90.9751525141655));
#10904=CARTESIAN_POINT('Ctrl Pts',(-1.89911681959994,-1.54864636231536,
90.9792851930865));
#10905=CARTESIAN_POINT('Ctrl Pts',(-1.84773718206216,-1.61165360283673,
90.9835054814086));
#10906=CARTESIAN_POINT('Ctrl Pts',(-1.7932861136744,-1.67201785723896,90.9877257697308));
#10907=CARTESIAN_POINT('Ctrl Pts',(-1.73608761335537,-1.72943633845078,
90.991946058053));
#10908=CARTESIAN_POINT('Ctrl Pts',(-1.67888911303634,-1.7868548196626,90.9961663463752));
#10909=CARTESIAN_POINT('Ctrl Pts',(-1.61894362655612,-1.84132723005314,
91.0003866346973));
#10910=CARTESIAN_POINT('Ctrl Pts',(-1.55660843855108,-1.89259621130117,
91.0046069230195));
#10911=CARTESIAN_POINT('Ctrl Pts',(-1.49409889418781,-1.94400859586838,
91.0088390158156));
#10912=CARTESIAN_POINT('Ctrl Pts',(-1.42892132213003,-1.99241796493926,
91.0130711086118));
#10913=CARTESIAN_POINT('Ctrl Pts',(-1.36139612885017,-2.03753547953202,
91.0173032014079));
#10914=CARTESIAN_POINT('Ctrl Pts',(-1.29396893282173,-2.08258751645332,
91.0215291522969));
#10915=CARTESIAN_POINT('Ctrl Pts',(-1.22420126527627,-2.12435693113119,
91.025755103186));
#10916=CARTESIAN_POINT('Ctrl Pts',(-1.15244672085264,-2.16259492406599,
91.029981054075));
#10917=CARTESIAN_POINT('Ctrl Pts',(-1.08035988608247,-2.20100999450893,
91.0342265750512));
#10918=CARTESIAN_POINT('Ctrl Pts',(-1.00626809011726,-2.23586054731741,
91.0384720960274));
#10919=CARTESIAN_POINT('Ctrl Pts',(-0.930559563531785,-2.26693827633651,
91.0427176170036));
#10920=CARTESIAN_POINT('Ctrl Pts',(-0.855338954235491,-2.29781571931148,
91.0469357769521));
#10921=CARTESIAN_POINT('Ctrl Pts',(-0.778522825667158,-2.32496864381566,
91.0511539369007));
#10922=CARTESIAN_POINT('Ctrl Pts',(-0.700515124397133,-2.34823951301627,
91.0553720968493));
#10923=CARTESIAN_POINT('Ctrl Pts',(-0.622534457104597,-2.37150231757526,
91.0595887949724));
#10924=CARTESIAN_POINT('Ctrl Pts',(-0.543363482118892,-2.39088560576755,
91.0638054930955));
#10925=CARTESIAN_POINT('Ctrl Pts',(-0.463422411726648,-2.40628134645753,
91.0680221912187));
#10926=CARTESIAN_POINT('Ctrl Pts',(-0.383484579401404,-2.42167646353264,
91.0722387185416));
#10927=CARTESIAN_POINT('Ctrl Pts',(-0.302777170206746,-2.43308426730393,
91.0764552458646));
#10928=CARTESIAN_POINT('Ctrl Pts',(-0.221730309608513,-2.44044789327716,
91.0806717731875));
#10929=CARTESIAN_POINT('Ctrl Pts',(-0.139716850862543,-2.44789934087819,
91.0849385885471));
#10930=CARTESIAN_POINT('Ctrl Pts',(-0.0573562728661285,-2.45120944097674,
91.0892054039068));
#10931=CARTESIAN_POINT('Ctrl Pts',(0.0249025668580095,-2.45037346381401,
91.0934722192664));
#10932=CARTESIAN_POINT('Ctrl Pts',(0.106307188240684,-2.44954616787057,
91.0976947258083));
#10933=CARTESIAN_POINT('Ctrl Pts',(0.187611708700424,-2.44465859566981,
91.1019172323501));
#10934=CARTESIAN_POINT('Ctrl Pts',(0.268385105960193,-2.43575854404716,
91.106139738892));
#10935=CARTESIAN_POINT('Ctrl Pts',(0.350429895118906,-2.42671840355965,
91.1104287086605));
#10936=CARTESIAN_POINT('Ctrl Pts',(0.431926203475093,-2.41353845486016,
91.114717678429));
#10937=CARTESIAN_POINT('Ctrl Pts',(0.51243385038469,-2.39632255737409,91.1190066481976));
#10938=CARTESIAN_POINT('Ctrl Pts',(0.592941497294287,-2.37910665988803,
91.1232956179661));
#10939=CARTESIAN_POINT('Ctrl Pts',(0.672460020853889,-2.35785500412892,
91.1275845877346));
#10940=CARTESIAN_POINT('Ctrl Pts',(0.750567944672692,-2.33272330344381,
91.1318735575032));
#10941=CARTESIAN_POINT('Ctrl Pts',(0.827728943281444,-2.3078962817181,91.1361105308365));
#10942=CARTESIAN_POINT('Ctrl Pts',(0.903797115072659,-2.27919155039504,
91.1403475041698));
#10943=CARTESIAN_POINT('Ctrl Pts',(0.978355688278953,-2.24672437054753,
91.1445844775031));
#10944=CARTESIAN_POINT('Ctrl Pts',(1.05280945564194,-2.21430282931699,91.148815494988));
#10945=CARTESIAN_POINT('Ctrl Pts',(1.12575741783497,-2.17812952808982,91.1530465124729));
#10946=CARTESIAN_POINT('Ctrl Pts',(1.19679876863617,-2.13836922849889,91.1572775299578));
#10947=CARTESIAN_POINT('Ctrl Pts',(1.26806276455654,-2.09848431927512,91.1615218075423));
#10948=CARTESIAN_POINT('Ctrl Pts',(1.33740773158128,-2.05499004088285,91.1657660851268));
#10949=CARTESIAN_POINT('Ctrl Pts',(1.40445014968875,-2.0081010998053,91.1700103627114));
#10950=CARTESIAN_POINT('Ctrl Pts',(1.47116663636426,-1.96144011261336,91.1742340064419));
#10951=CARTESIAN_POINT('Ctrl Pts',(1.53560252560777,-1.91141765803171,91.1784576501724));
#10952=CARTESIAN_POINT('Ctrl Pts',(1.59740686925234,-1.85828995155907,91.1826812939028));
#10953=CARTESIAN_POINT('Ctrl Pts',(1.65919194304514,-1.80517880966699,91.186903620752));
#10954=CARTESIAN_POINT('Ctrl Pts',(1.71834674956607,-1.74896464061557,91.1911259476011));
#10955=CARTESIAN_POINT('Ctrl Pts',(1.77455333156267,-1.6899440000899,91.1953482744502));
#10956=CARTESIAN_POINT('Ctrl Pts',(1.83075947177766,-1.63092382346423,91.199570568112));
#10957=CARTESIAN_POINT('Ctrl Pts',(1.88401711481614,-1.56909755566347,91.2037928617738));
#10958=CARTESIAN_POINT('Ctrl Pts',(1.9340460977904,-1.50479764141951,91.2080151554355));
#10959=CARTESIAN_POINT('Ctrl Pts',(1.98452682754016,-1.43991711815258,91.2122755751481));
#10960=CARTESIAN_POINT('Ctrl Pts',(2.03171998594613,-1.37251841771079,91.2165359948607));
#10961=CARTESIAN_POINT('Ctrl Pts',(2.07538130018495,-1.30297456185554,91.2207964145733));
#10962=CARTESIAN_POINT('Ctrl Pts',(2.11871604921364,-1.23395085992365,91.2250249684367));
#10963=CARTESIAN_POINT('Ctrl Pts',(2.15857143470742,-1.16281442289989,91.2292535223));
#10964=CARTESIAN_POINT('Ctrl Pts',(2.19475485581178,-1.08995475726775,91.2334820761633));
#10965=CARTESIAN_POINT('Ctrl Pts',(2.23134728747168,-1.01627149974169,91.2377584288005));
#10966=CARTESIAN_POINT('Ctrl Pts',(2.26418402344729,-0.940826257024861,
91.2420347814378));
#10967=CARTESIAN_POINT('Ctrl Pts',(2.29311657414475,-0.864040871361226,
91.246311134075));
#10968=CARTESIAN_POINT('Ctrl Pts',(2.3220491248422,-0.78725548569759,91.2505874867123));
#10969=CARTESIAN_POINT('Ctrl Pts',(2.34707740405044,-0.709130436852748,
91.2548638393495));
#10970=CARTESIAN_POINT('Ctrl Pts',(2.36810573449615,-0.630099579627262,
91.2591401919867));
#10971=CARTESIAN_POINT('Ctrl Pts',(2.38888774293271,-0.551994475379956,
91.2633664522129));
#10972=CARTESIAN_POINT('Ctrl Pts',(2.40584138049712,-0.472710168724586,
91.267592712439));
#10973=CARTESIAN_POINT('Ctrl Pts',(2.41883666287613,-0.39265690917934,91.2718189726651));
#10974=CARTESIAN_POINT('Ctrl Pts',(2.43181305628693,-0.31272000905053,91.2760390899163));
#10975=CARTESIAN_POINT('Ctrl Pts',(2.44084244652806,-0.232016831806835,
91.2802592071674));
#10976=CARTESIAN_POINT('Ctrl Pts',(2.44584503305822,-0.150971269665648,
91.2844793244185));
#10977=CARTESIAN_POINT('Ctrl Pts',(2.45087946218339,-0.0694098341860879,
91.2887263036707));
#10978=CARTESIAN_POINT('Ctrl Pts',(2.45183551013241,0.0124978994752909,
91.2929732829228));
#10979=CARTESIAN_POINT('Ctrl Pts',(2.44868447964768,0.0943110233884802,
91.297220262175));
#10980=CARTESIAN_POINT('Ctrl Pts',(2.44555912884175,0.175457402008593,91.3014326301901));
#10981=CARTESIAN_POINT('Ctrl Pts',(2.43839341430412,0.256510233847653,91.3056449982052));
#10982=CARTESIAN_POINT('Ctrl Pts',(2.42721154767961,0.337037613347162,91.3098573662203));
#10983=CARTESIAN_POINT('Ctrl Pts',(2.41603348499446,0.417537598380396,91.3140683012374));
#10984=CARTESIAN_POINT('Ctrl Pts',(2.40084204720005,0.497512024633151,91.3182792362545));
#10985=CARTESIAN_POINT('Ctrl Pts',(2.38171323801658,0.576534736036415,91.3224901712716));
#10986=CARTESIAN_POINT('Ctrl Pts',(2.36258503746332,0.655554933137372,91.3267009723074));
#10987=CARTESIAN_POINT('Ctrl Pts',(2.33951982525727,0.733623022717624,91.3309117733433));
#10988=CARTESIAN_POINT('Ctrl Pts',(2.31264426668479,0.810325086474536,91.3351225743791));
#10989=CARTESIAN_POINT('Ctrl Pts',(2.28536733233596,0.888172665042057,91.3393962620534));
#10990=CARTESIAN_POINT('Ctrl Pts',(2.25416544730402,0.964612606952473,91.3436699497276));
#10991=CARTESIAN_POINT('Ctrl Pts',(2.2192221583429,1.03923205393208,91.3479436374019));
#10992=CARTESIAN_POINT('Ctrl Pts',(2.18474293714266,1.11286051006029,91.3521605679497));
#10993=CARTESIAN_POINT('Ctrl Pts',(2.14662137229914,1.18471614940506,91.3563774984976));
#10994=CARTESIAN_POINT('Ctrl Pts',(2.10507981829468,1.25442784113254,91.3605944290454));
#10995=CARTESIAN_POINT('Ctrl Pts',(2.06269958107988,1.32554694350742,91.3648964952829));
#10996=CARTESIAN_POINT('Ctrl Pts',(2.01676003344093,1.39443415560823,91.3691985615204));
#10997=CARTESIAN_POINT('Ctrl Pts',(1.96754200890561,1.46072882260592,91.3735006277579));
#10998=CARTESIAN_POINT('Ctrl Pts',(1.91832398437029,1.52702348960362,91.3778026939954));
#10999=CARTESIAN_POINT('Ctrl Pts',(1.86582785852188,1.59072526320331,91.3821047602329));
#11000=CARTESIAN_POINT('Ctrl Pts',(1.81037443843145,1.65151283454717,91.3864068264704));
#11001=CARTESIAN_POINT('Ctrl Pts',(1.75584060816807,1.71129235927951,91.3906375510964));
#11002=CARTESIAN_POINT('Ctrl Pts',(1.69823993396493,1.76848049263467,91.3948682757225));
#11003=CARTESIAN_POINT('Ctrl Pts',(1.63784841461398,1.8227459561734,91.3990990003486));
#11004=CARTESIAN_POINT('Ctrl Pts',(1.57754383172299,1.87693330200042,91.4033236346457));
#11005=CARTESIAN_POINT('Ctrl Pts',(1.51445672572685,1.92820602577567,91.4075482689428));
#11006=CARTESIAN_POINT('Ctrl Pts',(1.44890163164046,1.97626777331151,91.4117729032399));
#11007=CARTESIAN_POINT('Ctrl Pts',(1.38301722427066,2.02457095703332,91.4160187598113));
#11008=CARTESIAN_POINT('Ctrl Pts',(1.31464028193079,2.06963045947639,91.4202646163827));
#11009=CARTESIAN_POINT('Ctrl Pts',(1.24412577577074,2.11118481049454,91.4245104729541));
#11010=CARTESIAN_POINT('Ctrl Pts',(1.17409084086693,2.15245654913396,91.4287274533286));
#11011=CARTESIAN_POINT('Ctrl Pts',(1.10194773272879,2.19027042611534,91.432944433703));
#11012=CARTESIAN_POINT('Ctrl Pts',(1.02807379065457,2.22441330039387,91.4371614140775));
#11013=CARTESIAN_POINT('Ctrl Pts',(0.954224502422788,2.258544780221,91.4413769871252));
#11014=CARTESIAN_POINT('Ctrl Pts',(0.878645949137833,2.28900749525625,91.445592560173));
#11015=CARTESIAN_POINT('Ctrl Pts',(0.801738584013049,2.31563500856779,91.4498081332208));
#11016=CARTESIAN_POINT('Ctrl Pts',(0.724833307421517,2.34226179876983,91.4540235917884));
#11017=CARTESIAN_POINT('Ctrl Pts',(0.646599730549771,2.36505344316696,91.4582390503561));
#11018=CARTESIAN_POINT('Ctrl Pts',(0.567455362713911,2.38389275373856,91.4624545089237));
#11019=CARTESIAN_POINT('Ctrl Pts',(0.487319921642071,2.4029679766941,91.4667227549262));
#11020=CARTESIAN_POINT('Ctrl Pts',(0.406251190842225,2.41799106019703,91.4709910009288));
#11021=CARTESIAN_POINT('Ctrl Pts',(0.324693356818091,2.42889367285565,91.4752592469313));
#11022=CARTESIAN_POINT('Ctrl Pts',(0.24402705096861,2.43967710644975,91.4794808357167));
#11023=CARTESIAN_POINT('Ctrl Pts',(0.162882757072662,2.44642973684538,91.4837024245022));
#11024=CARTESIAN_POINT('Ctrl Pts',(0.0816936827292237,2.44913788754372,
91.4879240132876));
#11025=CARTESIAN_POINT('Ctrl Pts',(-0.000841350372748101,2.45189093417396,
91.4922155878987));
#11026=CARTESIAN_POINT('Ctrl Pts',(-0.0834221605331062,2.45046419170395,
91.4965071625098));
#11027=CARTESIAN_POINT('Ctrl Pts',(-0.165597476810826,2.4448983057939,91.5007987371208));
#11028=CARTESIAN_POINT('Ctrl Pts',(-0.247772793088547,2.43933241988385,
91.5050903117319));
#11029=CARTESIAN_POINT('Ctrl Pts',(-0.329542129134761,2.42962751502606,
91.509381886343));
#11030=CARTESIAN_POINT('Ctrl Pts',(-0.410465475052023,2.41587837934576,
91.5136734609541));
#11031=CARTESIAN_POINT('Ctrl Pts',(-0.490245391315762,2.40232351602617,
91.5179043965293));
#11032=CARTESIAN_POINT('Ctrl Pts',(-0.569503016509799,2.38478706615771,
91.5221353321046));
#11033=CARTESIAN_POINT('Ctrl Pts',(-0.647810405818882,2.36332222265877,
91.5263662676798));
#11034=CARTESIAN_POINT('Ctrl Pts',(-0.726005377566023,2.34188819394493,
91.5305911293524));
#11035=CARTESIAN_POINT('Ctrl Pts',(-0.803252378057271,2.31653709402733,
91.534815991025));
#11036=CARTESIAN_POINT('Ctrl Pts',(-0.879132023708561,2.2873734139598,91.5390408526976));
#11037=CARTESIAN_POINT('Ctrl Pts',(-0.955387759304852,2.25806518700174,
91.5432866544784));
#11038=CARTESIAN_POINT('Ctrl Pts',(-1.03026207846466,2.22490655876264,91.5475324562593));
#11039=CARTESIAN_POINT('Ctrl Pts',(-1.10334318304459,2.18805486001358,91.5517782580401));
#11040=CARTESIAN_POINT('Ctrl Pts',(-1.17593277617475,2.15145100962399,91.5559955044207));
#11041=CARTESIAN_POINT('Ctrl Pts',(-1.24675278077154,2.11120382374383,91.5602127508014));
#11042=CARTESIAN_POINT('Ctrl Pts',(-1.31541988539227,2.06751560456375,91.564429997182));
#11043=CARTESIAN_POINT('Ctrl Pts',(-1.38406430308522,2.02384181953636,91.5686458502264));
#11044=CARTESIAN_POINT('Ctrl Pts',(-1.45055684129531,1.97672950827991,91.5728617032708));
#11045=CARTESIAN_POINT('Ctrl Pts',(-1.51454099345995,1.92642566145942,91.5770775563152));
#11046=CARTESIAN_POINT('Ctrl Pts',(-1.57852361556741,1.87612301755807,91.5812933085457));
#11047=CARTESIAN_POINT('Ctrl Pts',(-1.63999760600182,1.8226292780823,91.5855090607761));
#11048=CARTESIAN_POINT('Ctrl Pts',(-1.69863867736784,1.76623240083236,91.5897248130065));
#11049=CARTESIAN_POINT('Ctrl Pts',(-1.75800568290457,1.70913737091632,91.5939927532091));
#11050=CARTESIAN_POINT('Ctrl Pts',(-1.81446878279535,1.64906715546246,91.5982606934117));
#11051=CARTESIAN_POINT('Ctrl Pts',(-1.8677305025613,1.58635841467246,91.6025286336143));
#11052=CARTESIAN_POINT('Ctrl Pts',(-1.92041783061837,1.52432594533862,91.6067505469616));
#11053=CARTESIAN_POINT('Ctrl Pts',(-1.96997225921513,1.4597119979723,91.610972460309));
#11054=CARTESIAN_POINT('Ctrl Pts',(-2.0161481003516,1.39287367964529,91.6151943736563));
#11055=CARTESIAN_POINT('Ctrl Pts',(-2.06307904773308,1.32494236484367,91.6194853272865));
#11056=CARTESIAN_POINT('Ctrl Pts',(-2.1065196539566,1.25471370317424,91.6237762809168));
#11057=CARTESIAN_POINT('Ctrl Pts',(-2.14626030531889,1.18258908831955,91.628067234547));
#11058=CARTESIAN_POINT('Ctrl Pts',(-2.18600095668118,1.11046447346486,91.6323581881772));
#11059=CARTESIAN_POINT('Ctrl Pts',(-2.22204149530785,1.0364443813276,91.6366491418074));
#11060=CARTESIAN_POINT('Ctrl Pts',(-2.25422390054525,0.96094997591474,91.6409400954376));
#11061=CARTESIAN_POINT('Ctrl Pts',(-2.28939609327408,0.878442041608973,
91.645629684266));
#11062=CARTESIAN_POINT('Ctrl Pts',(-2.32007409940227,0.793908437648198,
91.6503192730944));
#11063=CARTESIAN_POINT('Ctrl Pts',(-2.34604528037445,0.707828928790533,
91.6550088619228));
#11064=CARTESIAN_POINT('Ctrl Pts',(-2.3719365489229,0.622014283598263,91.6596840210489));
#11065=CARTESIAN_POINT('Ctrl Pts',(-2.39314975910987,0.534663482575286,
91.6643591801751));
#11066=CARTESIAN_POINT('Ctrl Pts',(-2.40952050134751,0.446274807250013,
91.6690343393012));
#11067=CARTESIAN_POINT('Ctrl Pts',(-2.42580494861234,0.358352054497048,
91.6736848542955));
#11068=CARTESIAN_POINT('Ctrl Pts',(-2.43729772338479,0.269402608710182,
91.6783353692898));
#11069=CARTESIAN_POINT('Ctrl Pts',(-2.4438848934866,0.17993575905863,91.682985884284));
#11070=CARTESIAN_POINT('Ctrl Pts',(-2.44825709721058,0.120552550917064,
91.6860726421273));
#11071=CARTESIAN_POINT('Ctrl Pts',(-2.45046908401557,0.0609417786025406,
91.6891593999705));
#11072=CARTESIAN_POINT('Ctrl Pts',(-2.45049967807228,0.00125609221651381,
91.6922461578137));
#11073=CARTESIAN_POINT('',(-2.45049913396335,-0.00206020505177885,92.4922461578873));
#11074=CARTESIAN_POINT('Ctrl Pts',(-2.45049967807254,0.00125609170658984,
91.6922461578401));
#11075=CARTESIAN_POINT('Ctrl Pts',(-2.45054204849881,-0.081404047988421,
91.6965210828678));
#11076=CARTESIAN_POINT('Ctrl Pts',(-2.44639764250949,-0.164058934585186,
91.7007960078954));
#11077=CARTESIAN_POINT('Ctrl Pts',(-2.43809446303437,-0.246263353589474,
91.7050709329231));
#11078=CARTESIAN_POINT('Ctrl Pts',(-2.4297882751226,-0.328497557182675,
91.7093474068564));
#11079=CARTESIAN_POINT('Ctrl Pts',(-2.41732036322395,-0.410280524442328,
91.7136238807896));
#11080=CARTESIAN_POINT('Ctrl Pts',(-2.40077043863469,-0.49117364646101,
91.7179003547229));
#11081=CARTESIAN_POINT('Ctrl Pts',(-2.3841963819031,-0.572184722149131,
91.722183064363));
#11082=CARTESIAN_POINT('Ctrl Pts',(-2.36352851502258,-0.652302922682686,
91.726465774003));
#11083=CARTESIAN_POINT('Ctrl Pts',(-2.33889738497076,-0.731101410597003,
91.7307484836431));
#11084=CARTESIAN_POINT('Ctrl Pts',(-2.31424815295302,-0.80995780927467,
91.7350343407419));
#11085=CARTESIAN_POINT('Ctrl Pts',(-2.28563001059868,-0.887492144238603,
91.7393201978406));
#11086=CARTESIAN_POINT('Ctrl Pts',(-2.25322208313341,-0.963296680197705,
91.7436060549394));
#11087=CARTESIAN_POINT('Ctrl Pts',(-2.22074618234079,-1.03926021078992,
91.7479009013192));
#11088=CARTESIAN_POINT('Ctrl Pts',(-2.18446480815363,-1.11348628981486,
91.7521957476989));
#11089=CARTESIAN_POINT('Ctrl Pts',(-2.14460364977197,-1.18559075375305,
91.7564905940787));
#11090=CARTESIAN_POINT('Ctrl Pts',(-2.10835720421532,-1.25115659861646,
91.7603959726929));
#11091=CARTESIAN_POINT('Ctrl Pts',(-2.06915148962827,-1.31496829758165,
91.7643013513071));
#11092=CARTESIAN_POINT('Ctrl Pts',(-2.02718605476699,-1.37675958299125,
91.7682067299212));
#11093=CARTESIAN_POINT('Ctrl Pts',(-1.98172888403876,-1.44369221504108,
91.772437055736));
#11094=CARTESIAN_POINT('Ctrl Pts',(-1.93286753073307,-1.50849728424299,
91.7766673815508));
#11095=CARTESIAN_POINT('Ctrl Pts',(-1.88082792531648,-1.57080761563907,
91.7808977073656));
#11096=CARTESIAN_POINT('Ctrl Pts',(-1.82886321192093,-1.6330282740522,91.7851219451701));
#11097=CARTESIAN_POINT('Ctrl Pts',(-1.77372962606296,-1.69276097108578,
91.7893461829747));
#11098=CARTESIAN_POINT('Ctrl Pts',(-1.71569621861873,-1.74966760712353,
91.7935704207792));
#11099=CARTESIAN_POINT('Ctrl Pts',(-1.65736444256019,-1.80686681867748,
91.7978163767636));
#11100=CARTESIAN_POINT('Ctrl Pts',(-1.59610320588525,-1.86121043003094,
91.802062332748));
#11101=CARTESIAN_POINT('Ctrl Pts',(-1.53222666532007,-1.91238900229062,
91.8063082887324));
#11102=CARTESIAN_POINT('Ctrl Pts',(-1.4687918697727,-1.96321364368439,91.8105248813561));
#11103=CARTESIAN_POINT('Ctrl Pts',(-1.40277819676894,-2.01091658948931,
91.8147414739798));
#11104=CARTESIAN_POINT('Ctrl Pts',(-1.33452872187373,-2.05523315964249,
91.8189580666035));
#11105=CARTESIAN_POINT('Ctrl Pts',(-1.26630195816462,-2.09953498269508,
91.8231732560835));
#11106=CARTESIAN_POINT('Ctrl Pts',(-1.19584125982708,-2.14045241472924,
91.8273884455635));
#11107=CARTESIAN_POINT('Ctrl Pts',(-1.12351923302871,-2.17776371147436,
91.8316036350435));
#11108=CARTESIAN_POINT('Ctrl Pts',(-1.05119908926899,-2.21507403675039,
91.8358187147732));
#11109=CARTESIAN_POINT('Ctrl Pts',(-0.97701812728281,-2.24877820109266,
91.8400337945029));
#11110=CARTESIAN_POINT('Ctrl Pts',(-0.901372849030125,-2.27870077830138,
91.8442488742326));
#11111=CARTESIAN_POINT('Ctrl Pts',(-0.824765148011244,-2.30900405567004,
91.848517581747));
#11112=CARTESIAN_POINT('Ctrl Pts',(-0.746656054289783,-2.33542864332484,
91.8527862892613));
#11113=CARTESIAN_POINT('Ctrl Pts',(-0.667475684203846,-2.35784360401546,
91.8570549967757));
#11114=CARTESIAN_POINT('Ctrl Pts',(-0.589176057216373,-2.38000923748129,
91.8612762223867));
#11115=CARTESIAN_POINT('Ctrl Pts',(-0.509829340652844,-2.39825395685959,
91.8654974479976));
#11116=CARTESIAN_POINT('Ctrl Pts',(-0.429862314547043,-2.41250256798459,
91.8697186736086));
#11117=CARTESIAN_POINT('Ctrl Pts',(-0.348546040512666,-2.42699158956353,
91.8740111220747));
#11118=CARTESIAN_POINT('Ctrl Pts',(-0.266588829685823,-2.4373483447573,
91.8783035705407));
#11119=CARTESIAN_POINT('Ctrl Pts',(-0.184443459463732,-2.44354882502091,
91.8825960190068));
#11120=CARTESIAN_POINT('Ctrl Pts',(-0.102298089241641,-2.44974930528451,
91.8868884674728));
#11121=CARTESIAN_POINT('Ctrl Pts',(-0.0199650595547671,-2.45179356480318,
91.8911809159389));
#11122=CARTESIAN_POINT('Ctrl Pts',(0.0621063035833999,-2.44971285195943,
91.8954733644049));
#11123=CARTESIAN_POINT('Ctrl Pts',(0.14298947043929,-2.4476622628418,91.8997036685235));
#11124=CARTESIAN_POINT('Ctrl Pts',(0.223923433706141,-2.44159767315364,
91.9039339726421));
#11125=CARTESIAN_POINT('Ctrl Pts',(0.304477161884593,-2.43151062261523,
91.9081642767606));
#11126=CARTESIAN_POINT('Ctrl Pts',(0.384914985049505,-2.42143808586477,
91.9123884940913));
#11127=CARTESIAN_POINT('Ctrl Pts',(0.464973202064389,-2.40735464023245,
91.916612711422));
#11128=CARTESIAN_POINT('Ctrl Pts',(0.544221926826333,-2.38930382001985,
91.9208369287527));
#11129=CARTESIAN_POINT('Ctrl Pts',(0.623878580013838,-2.37116008420902,
91.9250828900084));
#11130=CARTESIAN_POINT('Ctrl Pts',(0.702716906930503,-2.34900802085591,
91.929328851264));
#11131=CARTESIAN_POINT('Ctrl Pts',(0.780306737278808,-2.32294460669154,
91.9335748125197));
#11132=CARTESIAN_POINT('Ctrl Pts',(0.857359574879215,-2.29706157524393,
91.9377913878314));
#11133=CARTESIAN_POINT('Ctrl Pts',(0.933180696082373,-2.26732131234926,
91.9420079631432));
#11134=CARTESIAN_POINT('Ctrl Pts',(1.00736195527359,-2.23386932049916,91.9462245384549));
#11135=CARTESIAN_POINT('Ctrl Pts',(1.08151855097934,-2.20042845063221,91.9504397118567));
#11136=CARTESIAN_POINT('Ctrl Pts',(1.15403594365693,-2.16327849348567,91.9546548852586));
#11137=CARTESIAN_POINT('Ctrl Pts',(1.22452614081644,-2.12261300769999,91.9588700586604));
#11138=CARTESIAN_POINT('Ctrl Pts',(1.29501452371866,-2.08194856855139,91.9630851235732));
#11139=CARTESIAN_POINT('Ctrl Pts',(1.36347541244613,-2.03776901403212,91.9673001884861));
#11140=CARTESIAN_POINT('Ctrl Pts',(1.42954685953016,-1.9903130473389,91.9715152533989));
#11141=CARTESIAN_POINT('Ctrl Pts',(1.49645949177866,-1.94225289749381,91.9757839821897));
#11142=CARTESIAN_POINT('Ctrl Pts',(1.56092100197455,-1.8908325881893,91.9800527109805));
#11143=CARTESIAN_POINT('Ctrl Pts',(1.62258868631153,-1.83634316102787,91.9843214397713));
#11144=CARTESIAN_POINT('Ctrl Pts',(1.68356995501418,-1.78246024917687,91.9885426538514));
#11145=CARTESIAN_POINT('Ctrl Pts',(1.74181899125051,-1.72557657784546,91.9927638679315));
#11146=CARTESIAN_POINT('Ctrl Pts',(1.79704179678401,-1.66601051335558,91.9969850820116));
#11147=CARTESIAN_POINT('Ctrl Pts',(1.85319699839329,-1.60543872008672,92.0012775681577));
#11148=CARTESIAN_POINT('Ctrl Pts',(1.90622251051549,-1.54209350109308,92.0055700543039));
#11149=CARTESIAN_POINT('Ctrl Pts',(1.95585333010915,-1.47634277899847,92.00986254045));
#11150=CARTESIAN_POINT('Ctrl Pts',(2.00548414970282,-1.41059205690386,92.0141550265961));
#11151=CARTESIAN_POINT('Ctrl Pts',(2.05172005205402,-1.3424362816015,92.0184475127423));
#11152=CARTESIAN_POINT('Ctrl Pts',(2.09434438701957,-1.27227034806272,92.0227399988884));
#11153=CARTESIAN_POINT('Ctrl Pts',(2.13634997159352,-1.20312296880493,92.0269701737402));
#11154=CARTESIAN_POINT('Ctrl Pts',(2.17500662817988,-1.13176262298302,92.031200348592));
#11155=CARTESIAN_POINT('Ctrl Pts',(2.21007417864682,-1.05854729458752,92.0354305234437));
#11156=CARTESIAN_POINT('Ctrl Pts',(2.24509125006682,-0.98543735821257,92.0396546090423));
#11157=CARTESIAN_POINT('Ctrl Pts',(2.27652927687386,-0.910478158374995,
92.0438786946408));
#11158=CARTESIAN_POINT('Ctrl Pts',(2.30419243730191,-0.834054831459353,
92.0481027802393));
#11159=CARTESIAN_POINT('Ctrl Pts',(2.33199907311781,-0.757235133836242,
92.0523487741199));
#11160=CARTESIAN_POINT('Ctrl Pts',(2.355991321361,-0.678936482874058,92.0565947680004));
#11161=CARTESIAN_POINT('Ctrl Pts',(2.37601814514858,-0.599573201473082,
92.0608407618809));
#11162=CARTESIAN_POINT('Ctrl Pts',(2.3959055669807,-0.5207623489913,92.0650572004083));
#11163=CARTESIAN_POINT('Ctrl Pts',(2.41188247855823,-0.440902097328574,
92.0692736389357));
#11164=CARTESIAN_POINT('Ctrl Pts',(2.42385059077933,-0.360414433088791,
92.073490077463));
#11165=CARTESIAN_POINT('Ctrl Pts',(2.43581471922367,-0.279953560449852,
92.0777051124817));
#11166=CARTESIAN_POINT('Ctrl Pts',(2.44377262978494,-0.198866149730817,
92.0819201475003));
#11167=CARTESIAN_POINT('Ctrl Pts',(2.44767735546206,-0.117583219713877,
92.086135182519));
#11168=CARTESIAN_POINT('Ctrl Pts',(2.45158197932559,-0.0363024091047066,
92.0903501076329));
#11169=CARTESIAN_POINT('Ctrl Pts',(2.45143360717036,0.0451734459503161,
92.0945650327469));
#11170=CARTESIAN_POINT('Ctrl Pts',(2.44723733078306,0.126410825571998,92.0987799578608));
#11171=CARTESIAN_POINT('Ctrl Pts',(2.44298732864705,0.2086883032809,92.1030488474867));
#11172=CARTESIAN_POINT('Ctrl Pts',(2.43458503926964,0.290720666427331,92.1073177371127));
#11173=CARTESIAN_POINT('Ctrl Pts',(2.42209000187813,0.372062189428047,92.1115866267386));
#11174=CARTESIAN_POINT('Ctrl Pts',(2.40973492603825,0.452492575837969,92.1158076989474));
#11175=CARTESIAN_POINT('Ctrl Pts',(2.39337848850781,0.532247072678141,92.1200287711562));
#11176=CARTESIAN_POINT('Ctrl Pts',(2.37312953875738,0.610906246716464,92.1242498433649));
#11177=CARTESIAN_POINT('Ctrl Pts',(2.35253651085689,0.690902028500942,92.1285426416995));
#11178=CARTESIAN_POINT('Ctrl Pts',(2.32791760380993,0.769764436858667,92.132835440034));
#11179=CARTESIAN_POINT('Ctrl Pts',(2.29943908779298,0.847071503197811,92.1371282383685));
#11180=CARTESIAN_POINT('Ctrl Pts',(2.27096057177603,0.924378569536955,92.1414210367031));
#11181=CARTESIAN_POINT('Ctrl Pts',(2.238622703912,1.00012986131522,92.1457138350376));
#11182=CARTESIAN_POINT('Ctrl Pts',(2.20264060816859,1.0739295140961,92.1500066333722));
#11183=CARTESIAN_POINT('Ctrl Pts',(2.16718280059893,1.14665384637717,92.1542368821705));
#11184=CARTESIAN_POINT('Ctrl Pts',(2.12805256397583,1.2177573626794,92.1584671309689));
#11185=CARTESIAN_POINT('Ctrl Pts',(2.08542120336568,1.28684445623893,92.1626973797673));
#11186=CARTESIAN_POINT('Ctrl Pts',(2.04285119845761,1.35583211860344,92.1669215403273));
#11187=CARTESIAN_POINT('Ctrl Pts',(1.99679031914875,1.42280872933492,92.1711457008873));
#11188=CARTESIAN_POINT('Ctrl Pts',(1.947456693669,1.48740131648583,92.1753698614473));
#11189=CARTESIAN_POINT('Ctrl Pts',(1.8978682960114,1.55232747721748,92.1796158367143));
#11190=CARTESIAN_POINT('Ctrl Pts',(1.84497345720986,1.61484448977382,92.1838618119814));
#11191=CARTESIAN_POINT('Ctrl Pts',(1.78903905334931,1.67460130048648,92.1881077872484));
#11192=CARTESIAN_POINT('Ctrl Pts',(1.73349273925385,1.73394350042237,92.1923243026583));
#11193=CARTESIAN_POINT('Ctrl Pts',(1.67494922751663,1.79056333542785,92.1965408180682));
#11194=CARTESIAN_POINT('Ctrl Pts',(1.61371037718443,1.84414995826458,92.2007573334782));
#11195=CARTESIAN_POINT('Ctrl Pts',(1.55249190279551,1.89771875127628,92.204972445931));
#11196=CARTESIAN_POINT('Ctrl Pts',(1.48858022051328,1.94825603017984,92.2091875583838));
#11197=CARTESIAN_POINT('Ctrl Pts',(1.42231253559508,1.99548923853001,92.2134026708367));
#11198=CARTESIAN_POINT('Ctrl Pts',(1.35604657149998,2.04272122033974,92.2176176738325));
#11199=CARTESIAN_POINT('Ctrl Pts',(1.28742510583333,2.08664903305199,92.2218326768284));
#11200=CARTESIAN_POINT('Ctrl Pts',(1.21681559436603,2.12704256170572,92.2260476798242));
#11201=CARTESIAN_POINT('Ctrl Pts',(1.14530489498446,2.16795163223308,92.2303164788268));
#11202=CARTESIAN_POINT('Ctrl Pts',(1.07175545809905,2.20523530393737,92.2345852778295));
#11203=CARTESIAN_POINT('Ctrl Pts',(0.99657439692856,2.23870268713522,92.2388540768321));
#11204=CARTESIAN_POINT('Ctrl Pts',(0.922232511514979,2.27179650528639,92.2430752272304));
#11205=CARTESIAN_POINT('Ctrl Pts',(0.84629570675226,2.30115869439306,92.2472963776287));
#11206=CARTESIAN_POINT('Ctrl Pts',(0.76917568667271,2.32665403810527,92.2515175280271));
#11207=CARTESIAN_POINT('Ctrl Pts',(0.690749863326335,2.35258107132008,92.2558101513319));
#11208=CARTESIAN_POINT('Ctrl Pts',(0.611100869247195,2.37450896412485,92.2601027746366));
#11209=CARTESIAN_POINT('Ctrl Pts',(0.53067350902201,2.39234944705456,92.2643953979414));
#11210=CARTESIAN_POINT('Ctrl Pts',(0.450246148796826,2.41018992998427,92.2686880212462));
#11211=CARTESIAN_POINT('Ctrl Pts',(0.369040925144304,2.42394298546787,92.2729806445509));
#11212=CARTESIAN_POINT('Ctrl Pts',(0.287507097297213,2.43357554207872,92.2772732678557));
#11213=CARTESIAN_POINT('Ctrl Pts',(0.207158160424407,2.44306811348724,92.2815035085796));
#11214=CARTESIAN_POINT('Ctrl Pts',(0.126187085558151,2.44859500635354,92.2857337493035));
#11215=CARTESIAN_POINT('Ctrl Pts',(0.0450192880203518,2.45008642984409,
92.2899639900274));
#11216=CARTESIAN_POINT('Ctrl Pts',(-0.0360316924424859,2.45157570687095,
92.294188142569));
#11217=CARTESIAN_POINT('Ctrl Pts',(-0.117278372142718,2.4490410406876,92.2984122951106));
#11218=CARTESIAN_POINT('Ctrl Pts',(-0.198289060329829,2.44246426761038,
92.3026364476522));
#11219=CARTESIAN_POINT('Ctrl Pts',(-0.279718302759078,2.4358535146185,92.3068824249309));
#11220=CARTESIAN_POINT('Ctrl Pts',(-0.36090863530143,2.42515870594721,92.3111284022095));
#11221=CARTESIAN_POINT('Ctrl Pts',(-0.441420445307773,2.41041453705878,
92.3153743794881));
#11222=CARTESIAN_POINT('Ctrl Pts',(-0.521373453947438,2.39577270175003,
92.3195908870789));
#11223=CARTESIAN_POINT('Ctrl Pts',(-0.600656865358687,2.37713762325674,
92.3238073946698));
#11224=CARTESIAN_POINT('Ctrl Pts',(-0.678845978104483,2.35459516435658,
92.3280239022606));
#11225=CARTESIAN_POINT('Ctrl Pts',(-0.757009076738581,2.33206020550371,
92.3322390069873));
#11226=CARTESIAN_POINT('Ctrl Pts',(-0.834078153080863,2.30562057658316,
92.336454111714));
#11227=CARTESIAN_POINT('Ctrl Pts',(-0.909641605973001,2.27541257768407,
92.3406692164407));
#11228=CARTESIAN_POINT('Ctrl Pts',(-0.98520309851335,2.24520536247474,92.3448842118145));
#11229=CARTESIAN_POINT('Ctrl Pts',(-1.05925861371348,2.21123014533049,92.3490992071882));
#11230=CARTESIAN_POINT('Ctrl Pts',(-1.13141589754081,2.17367162119579,92.3533142025619));
#11231=CARTESIAN_POINT('Ctrl Pts',(-1.20449441503888,2.13563358653601,92.3575830108767));
#11232=CARTESIAN_POINT('Ctrl Pts',(-1.27562544557686,2.09392030856426,92.3618518191915));
#11233=CARTESIAN_POINT('Ctrl Pts',(-1.34442828614813,2.04877105441403,92.3661206275063));
#11234=CARTESIAN_POINT('Ctrl Pts',(-1.4124628792332,2.00412593353385,92.3703417706196));
#11235=CARTESIAN_POINT('Ctrl Pts',(-1.47822067261861,1.95612151404289,92.3745629137329));
#11236=CARTESIAN_POINT('Ctrl Pts',(-1.54136531969538,1.90503102369498,92.3787840568463));
#11237=CARTESIAN_POINT('Ctrl Pts',(-1.60557951200315,1.85307516165161,92.3830766977618));
#11238=CARTESIAN_POINT('Ctrl Pts',(-1.66709083966827,1.79792805094266,92.3873693386773));
#11239=CARTESIAN_POINT('Ctrl Pts',(-1.72558454712129,1.73991615336378,92.3916619795928));
#11240=CARTESIAN_POINT('Ctrl Pts',(-1.78407825457432,1.6819042557849,92.3959546205083));
#11241=CARTESIAN_POINT('Ctrl Pts',(-1.83955405521674,1.62102798475228,92.4002472614238));
#11242=CARTESIAN_POINT('Ctrl Pts',(-1.89174122025013,1.55764739450446,92.4045399023394));
#11243=CARTESIAN_POINT('Ctrl Pts',(-1.94293841432775,1.49546911029234,92.408751113466));
#11244=CARTESIAN_POINT('Ctrl Pts',(-1.99116949696977,1.43063916186968,92.4129623245927));
#11245=CARTESIAN_POINT('Ctrl Pts',(-2.03614600671605,1.36347339150212,92.4171735357193));
#11246=CARTESIAN_POINT('Ctrl Pts',(-2.08106070506784,1.2963999273173,92.421378959362));
#11247=CARTESIAN_POINT('Ctrl Pts',(-2.12272944818328,1.22699739761737,92.4255843830046));
#11248=CARTESIAN_POINT('Ctrl Pts',(-2.16090346112967,1.15561519619543,92.4297898066472));
#11249=CARTESIAN_POINT('Ctrl Pts',(-2.19903697527135,1.08430872414048,92.4339907687565));
#11250=CARTESIAN_POINT('Ctrl Pts',(-2.2336828995433,1.01102716117391,92.4381917308658));
#11251=CARTESIAN_POINT('Ctrl Pts',(-2.26463614119372,0.936148170963978,
92.4423926929751));
#11252=CARTESIAN_POINT('Ctrl Pts',(-2.29556969780512,0.861316800834073,
92.4465909834384));
#11253=CARTESIAN_POINT('Ctrl Pts',(-2.32281505157425,0.784890451273078,
92.4507892739017));
#11254=CARTESIAN_POINT('Ctrl Pts',(-2.34621401464293,0.70726943062253,92.4549875643651));
#11255=CARTESIAN_POINT('Ctrl Pts',(-2.36960328362365,0.629680568021022,
92.459184115495));
#11256=CARTESIAN_POINT('Ctrl Pts',(-2.38914919410262,0.550898467200658,
92.463380666625));
#11257=CARTESIAN_POINT('Ctrl Pts',(-2.40474302292967,0.471339838832957,
92.467577217755));
#11258=CARTESIAN_POINT('Ctrl Pts',(-2.42034235417786,0.391753137495906,
92.4717752496753));
#11259=CARTESIAN_POINT('Ctrl Pts',(-2.43198671970401,0.311389820912447,
92.4759732815957));
#11260=CARTESIAN_POINT('Ctrl Pts',(-2.4396184727168,0.230677171776809,92.480171313516));
#11261=CARTESIAN_POINT('Ctrl Pts',(-2.44693557045041,0.153292285096926,
92.4841962616241));
#11262=CARTESIAN_POINT('Ctrl Pts',(-2.45056441392189,0.0755867030845429,
92.4882212097322));
#11263=CARTESIAN_POINT('Ctrl Pts',(-2.45049913396412,-0.00206020414336211,
92.4922461578402));
#11264=CARTESIAN_POINT('',(-2.45049997091768,-0.0003775346874681,93.2922461577912));
#11265=CARTESIAN_POINT('Ctrl Pts',(-2.45049913396335,-0.00206020505177728,
92.4922461578873));
#11266=CARTESIAN_POINT('Ctrl Pts',(-2.45041769687901,-0.0989250799796706,
92.497267299218));
#11267=CARTESIAN_POINT('Ctrl Pts',(-2.44458900316372,-0.195541487778647,
92.5022884405487));
#11268=CARTESIAN_POINT('Ctrl Pts',(-2.43312414260481,-0.291302517451572,
92.5073095818795));
#11269=CARTESIAN_POINT('Ctrl Pts',(-2.42151339890458,-0.388282046010988,
92.5123946140762));
#11270=CARTESIAN_POINT('Ctrl Pts',(-2.40412222586561,-0.484384242648835,
92.517479646273));
#11271=CARTESIAN_POINT('Ctrl Pts',(-2.38111506273585,-0.579000265986519,
92.5225646784698));
#11272=CARTESIAN_POINT('Ctrl Pts',(-2.36717683943469,-0.636320642849597,
92.5256452979209));
#11273=CARTESIAN_POINT('Ctrl Pts',(-2.35117837970355,-0.693095985603747,
92.528725917372));
#11274=CARTESIAN_POINT('Ctrl Pts',(-2.33316468060956,-0.74919478318798,
92.5318065368231));
#11275=CARTESIAN_POINT('Ctrl Pts',(-2.30842868017434,-0.82622837158192,
92.5360367731385));
#11276=CARTESIAN_POINT('Ctrl Pts',(-2.27982683123968,-0.902180851879758,
92.540267009454));
#11277=CARTESIAN_POINT('Ctrl Pts',(-2.24747233236836,-0.976636250217406,
92.5444972457694));
#11278=CARTESIAN_POINT('Ctrl Pts',(-2.21516439938128,-1.05098448937841,
92.5487213937602));
#11279=CARTESIAN_POINT('Ctrl Pts',(-2.17911472678708,-1.12383950280866,
92.552945541751));
#11280=CARTESIAN_POINT('Ctrl Pts',(-2.13948608332324,-1.19480105007744,
92.5571696897417));
#11281=CARTESIAN_POINT('Ctrl Pts',(-2.09965263892713,-1.26612932680668,
92.5614156681403));
#11282=CARTESIAN_POINT('Ctrl Pts',(-2.05620326646652,-1.33554405505853,
92.5656616465388));
#11283=CARTESIAN_POINT('Ctrl Pts',(-2.00935211029651,-1.4026597402246,92.5699076249373));
#11284=CARTESIAN_POINT('Ctrl Pts',(-1.96282619586518,-1.46930950685375,
92.5741241276621));
#11285=CARTESIAN_POINT('Ctrl Pts',(-1.91294584845879,-1.53369166287166,
92.5783406303868));
#11286=CARTESIAN_POINT('Ctrl Pts',(-1.8599655640961,-1.59545553067977,92.5825571331115));
#11287=CARTESIAN_POINT('Ctrl Pts',(-1.80700290805457,-1.65719884757331,
92.5867722328641));
#11288=CARTESIAN_POINT('Ctrl Pts',(-1.7509426659481,-1.71632525347441,92.5909873326167));
#11289=CARTESIAN_POINT('Ctrl Pts',(-1.69207977436681,-1.77251693565358,
92.5952024323692));
#11290=CARTESIAN_POINT('Ctrl Pts',(-1.63321841129507,-1.82870715868726,
92.5994174226671));
#11291=CARTESIAN_POINT('Ctrl Pts',(-1.57155488066292,-1.88196248907348,
92.603632412965));
#11292=CARTESIAN_POINT('Ctrl Pts',(-1.50742010717977,-1.93200281326662,
92.6078474032628));
#11293=CARTESIAN_POINT('Ctrl Pts',(-1.4424663588154,-1.9826821319761,92.6121162172665));
#11294=CARTESIAN_POINT('Ctrl Pts',(-1.37497818012107,-2.03006343782352,
92.6163850312701));
#11295=CARTESIAN_POINT('Ctrl Pts',(-1.30533134409059,-2.07389978835397,
92.6206538452738));
#11296=CARTESIAN_POINT('Ctrl Pts',(-1.23646235739739,-2.11724655345381,
92.624874983111));
#11297=CARTESIAN_POINT('Ctrl Pts',(-1.16548313209144,-2.15712697598517,
92.6290961209483));
#11298=CARTESIAN_POINT('Ctrl Pts',(-1.09278190898211,-2.19334856997273,
92.6333172587855));
#11299=CARTESIAN_POINT('Ctrl Pts',(-1.01884898636047,-2.230183827909,92.6376099108724));
#11300=CARTESIAN_POINT('Ctrl Pts',(-0.943135637492417,-2.2632349308766,
92.6419025629592));
#11301=CARTESIAN_POINT('Ctrl Pts',(-0.866069566338952,-2.29235114157091,
92.6461952150461));
#11302=CARTESIAN_POINT('Ctrl Pts',(-0.789003495185486,-2.32146735226522,
92.6504878671329));
#11303=CARTESIAN_POINT('Ctrl Pts',(-0.710585196862659,-2.34664858167637,
92.6547805192198));
#11304=CARTESIAN_POINT('Ctrl Pts',(-0.631254648110631,-2.36779809511679,
92.6590731713066));
#11305=CARTESIAN_POINT('Ctrl Pts',(-0.553077606236169,-2.38864008378152,
92.6633034060299));
#11306=CARTESIAN_POINT('Ctrl Pts',(-0.473719831384154,-2.40564548227121,
92.6675336407531));
#11307=CARTESIAN_POINT('Ctrl Pts',(-0.393592456264391,-2.41868460704817,
92.6717638754764));
#11308=CARTESIAN_POINT('Ctrl Pts',(-0.31358040377632,-2.43170496537756,
92.6759880218709));
#11309=CARTESIAN_POINT('Ctrl Pts',(-0.232801406065574,-2.44077031305807,
92.6802121682654));
#11310=CARTESIAN_POINT('Ctrl Pts',(-0.151680162123258,-2.44580117311654,
92.68443631466));
#11311=CARTESIAN_POINT('Ctrl Pts',(-0.0701396449149185,-2.45085803505844,
92.688682293457));
#11312=CARTESIAN_POINT('Ctrl Pts',(0.0117462071124492,-2.45183845801596,
92.6929282722542));
#11313=CARTESIAN_POINT('Ctrl Pts',(0.0935373210967758,-2.44871415636085,
92.6971742510512));
#11314=CARTESIAN_POINT('Ctrl Pts',(0.174760601070809,-2.44561154513948,
92.701390752182));
#11315=CARTESIAN_POINT('Ctrl Pts',(0.25588998330297,-2.43846104083498,92.7056072533127));
#11316=CARTESIAN_POINT('Ctrl Pts',(0.336492867185838,-2.4272871277072,92.7098237544435));
#11317=CARTESIAN_POINT('Ctrl Pts',(0.417068931855568,-2.41611693250541,
92.7140388526065));
#11318=CARTESIAN_POINT('Ctrl Pts',(0.497118385644902,-2.40092605074118,
92.7182539507696));
#11319=CARTESIAN_POINT('Ctrl Pts',(0.576214409324468,-2.38179075581522,
92.7224690489326));
#11320=CARTESIAN_POINT('Ctrl Pts',(0.655308379219406,-2.36265595775084,
92.7266840376477));
#11321=CARTESIAN_POINT('Ctrl Pts',(0.733448516334295,-2.33957706057718,
92.7308990263627));
#11322=CARTESIAN_POINT('Ctrl Pts',(0.810220256939178,-2.31268099513215,
92.7351140150777));
#11323=CARTESIAN_POINT('Ctrl Pts',(0.887972404943038,-2.28544145562546,
92.7393828309704));
#11324=CARTESIAN_POINT('Ctrl Pts',(0.964320490939832,-2.25428670631132,
92.7436516468631));
#11325=CARTESIAN_POINT('Ctrl Pts',(1.03885360603746,-2.21939934108825,92.7479204627558));
#11326=CARTESIAN_POINT('Ctrl Pts',(1.1125542398088,-2.18490164266005,92.7521415990432));
#11327=CARTESIAN_POINT('Ctrl Pts',(1.18447985772426,-2.14675456991049,92.7563627353305));
#11328=CARTESIAN_POINT('Ctrl Pts',(1.25425862109093,-2.10518064816753,92.7605838716178));
#11329=CARTESIAN_POINT('Ctrl Pts',(1.32521965755015,-2.06290233261395,92.7648765273132));
#11330=CARTESIAN_POINT('Ctrl Pts',(1.39395999724159,-2.01708024633689,92.7691691830086));
#11331=CARTESIAN_POINT('Ctrl Pts',(1.46012158338997,-1.96799268589057,92.773461838704));
#11332=CARTESIAN_POINT('Ctrl Pts',(1.52628316953835,-1.91890512544425,92.7777544943994));
#11333=CARTESIAN_POINT('Ctrl Pts',(1.58986565956419,-1.86655245921086,92.7820471500948));
#11334=CARTESIAN_POINT('Ctrl Pts',(1.65054978974358,-1.81125250629983,92.7863398057902));
#11335=CARTESIAN_POINT('Ctrl Pts',(1.71035147192646,-1.75675670650938,92.7905700391454));
#11336=CARTESIAN_POINT('Ctrl Pts',(1.7675641112248,-1.69919327125266,92.7948002725007));
#11337=CARTESIAN_POINT('Ctrl Pts',(1.82185632257683,-1.63883793887219,92.7990305058559));
#11338=CARTESIAN_POINT('Ctrl Pts',(1.87607039392428,-1.57856947283646,92.8032546508525));
#11339=CARTESIAN_POINT('Ctrl Pts',(1.92737207662859,-1.5155174329386,92.807478795849));
#11340=CARTESIAN_POINT('Ctrl Pts',(1.97546488571195,-1.44999611562207,92.8117029408456));
#11341=CARTESIAN_POINT('Ctrl Pts',(2.02380628129709,-1.38413612573941,92.8159489199884));
#11342=CARTESIAN_POINT('Ctrl Pts',(2.06890517990798,-1.31578157587251,92.8201948991313));
#11343=CARTESIAN_POINT('Ctrl Pts',(2.11049984743144,-1.24528737405944,92.8244408782741));
#11344=CARTESIAN_POINT('Ctrl Pts',(2.1518057267086,-1.17528260750641,92.8286573779442));
#11345=CARTESIAN_POINT('Ctrl Pts',(2.18965564044924,-1.10316821168101,92.8328738776142));
#11346=CARTESIAN_POINT('Ctrl Pts',(2.2238362864575,-1.02932134002698,92.8370903772842));
#11347=CARTESIAN_POINT('Ctrl Pts',(2.2580055592786,-0.955499040006019,92.8413054739661));
#11348=CARTESIAN_POINT('Ctrl Pts',(2.28850779359906,-0.879945830712804,
92.8455205706481));
#11349=CARTESIAN_POINT('Ctrl Pts',(2.31517637954871,-0.803062003571175,
92.84973566733));
#11350=CARTESIAN_POINT('Ctrl Pts',(2.34184427291244,-0.72618017311041,92.8539506545454));
#11351=CARTESIAN_POINT('Ctrl Pts',(2.36467856441186,-0.647968233352739,
92.8581656417608));
#11352=CARTESIAN_POINT('Ctrl Pts',(2.38356188492226,-0.568843555598427,
92.8623806289763));
#11353=CARTESIAN_POINT('Ctrl Pts',(2.40268636786249,-0.488708361736159,
92.8666494465844));
#11354=CARTESIAN_POINT('Ctrl Pts',(2.41775811482212,-0.407637422049397,
92.8709182641925));
#11355=CARTESIAN_POINT('Ctrl Pts',(2.42870855794048,-0.326075130279298,
92.8751870818006));
#11356=CARTESIAN_POINT('Ctrl Pts',(2.43953668420367,-0.245423892328883,
92.879408216558));
#11357=CARTESIAN_POINT('Ctrl Pts',(2.44633514093541,-0.164292698917119,
92.8836293513154));
#11358=CARTESIAN_POINT('Ctrl Pts',(2.44909007639386,-0.0831146660291083,
92.8878504860727));
#11359=CARTESIAN_POINT('Ctrl Pts',(2.45189169237209,-0.000561126227321199,
92.8921431451062));
#11360=CARTESIAN_POINT('Ctrl Pts',(2.45051149473331,0.0820403524250221,
92.8964358041397));
#11361=CARTESIAN_POINT('Ctrl Pts',(2.44498999982381,0.164238091688756,92.9007284631733));
#11362=CARTESIAN_POINT('Ctrl Pts',(2.43946850491431,0.246435830952492,92.9050211222068));
#11363=CARTESIAN_POINT('Ctrl Pts',(2.42980583740192,0.328229343459863,92.9093137812403));
#11364=CARTESIAN_POINT('Ctrl Pts',(2.41609673601504,0.409178215717133,92.9136064402738));
#11365=CARTESIAN_POINT('Ctrl Pts',(2.40258699467626,0.488949915918327,92.9178366747408));
#11366=CARTESIAN_POINT('Ctrl Pts',(2.38509682483617,0.568202252882996,92.9220669092078));
#11367=CARTESIAN_POINT('Ctrl Pts',(2.36367901183605,0.64650736964536,92.9262971436748));
#11368=CARTESIAN_POINT('Ctrl Pts',(2.34229202430589,0.724699786197636,92.9305212898001));
#11369=CARTESIAN_POINT('Ctrl Pts',(2.3169887420444,0.801947245197778,92.9347454359253));
#11370=CARTESIAN_POINT('Ctrl Pts',(2.28787325634421,0.877830400991535,92.9389695820505));
#11371=CARTESIAN_POINT('Ctrl Pts',(2.25860728561363,0.954105763156957,92.9432155609133));
#11372=CARTESIAN_POINT('Ctrl Pts',(2.22548966609151,1.02900220793019,92.9474615397761));
#11373=CARTESIAN_POINT('Ctrl Pts',(2.18867744163181,1.10210766556268,92.9517075186389));
#11374=CARTESIAN_POINT('Ctrl Pts',(2.15212078884102,1.17470558299384,92.9559240194704));
#11375=CARTESIAN_POINT('Ctrl Pts',(2.11192088078324,1.24553688170727,92.9601405203019));
#11376=CARTESIAN_POINT('Ctrl Pts',(2.06827966112225,1.31421820615453,92.9643570211334));
#11377=CARTESIAN_POINT('Ctrl Pts',(2.02465296243216,1.38287667790607,92.9685721189866));
#11378=CARTESIAN_POINT('Ctrl Pts',(1.97758747525721,1.44938620366654,92.9727872168398));
#11379=CARTESIAN_POINT('Ctrl Pts',(1.92732985321778,1.51339019651098,92.9770023146929));
#11380=CARTESIAN_POINT('Ctrl Pts',(1.87707353627578,1.57739252729018,92.9812173030878));
#11381=CARTESIAN_POINT('Ctrl Pts',(1.82362553740962,1.63888908930236,92.9854322914827));
#11382=CARTESIAN_POINT('Ctrl Pts',(1.76727350183467,1.6975554835448,92.9896472798776));
#11383=CARTESIAN_POINT('Ctrl Pts',(1.71020181809974,1.75697108164897,92.9939160961176));
#11384=CARTESIAN_POINT('Ctrl Pts',(1.65015172398301,1.81348334779756,92.9981849123576));
#11385=CARTESIAN_POINT('Ctrl Pts',(1.58745998202576,1.86679432596812,93.0024537285975));
#11386=CARTESIAN_POINT('Ctrl Pts',(1.52546847183818,1.91950985026515,93.0066748645425));
#11387=CARTESIAN_POINT('Ctrl Pts',(1.46089444274103,1.96909500614548,93.0108960004875));
#11388=CARTESIAN_POINT('Ctrl Pts',(1.39409475467345,2.01530396342387,93.0151171364325));
#11389=CARTESIAN_POINT('Ctrl Pts',(1.32616325201592,2.0622958580714,93.01940979282));
#11390=CARTESIAN_POINT('Ctrl Pts',(1.25593039761607,2.10579581939649,93.0237024492075));
#11391=CARTESIAN_POINT('Ctrl Pts',(1.18379806120738,2.14559371743153,93.027995105595));
#11392=CARTESIAN_POINT('Ctrl Pts',(1.11166572479868,2.18539161546657,93.0322877619825));
#11393=CARTESIAN_POINT('Ctrl Pts',(1.03763438377147,2.22148729157579,93.03658041837));
#11394=CARTESIAN_POINT('Ctrl Pts',(0.962125748599477,2.25372231960415,93.0408730747575));
#11395=CARTESIAN_POINT('Ctrl Pts',(0.887715131358506,2.28548859808219,93.045103308964));
#11396=CARTESIAN_POINT('Ctrl Pts',(0.811589274561371,2.31362562066973,93.0493335431706));
#11397=CARTESIAN_POINT('Ctrl Pts',(0.734136643297586,2.33794645767771,93.0535637773772));
#11398=CARTESIAN_POINT('Ctrl Pts',(0.656795485347559,2.36223229104217,93.0577879232403));
#11399=CARTESIAN_POINT('Ctrl Pts',(0.578131785408882,2.38271270881352,93.0620120691033));
#11400=CARTESIAN_POINT('Ctrl Pts',(0.498554588782068,2.39924854319104,93.0662362149664));
#11401=CARTESIAN_POINT('Ctrl Pts',(0.418566086730034,2.41586984524873,93.0704821938945));
#11402=CARTESIAN_POINT('Ctrl Pts',(0.337655054348106,2.42850547916418,93.0747281728226));
#11403=CARTESIAN_POINT('Ctrl Pts',(0.256253046795857,2.43706475621963,93.0789741517507));
#11404=CARTESIAN_POINT('Ctrl Pts',(0.175416185187573,2.44556460917908,93.0831906523178));
#11405=CARTESIAN_POINT('Ctrl Pts',(0.094095612890168,2.45004447821745,93.0874071528849));
#11406=CARTESIAN_POINT('Ctrl Pts',(0.012723006264846,2.4504669708265,93.0916236534519));
#11407=CARTESIAN_POINT('Ctrl Pts',(-0.0686225248214064,2.45088932285733,
93.0958387510404));
#11408=CARTESIAN_POINT('Ctrl Pts',(-0.150019591046555,2.44725697694501,
93.1000538486288));
#11409=CARTESIAN_POINT('Ctrl Pts',(-0.231034860726386,2.43958462512149,
93.1042689462173));
#11410=CARTESIAN_POINT('Ctrl Pts',(-0.312048026591457,2.43191247253456,
93.1084839343476));
#11411=CARTESIAN_POINT('Ctrl Pts',(-0.392678952610482,2.420200567542,93.1126989224778));
#11412=CARTESIAN_POINT('Ctrl Pts',(-0.472499221088961,2.40451548883976,
93.1169139106081));
#11413=CARTESIAN_POINT('Ctrl Pts',(-0.553338851663316,2.38863010042917,
93.1211827271608));
#11414=CARTESIAN_POINT('Ctrl Pts',(-0.633346489175556,2.36866941352884,
93.1254515437136));
#11415=CARTESIAN_POINT('Ctrl Pts',(-0.712089403515037,2.3447556229598,93.1297203602664));
#11416=CARTESIAN_POINT('Ctrl Pts',(-0.789952792916594,2.32110893928339,
93.1339414959497));
#11417=CARTESIAN_POINT('Ctrl Pts',(-0.866579149086681,2.29359723875549,
93.1381626316331));
#11418=CARTESIAN_POINT('Ctrl Pts',(-0.941568725504837,2.26238780609143,
93.1423837673165));
#11419=CARTESIAN_POINT('Ctrl Pts',(-1.01782889654489,2.23064957277014,93.1466764243039));
#11420=CARTESIAN_POINT('Ctrl Pts',(-1.09239585355719,2.19508735535688,93.1509690812914));
#11421=CARTESIAN_POINT('Ctrl Pts',(-1.16487554585739,2.1559256046217,93.1552617382788));
#11422=CARTESIAN_POINT('Ctrl Pts',(-1.23735523815759,2.11676385388653,93.1595543952663));
#11423=CARTESIAN_POINT('Ctrl Pts',(-1.30774727418056,2.07400288565244,93.1638470522537));
#11424=CARTESIAN_POINT('Ctrl Pts',(-1.37569037043724,2.02791179657456,93.1681397092411));
#11425=CARTESIAN_POINT('Ctrl Pts',(-1.44236725713998,1.98267967596525,93.1723523668823));
#11426=CARTESIAN_POINT('Ctrl Pts',(-1.50694183239721,1.9340667131829,93.1765650245233));
#11427=CARTESIAN_POINT('Ctrl Pts',(-1.56904854747722,1.88229564778215,93.1807776821644));
#11428=CARTESIAN_POINT('Ctrl Pts',(-1.63106572752764,1.83059921720739,93.1849842667034));
#11429=CARTESIAN_POINT('Ctrl Pts',(-1.69062175416469,1.77575402204514,93.1891908512423));
#11430=CARTESIAN_POINT('Ctrl Pts',(-1.74737996150074,1.71802605339549,93.1933974357812));
#11431=CARTESIAN_POINT('Ctrl Pts',(-1.80407245956903,1.66036491671123,93.1975991503356));
#11432=CARTESIAN_POINT('Ctrl Pts',(-1.85797324684742,1.59982797090653,93.2018008648901));
#11433=CARTESIAN_POINT('Ctrl Pts',(-1.90877985805194,1.5367204376513,93.2060025794445));
#11434=CARTESIAN_POINT('Ctrl Pts',(-1.95955446527867,1.47365265694098,93.210201647265));
#11435=CARTESIAN_POINT('Ctrl Pts',(-2.00723847084698,1.40801786702482,93.2144007150856));
#11436=CARTESIAN_POINT('Ctrl Pts',(-2.05156816015713,1.34015608577116,93.2185997829061));
#11437=CARTESIAN_POINT('Ctrl Pts',(-2.09588382052396,1.27231578062297,93.2227975218546));
#11438=CARTESIAN_POINT('Ctrl Pts',(-2.13684701574996,1.20225027628605,93.2269952608031));
#11439=CARTESIAN_POINT('Ctrl Pts',(-2.17423691200447,1.13032920004628,93.2311929997516));
#11440=CARTESIAN_POINT('Ctrl Pts',(-2.21162669527163,1.05840834114253,93.2353907260151));
#11441=CARTESIAN_POINT('Ctrl Pts',(-2.24544298590763,0.984632338829554,
93.2395884522786));
#11442=CARTESIAN_POINT('Ctrl Pts',(-2.27551124887344,0.909394747208525,
93.2437861785421));
#11443=CARTESIAN_POINT('Ctrl Pts',(-2.30560923408867,0.83408278379999,93.2479880542261));
#11444=CARTESIAN_POINT('Ctrl Pts',(-2.33195161769914,0.757306782595229,
93.2521899299101));
#11445=CARTESIAN_POINT('Ctrl Pts',(-2.35441257145108,0.679478986719307,
93.2563918055941));
#11446=CARTESIAN_POINT('Ctrl Pts',(-2.37688462206551,0.601612739922845,
93.2605957572201));
#11447=CARTESIAN_POINT('Ctrl Pts',(-2.39547131671404,0.52269412116537,93.264799708846));
#11448=CARTESIAN_POINT('Ctrl Pts',(-2.41009776619079,0.443146710923332,
93.269003660472));
#11449=CARTESIAN_POINT('Ctrl Pts',(-2.42475001582833,0.363458983923097,
93.2732150276111));
#11450=CARTESIAN_POINT('Ctrl Pts',(-2.43542800427714,0.283140716005997,
93.2774263947502));
#11451=CARTESIAN_POINT('Ctrl Pts',(-2.44210867626308,0.202621477935082,
93.2816377618892));
#11452=CARTESIAN_POINT('Ctrl Pts',(-2.44771819378852,0.13501239938064,93.2851738938566));
#11453=CARTESIAN_POINT('Ctrl Pts',(-2.4505103917333,0.0672618352071985,
93.2887100258239));
#11454=CARTESIAN_POINT('Ctrl Pts',(-2.45049997091768,-0.00037753468746127,
93.2922461577912));
#11455=CARTESIAN_POINT('',(-2.45049896913575,0.00224772432606832,94.0922461578025));
#11456=CARTESIAN_POINT('Ctrl Pts',(-2.45049997091754,-0.000377535622314954,
93.2922461578401));
#11457=CARTESIAN_POINT('Ctrl Pts',(-2.45049686660316,-0.020526951609039,
93.293299553135));
#11458=CARTESIAN_POINT('Ctrl Pts',(-2.45024524718698,-0.0406742062679038,
93.2943529484299));
#11459=CARTESIAN_POINT('Ctrl Pts',(-2.44974524247741,-0.0608152691294603,
93.2954063437248));
#11460=CARTESIAN_POINT('Ctrl Pts',(-2.44773731911088,-0.141697928777799,
93.2996365779332));
#11461=CARTESIAN_POINT('Ctrl Pts',(-2.44171557726676,-0.22263356198852,
93.3038668121415));
#11462=CARTESIAN_POINT('Ctrl Pts',(-2.43167131269257,-0.303191155919789,
93.3080970463499));
#11463=CARTESIAN_POINT('Ctrl Pts',(-2.42164150427865,-0.383632807715177,
93.3123211922137));
#11464=CARTESIAN_POINT('Ctrl Pts',(-2.40760072815549,-0.46369704314202,
93.3165453380776));
#11465=CARTESIAN_POINT('Ctrl Pts',(-2.38959227524804,-0.542953964968405,
93.3207694839414));
#11466=CARTESIAN_POINT('Ctrl Pts',(-2.37149074323843,-0.622620536816421,
93.3250154628692));
#11467=CARTESIAN_POINT('Ctrl Pts',(-2.34938040888767,-0.701470949068802,
93.329261441797));
#11468=CARTESIAN_POINT('Ctrl Pts',(-2.32335801214661,-0.779074962628212,
93.3335074207248));
#11469=CARTESIAN_POINT('Ctrl Pts',(-2.29751627990227,-0.856140198372773,
93.33772392129));
#11470=CARTESIAN_POINT('Ctrl Pts',(-2.26781678328248,-0.931975840389033,
93.3419404218552));
#11471=CARTESIAN_POINT('Ctrl Pts',(-2.23440479463291,-1.00617367473089,
93.3461569224204));
#11472=CARTESIAN_POINT('Ctrl Pts',(-2.20100392333932,-1.08034682081651,
93.350372020006));
#11473=CARTESIAN_POINT('Ctrl Pts',(-2.16389320388801,-1.1528828175805,93.3545871175917));
#11474=CARTESIAN_POINT('Ctrl Pts',(-2.12326597596168,-1.22339357744084,
93.3588022151773));
#11475=CARTESIAN_POINT('Ctrl Pts',(-2.08263980305785,-1.29390250625235,
93.3630172033038));
#11476=CARTESIAN_POINT('Ctrl Pts',(-2.03849753640268,-1.36238590019093,
93.3672321914303));
#11477=CARTESIAN_POINT('Ctrl Pts',(-1.9910776745944,-1.42848169177338,93.3714471795567));
#11478=CARTESIAN_POINT('Ctrl Pts',(-1.94305222706854,-1.49542157411968,
93.375715996111));
#11479=CARTESIAN_POINT('Ctrl Pts',(-1.89166514559194,-1.55991203050682,
93.3799848126653));
#11480=CARTESIAN_POINT('Ctrl Pts',(-1.83720731224929,-1.6216101694975,93.3842536292196));
#11481=CARTESIAN_POINT('Ctrl Pts',(-1.78335774989377,-1.68261916634639,
93.3884747648968));
#11482=CARTESIAN_POINT('Ctrl Pts',(-1.72650606536615,-1.74089761948361,
93.392695900574));
#11483=CARTESIAN_POINT('Ctrl Pts',(-1.66697045874657,-1.79615136880671,
93.3969170362512));
#11484=CARTESIAN_POINT('Ctrl Pts',(-1.60642610347734,-1.85234131661981,
93.4012096932441));
#11485=CARTESIAN_POINT('Ctrl Pts',(-1.54310641699523,-1.90540278796908,
93.4055023502369));
#11486=CARTESIAN_POINT('Ctrl Pts',(-1.4773792360893,-1.95507054675073,93.4097950072298));
#11487=CARTESIAN_POINT('Ctrl Pts',(-1.41165205518336,-2.00473830553238,
93.4140876642226));
#11488=CARTESIAN_POINT('Ctrl Pts',(-1.34351782977679,-2.05101212672075,
93.4183803212155));
#11489=CARTESIAN_POINT('Ctrl Pts',(-1.27337140062822,-2.09367512428794,
93.4226729782083));
#11490=CARTESIAN_POINT('Ctrl Pts',(-1.20424502459612,-2.13571772643152,
93.426903212378));
#11491=CARTESIAN_POINT('Ctrl Pts',(-1.13290389007825,-2.1744124353288,93.4311334465477));
#11492=CARTESIAN_POINT('Ctrl Pts',(-1.05970587076521,-2.20951888823467,
93.4353636807174));
#11493=CARTESIAN_POINT('Ctrl Pts',(-0.986613201362138,-2.24457481434092,
93.4395878265421));
#11494=CARTESIAN_POINT('Ctrl Pts',(-0.91166937073539,-2.27605254165549,
93.4438119723669));
#11495=CARTESIAN_POINT('Ctrl Pts',(-0.835259426902683,-2.30375605040338,
93.4480361181917));
#11496=CARTESIAN_POINT('Ctrl Pts',(-0.758454547149536,-2.33160274877004,
93.4522820971292));
#11497=CARTESIAN_POINT('Ctrl Pts',(-0.680168759841889,-2.35563584966458,
93.4565280760667));
#11498=CARTESIAN_POINT('Ctrl Pts',(-0.600816299475869,-2.37570411126557,
93.4607740550042));
#11499=CARTESIAN_POINT('Ctrl Pts',(-0.522014756707144,-2.39563304563698,
93.4649905555298));
#11500=CARTESIAN_POINT('Ctrl Pts',(-0.442161762012838,-2.41165190392492,
93.4692070560554));
#11501=CARTESIAN_POINT('Ctrl Pts',(-0.361679262256269,-2.42366217968878,
93.473423556581));
#11502=CARTESIAN_POINT('Ctrl Pts',(-0.281223541890074,-2.43566845920669,
93.4776386541268));
#11503=CARTESIAN_POINT('Ctrl Pts',(-0.200139192128692,-2.44366873625792,
93.4818537516727));
#11504=CARTESIAN_POINT('Ctrl Pts',(-0.118857218081033,-2.44761582191937,
93.4860688492186));
#11505=CARTESIAN_POINT('Ctrl Pts',(-0.0375773547942155,-2.45156280508142,
93.4902838373053));
#11506=CARTESIAN_POINT('Ctrl Pts',(0.0438996578856404,-2.45145678462448,
93.4944988253919));
#11507=CARTESIAN_POINT('Ctrl Pts',(0.125140287105287,-2.4473026291293,93.4987138134786));
#11508=CARTESIAN_POINT('Ctrl Pts',(0.207418419230373,-2.44309542199682,
93.5029826300797));
#11509=CARTESIAN_POINT('Ctrl Pts',(0.28945359834815,-2.43473595704496,93.5072514466808));
#11510=CARTESIAN_POINT('Ctrl Pts',(0.370800100238823,-2.42228353742143,
93.5115202632819));
#11511=CARTESIAN_POINT('Ctrl Pts',(0.451237994439687,-2.40997020631386,
93.5157413989195));
#11512=CARTESIAN_POINT('Ctrl Pts',(0.531002070396874,-2.39365505375892,
93.5199625345571));
#11513=CARTESIAN_POINT('Ctrl Pts',(0.609672827741539,-2.37344671166505,
93.5241836701947));
#11514=CARTESIAN_POINT('Ctrl Pts',(0.689676554872338,-2.35289596649349,
93.5284763272776));
#11515=CARTESIAN_POINT('Ctrl Pts',(0.768549090080892,-2.32831902775211,
93.5327689843605));
#11516=CARTESIAN_POINT('Ctrl Pts',(0.845868426999605,-2.29988192179625,
93.5370616414434));
#11517=CARTESIAN_POINT('Ctrl Pts',(0.923187763918315,-2.27144481584039,
93.5413542985263));
#11518=CARTESIAN_POINT('Ctrl Pts',(0.998953469984371,-2.23914779949084,
93.5456469556092));
#11519=CARTESIAN_POINT('Ctrl Pts',(1.07276961171991,-2.20320575756562,93.5499396126921));
#11520=CARTESIAN_POINT('Ctrl Pts',(1.1455123345218,-2.16778637731588,93.5541698468512));
#11521=CARTESIAN_POINT('Ctrl Pts',(1.2166361949348,-2.12869373847066,93.5584000810103));
#11522=CARTESIAN_POINT('Ctrl Pts',(1.28574549763879,-2.08609893468684,93.5626303151694));
#11523=CARTESIAN_POINT('Ctrl Pts',(1.3547553350938,-2.04356543528027,93.5668544609833));
#11524=CARTESIAN_POINT('Ctrl Pts',(1.42175598060787,-1.99754002349982,93.5710786067972));
#11525=CARTESIAN_POINT('Ctrl Pts',(1.48637434874918,-1.9482406282029,93.5753027526111));
#11526=CARTESIAN_POINT('Ctrl Pts',(1.55132670654323,-1.89868642164429,93.5795487315513));
#11527=CARTESIAN_POINT('Ctrl Pts',(1.61387165934902,-1.84582449470403,93.5837947104914));
#11528=CARTESIAN_POINT('Ctrl Pts',(1.67365800960765,-1.78992153930729,93.5880406894316));
#11529=CARTESIAN_POINT('Ctrl Pts',(1.73302928302839,-1.73440669962348,93.5922571899457));
#11530=CARTESIAN_POINT('Ctrl Pts',(1.78967979246899,-1.67589324537274,93.5964736904597));
#11531=CARTESIAN_POINT('Ctrl Pts',(1.84329853290387,-1.61468286935684,93.6006901909737));
#11532=CARTESIAN_POINT('Ctrl Pts',(1.89689943247359,-1.55349286021372,93.6049052885078));
#11533=CARTESIAN_POINT('Ctrl Pts',(1.94747025999694,-1.48960806092931,93.6091203860419));
#11534=CARTESIAN_POINT('Ctrl Pts',(1.99473828254142,-1.42336553076281,93.6133354835759));
#11535=CARTESIAN_POINT('Ctrl Pts',(2.04200507760965,-1.35712472081071,93.6175504716505));
#11536=CARTESIAN_POINT('Ctrl Pts',(2.08596896889155,-1.2885266809942,93.6217654597252));
#11537=CARTESIAN_POINT('Ctrl Pts',(2.12639964896309,-1.21793874348821,93.6259804477998));
#11538=CARTESIAN_POINT('Ctrl Pts',(2.16734665896066,-1.1464493453962,93.6302492644144));
#11539=CARTESIAN_POINT('Ctrl Pts',(2.20466931471134,-1.07291927885784,93.6345180810291));
#11540=CARTESIAN_POINT('Ctrl Pts',(2.23817650900993,-0.997755563510491,
93.6387868976437));
#11541=CARTESIAN_POINT('Ctrl Pts',(2.27130944122984,-0.923431397070061,
93.6430080332689));
#11542=CARTESIAN_POINT('Ctrl Pts',(2.30071160980411,-0.847510356062231,
93.647229168894));
#11543=CARTESIAN_POINT('Ctrl Pts',(2.32624758298905,-0.770404071015732,
93.6514503045192));
#11544=CARTESIAN_POINT('Ctrl Pts',(2.35221622900574,-0.691991323338812,
93.6557429616286));
#11545=CARTESIAN_POINT('Ctrl Pts',(2.37418631550918,-0.612353278914442,
93.660035618738));
#11546=CARTESIAN_POINT('Ctrl Pts',(2.39206933760362,-0.531934708490236,
93.6643282758474));
#11547=CARTESIAN_POINT('Ctrl Pts',(2.40995235969806,-0.451516138066032,
93.6686209329568));
#11548=CARTESIAN_POINT('Ctrl Pts',(2.42374829954972,-0.370317544383954,
93.6729135900662));
#11549=CARTESIAN_POINT('Ctrl Pts',(2.43342385047315,-0.288788181801841,
93.6772062471756));
#11550=CARTESIAN_POINT('Ctrl Pts',(2.44295870152505,-0.208444402442073,
93.6814364813482));
#11551=CARTESIAN_POINT('Ctrl Pts',(2.44852821755694,-0.127476393511042,
93.6856667155208));
#11552=CARTESIAN_POINT('Ctrl Pts',(2.45006238231793,-0.0463095319623845,
93.6898969496934));
#11553=CARTESIAN_POINT('Ctrl Pts',(2.45159433903938,0.0347405105559447,
93.694121095521));
#11554=CARTESIAN_POINT('Ctrl Pts',(2.44910247039975,0.115988376156796,93.6983452413487));
#11555=CARTESIAN_POINT('Ctrl Pts',(2.44256838395305,0.19700238504394,93.7025693871763));
#11556=CARTESIAN_POINT('Ctrl Pts',(2.43600052513471,0.278435126563032,93.7068153661131));
#11557=CARTESIAN_POINT('Ctrl Pts',(2.42534848213189,0.359631114209472,93.7110613450499));
#11558=CARTESIAN_POINT('Ctrl Pts',(2.41064671769813,0.440150715609106,93.7153073239867));
#11559=CARTESIAN_POINT('Ctrl Pts',(2.39604702268683,0.520111296406298,93.7195238245149));
#11560=CARTESIAN_POINT('Ctrl Pts',(2.37745374454511,0.599404389413137,93.7237403250432));
#11561=CARTESIAN_POINT('Ctrl Pts',(2.35495252107438,0.677605249009643,93.7279568255715));
#11562=CARTESIAN_POINT('Ctrl Pts',(2.33245878456142,0.755780088397308,93.73217192312));
#11563=CARTESIAN_POINT('Ctrl Pts',(2.30605981341392,0.832862969375039,93.7363870206685));
#11564=CARTESIAN_POINT('Ctrl Pts',(2.2758916896718,0.908442219892288,93.740602118217));
#11565=CARTESIAN_POINT('Ctrl Pts',(2.2457243493474,0.984019507737804,93.7448171063062));
#11566=CARTESIAN_POINT('Ctrl Pts',(2.21178822447472,1.05809281111239,93.7490320943954));
#11567=CARTESIAN_POINT('Ctrl Pts',(2.17426780217715,1.13026977948441,93.7532470824846));
#11568=CARTESIAN_POINT('Ctrl Pts',(2.13626821639556,1.20336850101147,93.7575158990825));
#11569=CARTESIAN_POINT('Ctrl Pts',(2.09459234416314,1.27452166630813,93.7617847156803));
#11570=CARTESIAN_POINT('Ctrl Pts',(2.04947925360533,1.3433484428998,93.7660535322782));
#11571=CARTESIAN_POINT('Ctrl Pts',(2.00487005805567,1.4114064521842,93.7702746679182));
#11572=CARTESIAN_POINT('Ctrl Pts',(1.95690037414002,1.47718943973062,93.7744958035581));
#11573=CARTESIAN_POINT('Ctrl Pts',(1.90584325146648,1.54036091577256,93.778716939198));
#11574=CARTESIAN_POINT('Ctrl Pts',(1.85392103487245,1.60460274707563,93.7830095962749));
#11575=CARTESIAN_POINT('Ctrl Pts',(1.79880611936775,1.66614337431273,93.7873022533518));
#11576=CARTESIAN_POINT('Ctrl Pts',(1.74082480547681,1.72466786560097,93.7915949104286));
#11577=CARTESIAN_POINT('Ctrl Pts',(1.68284349158587,1.78319235688922,93.7958875675055));
#11578=CARTESIAN_POINT('Ctrl Pts',(1.62199619258673,1.8387004254033,93.8001802245824));
#11579=CARTESIAN_POINT('Ctrl Pts',(1.5586428253669,1.89092114931646,93.8044728816592));
#11580=CARTESIAN_POINT('Ctrl Pts',(1.49621072937485,1.94238249053939,93.8087031158274));
#11581=CARTESIAN_POINT('Ctrl Pts',(1.4311095326108,1.99084559138337,93.8129333499956));
#11582=CARTESIAN_POINT('Ctrl Pts',(1.36365921747145,2.03602155897357,93.8171635841638));
#11583=CARTESIAN_POINT('Ctrl Pts',(1.29630597988765,2.08113250726038,93.821387729987));
#11584=CARTESIAN_POINT('Ctrl Pts',(1.22661072184333,2.12296546155753,93.8256118758102));
#11585=CARTESIAN_POINT('Ctrl Pts',(1.15492663987504,2.16127154853502,93.8298360216333));
#11586=CARTESIAN_POINT('Ctrl Pts',(1.08287204825753,2.19977562611878,93.8340820005712));
#11587=CARTESIAN_POINT('Ctrl Pts',(1.00880837945504,2.23471596665707,93.8383279795091));
#11588=CARTESIAN_POINT('Ctrl Pts',(0.933124097740295,2.26588386026653,93.842573958447));
#11589=CARTESIAN_POINT('Ctrl Pts',(0.857965266726225,2.2968353655961,93.8467904589706));
#11590=CARTESIAN_POINT('Ctrl Pts',(0.781208690093167,2.32406646032518,93.8510069594943));
#11591=CARTESIAN_POINT('Ctrl Pts',(0.70325797834281,2.34741953342328,93.855223460018));
#11592=CARTESIAN_POINT('Ctrl Pts',(0.625333203569053,2.37076483612267,93.8594385575618));
#11593=CARTESIAN_POINT('Ctrl Pts',(0.546215527961278,2.39023454618982,93.8636536551056));
#11594=CARTESIAN_POINT('Ctrl Pts',(0.466324838418034,2.40572055631455,93.8678687526495));
#11595=CARTESIAN_POINT('Ctrl Pts',(0.386436223508429,2.42120616429233,93.872083740734));
#11596=CARTESIAN_POINT('Ctrl Pts',(0.305775091462451,2.43270819053178,93.8762987288184));
#11597=CARTESIAN_POINT('Ctrl Pts',(0.224771247095008,2.44016969419738,93.8805137169029));
#11598=CARTESIAN_POINT('Ctrl Pts',(0.142732923655423,2.4477264867897,93.8847825335063));
#11599=CARTESIAN_POINT('Ctrl Pts',(0.0603435574257589,2.45113876008916,
93.8890513501096));
#11600=CARTESIAN_POINT('Ctrl Pts',(-0.0219472251692508,2.45040171590443,
93.8933201667129));
#11601=CARTESIAN_POINT('Ctrl Pts',(-0.103318852750464,2.44967290420742,
93.8975413023481));
#11602=CARTESIAN_POINT('Ctrl Pts',(-0.184593621574171,2.44488709555706,
93.9017624379833));
#11603=CARTESIAN_POINT('Ctrl Pts',(-0.265340834386893,2.43609205318823,
93.9059835736184));
#11604=CARTESIAN_POINT('Ctrl Pts',(-0.347456199853924,2.42714799068432,
93.9102762307058));
#11605=CARTESIAN_POINT('Ctrl Pts',(-0.429025469614802,2.41405765161002,
93.9145688877933));
#11606=CARTESIAN_POINT('Ctrl Pts',(-0.509607289736811,2.39692525128488,
93.9188615448807));
#11607=CARTESIAN_POINT('Ctrl Pts',(-0.590189109858818,2.37979285095975,
93.9231542019681));
#11608=CARTESIAN_POINT('Ctrl Pts',(-0.669783015604948,2.35861858196367,
93.9274468590555));
#11609=CARTESIAN_POINT('Ctrl Pts',(-0.747966499788094,2.3335587340358,93.9317395161429));
#11610=CARTESIAN_POINT('Ctrl Pts',(-0.825013056225563,2.30886330113379,
93.9359697503158));
#11611=CARTESIAN_POINT('Ctrl Pts',(-0.900980542187783,2.28030145499961,
93.9401999844887));
#11612=CARTESIAN_POINT('Ctrl Pts',(-0.975452924571176,2.24798617476744,
93.9444302186617));
#11613=CARTESIAN_POINT('Ctrl Pts',(-1.04981812292117,2.21571740415353,93.9486543644896));
#11614=CARTESIAN_POINT('Ctrl Pts',(-1.12269206818594,2.17970611183101,93.9528785103175));
#11615=CARTESIAN_POINT('Ctrl Pts',(-1.1936744345533,2.14011485539769,93.9571026561454));
#11616=CARTESIAN_POINT('Ctrl Pts',(-1.26502368355035,2.10031896582777,93.9613486350821));
#11617=CARTESIAN_POINT('Ctrl Pts',(-1.33446128837698,2.0569061397908,93.9655946140188));
#11618=CARTESIAN_POINT('Ctrl Pts',(-1.40160164122745,2.01009031869429,93.9698405929555));
#11619=CARTESIAN_POINT('Ctrl Pts',(-1.46827586111603,1.96359952414925,93.9740570934839));
#11620=CARTESIAN_POINT('Ctrl Pts',(-1.53268423950821,1.91375310619271,93.9782735940122));
#11621=CARTESIAN_POINT('Ctrl Pts',(-1.59447596508579,1.86080537584234,93.9824900945406));
#11622=CARTESIAN_POINT('Ctrl Pts',(-1.65624713035636,1.8078752630869,93.9867051920891));
#11623=CARTESIAN_POINT('Ctrl Pts',(-1.71540301879969,1.75184618956455,93.9909202896377));
#11624=CARTESIAN_POINT('Ctrl Pts',(-1.77162566265668,1.69301292417284,93.9951353871862));
#11625=CARTESIAN_POINT('Ctrl Pts',(-1.82784684650103,1.63418118658747,93.9993503752753));
#11626=CARTESIAN_POINT('Ctrl Pts',(-1.88113461658577,1.57254573896462,94.0035653633645));
#11627=CARTESIAN_POINT('Ctrl Pts',(-1.93120868537594,1.50843735817187,94.0077803514536));
#11628=CARTESIAN_POINT('Ctrl Pts',(-1.98192223697967,1.44351026604385,94.0120491680514));
#11629=CARTESIAN_POINT('Ctrl Pts',(-2.02933910651463,1.3760470038798,94.0163179846491));
#11630=CARTESIAN_POINT('Ctrl Pts',(-2.07321215311288,1.30642321557184,94.0205868012468));
#11631=CARTESIAN_POINT('Ctrl Pts',(-2.11659515549269,1.23757709687134,94.0248079368866));
#11632=CARTESIAN_POINT('Ctrl Pts',(-2.15651293011166,1.16661891696603,94.0290290725263));
#11633=CARTESIAN_POINT('Ctrl Pts',(-2.19277278687027,1.09393681497661,94.033250208166));
#11634=CARTESIAN_POINT('Ctrl Pts',(-2.22964701788347,1.02002321302489,94.0375428652427));
#11635=CARTESIAN_POINT('Ctrl Pts',(-2.26273802276296,0.944327188629773,
94.0418355223195));
#11636=CARTESIAN_POINT('Ctrl Pts',(-2.29189483860102,0.867276368174531,
94.0461281793963));
#11637=CARTESIAN_POINT('Ctrl Pts',(-2.32105165443908,0.790225547719291,
94.050420836473));
#11638=CARTESIAN_POINT('Ctrl Pts',(-2.34627419196474,0.71182042627785,94.0547134935498));
#11639=CARTESIAN_POINT('Ctrl Pts',(-2.36746548479031,0.632500931482782,
94.0590061506265));
#11640=CARTESIAN_POINT('Ctrl Pts',(-2.39481446363939,0.530133076754626,
94.0645461518225));
#11641=CARTESIAN_POINT('Ctrl Pts',(-2.41553687113253,0.425925319477767,
94.0700861530185));
#11642=CARTESIAN_POINT('Ctrl Pts',(-2.4294335776465,0.320628666534577,94.0756261542145));
#11643=CARTESIAN_POINT('Ctrl Pts',(-2.44333028416046,0.215332013591387,
94.0811661554105));
#11644=CARTESIAN_POINT('Ctrl Pts',(-2.45040109986711,0.108946103270164,
94.0867061566065));
#11645=CARTESIAN_POINT('Ctrl Pts',(-2.45049896913575,0.00224772432606995,
94.0922461578025));
#11646=CARTESIAN_POINT('',(-2.45049991819808,-0.000633175507849021,94.8922461578706));
#11647=CARTESIAN_POINT('Ctrl Pts',(-2.45049896913641,0.00224772360119427,
94.0922461578402));
#11648=CARTESIAN_POINT('Ctrl Pts',(-2.45057271168345,-0.0781474083459136,
94.0964204398822));
#11649=CARTESIAN_POINT('Ctrl Pts',(-2.44668583696763,-0.158638087010778,
94.1005947219241));
#11650=CARTESIAN_POINT('Ctrl Pts',(-2.43883687232859,-0.238798995329727,
94.1047690039661));
#11651=CARTESIAN_POINT('Ctrl Pts',(-2.43099234738414,-0.318914561368906,
94.1089409248639));
#11652=CARTESIAN_POINT('Ctrl Pts',(-2.41919022501533,-0.398700254556573,
94.1131128457616));
#11653=CARTESIAN_POINT('Ctrl Pts',(-2.40348106258373,-0.477733222417452,
94.1172847666594));
#11654=CARTESIAN_POINT('Ctrl Pts',(-2.38777572169291,-0.556746964064932,
94.1214556726612));
#11655=CARTESIAN_POINT('Ctrl Pts',(-2.3681653205176,-0.635007877358875,
94.125626578663));
#11656=CARTESIAN_POINT('Ctrl Pts',(-2.34475172025415,-0.712102254149771,
94.1297974846647));
#11657=CARTESIAN_POINT('Ctrl Pts',(-2.32133626790918,-0.789202729322328,
94.1339687205969));
#11658=CARTESIAN_POINT('Ctrl Pts',(-2.29411715983875,-0.865136030139195,
94.1381399565291));
#11659=CARTESIAN_POINT('Ctrl Pts',(-2.26324595694186,-0.939504118344522,
94.1423111924612));
#11660=CARTESIAN_POINT('Ctrl Pts',(-2.23234250510913,-1.01394989356819,
94.146486785785));
#11661=CARTESIAN_POINT('Ctrl Pts',(-2.19777952781821,-1.0868267529397,94.1506623791087));
#11662=CARTESIAN_POINT('Ctrl Pts',(-2.15975623063707,-1.15775786511013,
94.1548379724325));
#11663=CARTESIAN_POINT('Ctrl Pts',(-2.12171076230802,-1.22873033677055,
94.1590160005187));
#11664=CARTESIAN_POINT('Ctrl Pts',(-2.08020120611368,-1.29775439710323,
94.1631940286049));
#11665=CARTESIAN_POINT('Ctrl Pts',(-2.03547076110762,-1.36448123133884,
94.1673720566911));
#11666=CARTESIAN_POINT('Ctrl Pts',(-1.99066531938294,-1.43131994225288,
94.1715570898138));
#11667=CARTESIAN_POINT('Ctrl Pts',(-1.94262849669932,-1.49585336034432,
94.1757421229364));
#11668=CARTESIAN_POINT('Ctrl Pts',(-1.89164409947937,-1.55776533884436,
94.1799271560591));
#11669=CARTESIAN_POINT('Ctrl Pts',(-1.86587544065273,-1.58905704254671,
94.1820423657428));
#11670=CARTESIAN_POINT('Ctrl Pts',(-1.83935441286635,-1.61967967395596,
94.1841575754264));
#11671=CARTESIAN_POINT('Ctrl Pts',(-1.81212105752399,-1.64959616963612,
94.1862727851101));
#11672=CARTESIAN_POINT('Ctrl Pts',(-1.75765673124764,-1.7094265416665,94.1905030192809));
#11673=CARTESIAN_POINT('Ctrl Pts',(-1.70012340622187,-1.76666948427848,
94.1947332534517));
#11674=CARTESIAN_POINT('Ctrl Pts',(-1.63979664655005,-1.82099346730383,
94.1989634876225));
#11675=CARTESIAN_POINT('Ctrl Pts',(-1.57955671189084,-1.87523926478536,
94.2031876334481));
#11676=CARTESIAN_POINT('Ctrl Pts',(-1.51653167006043,-1.926574137586,94.2074117792738));
#11677=CARTESIAN_POINT('Ctrl Pts',(-1.45103566161278,-1.97470143533851,
94.2116359250994));
#11678=CARTESIAN_POINT('Ctrl Pts',(-1.38520112752636,-2.02307748602421,
94.2158819040366));
#11679=CARTESIAN_POINT('Ctrl Pts',(-1.31687032778023,-2.06821235319246,
94.2201278829739));
#11680=CARTESIAN_POINT('Ctrl Pts',(-1.24639803252967,-2.10984411616265,
94.2243738619112));
#11681=CARTESIAN_POINT('Ctrl Pts',(-1.17641500285063,-2.15118684372921,
94.2285903624371));
#11682=CARTESIAN_POINT('Ctrl Pts',(-1.10432052466984,-2.18907471509843,
94.2328068629629));
#11683=CARTESIAN_POINT('Ctrl Pts',(-1.03049163928184,-2.22329422959945,
94.2370233634888));
#11684=CARTESIAN_POINT('Ctrl Pts',(-0.956687319393937,-2.25750235804904,
94.2412384610348));
#11685=CARTESIAN_POINT('Ctrl Pts',(-0.881150160021461,-2.28804435802382,
94.2454535585807));
#11686=CARTESIAN_POINT('Ctrl Pts',(-0.804280365001129,-2.31475340899925,
94.2496686561267));
#11687=CARTESIAN_POINT('Ctrl Pts',(-0.727412566168601,-2.34146176638259,
94.2538836442132));
#11688=CARTESIAN_POINT('Ctrl Pts',(-0.649212640259519,-2.36433722099284,
94.2580986322996));
#11689=CARTESIAN_POINT('Ctrl Pts',(-0.570097896893327,-2.38326218405735,
94.2623136203861));
#11690=CARTESIAN_POINT('Ctrl Pts',(-0.489972799761986,-2.40242883289209,
94.2665824369868));
#11691=CARTESIAN_POINT('Ctrl Pts',(-0.408909824615682,-2.41754324086638,
94.2708512535874));
#11692=CARTESIAN_POINT('Ctrl Pts',(-0.327353328602962,-2.42853660632336,
94.2751200701881));
#11693=CARTESIAN_POINT('Ctrl Pts',(-0.246707785834168,-2.43940718031167,
94.279341205825));
#11694=CARTESIAN_POINT('Ctrl Pts',(-0.165580166612593,-2.44624833644876,
94.2835623414619));
#11695=CARTESIAN_POINT('Ctrl Pts',(-0.0844035797152592,-2.44904599502158,
94.2877834770988));
#11696=CARTESIAN_POINT('Ctrl Pts',(-0.00185156512608912,-2.4518910561426,
94.2920761341813));
#11697=CARTESIAN_POINT('Ctrl Pts',(0.0807505892343749,-2.45055433345196,
94.2963687912638));
#11698=CARTESIAN_POINT('Ctrl Pts',(0.162951184608371,-2.4450761054484,94.3006614483463));
#11699=CARTESIAN_POINT('Ctrl Pts',(0.245151779982366,-2.43959787744484,
94.3049541054288));
#11700=CARTESIAN_POINT('Ctrl Pts',(0.326950328938398,-2.42997826853912,
94.3092467625113));
#11701=CARTESIAN_POINT('Ctrl Pts',(0.407906368883997,-2.41631178539192,
94.3135394195939));
#11702=CARTESIAN_POINT('Ctrl Pts',(0.487685163948704,-2.40284403722898,
94.3177696538037));
#11703=CARTESIAN_POINT('Ctrl Pts',(0.566946691320933,-2.38539558823848,
94.3219998880135));
#11704=CARTESIAN_POINT('Ctrl Pts',(0.64526306635131,-2.36401899848603,94.3262301222233));
#11705=CARTESIAN_POINT('Ctrl Pts',(0.72346672490408,-2.34267317489072,94.3304542680882));
#11706=CARTESIAN_POINT('Ctrl Pts',(0.800727487791892,-2.31741056015666,
94.3346784139532));
#11707=CARTESIAN_POINT('Ctrl Pts',(0.876625954662874,-2.28833502477487,
94.3389025598181));
#11708=CARTESIAN_POINT('Ctrl Pts',(0.952916712904789,-2.2591092086021,94.3431485387456));
#11709=CARTESIAN_POINT('Ctrl Pts',(1.02783058150085,-2.226031018153,94.3473945176731));
#11710=CARTESIAN_POINT('Ctrl Pts',(1.10095540803066,-2.18925728034145,94.3516404966005));
#11711=CARTESIAN_POINT('Ctrl Pts',(1.17357255420321,-2.1527388498617,94.3558569971661));
#11712=CARTESIAN_POINT('Ctrl Pts',(1.24442499997529,-2.11257623508412,94.3600734977317));
#11713=CARTESIAN_POINT('Ctrl Pts',(1.31312928358055,-2.06897117780873,94.3642899982973));
#11714=CARTESIAN_POINT('Ctrl Pts',(1.38181070682456,-2.02538062948837,94.368505095883));
#11715=CARTESIAN_POINT('Ctrl Pts',(1.44834499484991,-1.97835016233186,94.3727201934688));
#11716=CARTESIAN_POINT('Ctrl Pts',(1.51237543097266,-1.92812624218184,94.3769352910545));
#11717=CARTESIAN_POINT('Ctrl Pts',(1.57640420432572,-1.87790362626801,94.3811502791808));
#11718=CARTESIAN_POINT('Ctrl Pts',(1.6379288896881,-1.82448801017855,94.385365267307));
#11719=CARTESIAN_POINT('Ctrl Pts',(1.69662493671454,-1.76816686828998,94.3895802554333));
#11720=CARTESIAN_POINT('Ctrl Pts',(1.7560705744423,-1.71112646494537,94.3938490719869));
#11721=CARTESIAN_POINT('Ctrl Pts',(1.81261444802059,-1.65110612281475,94.3981178885406));
#11722=CARTESIAN_POINT('Ctrl Pts',(1.86595842410606,-1.58844244765356,94.4023867050943));
#11723=CARTESIAN_POINT('Ctrl Pts',(1.91870657051599,-1.52647869926911,94.4066078407706));
#11724=CARTESIAN_POINT('Ctrl Pts',(1.96832570872978,-1.46193078482751,94.4108289764469));
#11725=CARTESIAN_POINT('Ctrl Pts',(2.01456982077987,-1.39515543478243,94.4150501121232));
#11726=CARTESIAN_POINT('Ctrl Pts',(2.06159747546096,-1.32724866862533,94.4193427691155));
#11727=CARTESIAN_POINT('Ctrl Pts',(2.10513440770179,-1.2570387122475,94.4236354261079));
#11728=CARTESIAN_POINT('Ctrl Pts',(2.14497027593332,-1.18492732492863,94.4279280831002));
#11729=CARTESIAN_POINT('Ctrl Pts',(2.18480614416486,-1.11281593760977,94.4322207400926));
#11730=CARTESIAN_POINT('Ctrl Pts',(2.22094078949991,-1.03880359665717,94.4365133970849));
#11731=CARTESIAN_POINT('Ctrl Pts',(2.25321556377465,-0.963311929316616,
94.4408060540773));
#11732=CARTESIAN_POINT('Ctrl Pts',(2.28502100500606,-0.888918046074483,
94.445036288146));
#11733=CARTESIAN_POINT('Ctrl Pts',(2.3131980940021,-0.81280701318249,94.4492665222147));
#11734=CARTESIAN_POINT('Ctrl Pts',(2.33755969660922,-0.735367197247882,
94.4534967562834));
#11735=CARTESIAN_POINT('Ctrl Pts',(2.36188623689144,-0.658038836213461,
94.4577209020072));
#11736=CARTESIAN_POINT('Ctrl Pts',(2.38240805854403,-0.579385930284001,
94.4619450477309));
#11737=CARTESIAN_POINT('Ctrl Pts',(2.39898577846083,-0.499817451418697,
94.4661691934546));
#11738=CARTESIAN_POINT('Ctrl Pts',(2.41564918323451,-0.419837708896056,
94.4704151724173));
#11739=CARTESIAN_POINT('Ctrl Pts',(2.4283274059592,-0.338933338094459,94.4746611513801));
#11740=CARTESIAN_POINT('Ctrl Pts',(2.43692953074504,-0.257535846403518,
94.4789071303429));
#11741=CARTESIAN_POINT('Ctrl Pts',(2.4454719336006,-0.176703472685579,94.483123630768));
#11742=CARTESIAN_POINT('Ctrl Pts',(2.44999460796228,-0.0953852722739111,
94.4873401311931));
#11743=CARTESIAN_POINT('Ctrl Pts',(2.45045993409078,-0.0140129017627399,
94.4915566316182));
#11744=CARTESIAN_POINT('Ctrl Pts',(2.45092510538877,0.0673323932739367,
94.495771729064));
#11745=CARTESIAN_POINT('Ctrl Pts',(2.44733560667782,0.148731357811173,94.4999868265098));
#11746=CARTESIAN_POINT('Ctrl Pts',(2.43970590188025,0.229750652514127,94.5042019239556));
#11747=CARTESIAN_POINT('Ctrl Pts',(2.43207639521272,0.310767843288186,94.5084169119428));
#11748=CARTESIAN_POINT('Ctrl Pts',(2.42040693573168,0.391404920793907,94.5126318999299));
#11749=CARTESIAN_POINT('Ctrl Pts',(2.40476387660299,0.471233432372271,94.516846887917));
#11750=CARTESIAN_POINT('Ctrl Pts',(2.38892104322614,0.552081417235941,94.5211157046374));
#11751=CARTESIAN_POINT('Ctrl Pts',(2.36900247361349,0.632099554290949,94.5253845213577));
#11752=CARTESIAN_POINT('Ctrl Pts',(2.34513013480676,0.710855049093141,94.529653338078));
#11753=CARTESIAN_POINT('Ctrl Pts',(2.32152444161996,0.788730872745221,94.5338744736185));
#11754=CARTESIAN_POINT('Ctrl Pts',(2.29405308119321,0.865371697897479,94.5380956091589));
#11755=CARTESIAN_POINT('Ctrl Pts',(2.26288312779351,0.940377690051954,94.5423167446994));
#11756=CARTESIAN_POINT('Ctrl Pts',(2.23118503920108,1.01665456328908,94.5466094020097));
#11757=CARTESIAN_POINT('Ctrl Pts',(2.19566207516387,1.0912402353514,94.5509020593199));
#11758=CARTESIAN_POINT('Ctrl Pts',(2.15653847906908,1.16374053735978,94.5551947166302));
#11759=CARTESIAN_POINT('Ctrl Pts',(2.11741488297429,1.23624083936815,94.5594873739404));
#11760=CARTESIAN_POINT('Ctrl Pts',(2.07469097043895,1.30665537959105,94.5637800312507));
#11761=CARTESIAN_POINT('Ctrl Pts',(2.02863564799526,1.37462273285541,94.568072688561));
#11762=CARTESIAN_POINT('Ctrl Pts',(1.98325005421671,1.44160171642957,94.5723029227788));
#11763=CARTESIAN_POINT('Ctrl Pts',(1.93445816508792,1.50645685988666,94.5765331569966));
#11764=CARTESIAN_POINT('Ctrl Pts',(1.88248550546635,1.56882075831151,94.5807633912144));
#11765=CARTESIAN_POINT('Ctrl Pts',(1.83058764726583,1.63109489977072,94.5849875370863));
#11766=CARTESIAN_POINT('Ctrl Pts',(1.7755184057447,1.69088456284987,94.5892116829582));
#11767=CARTESIAN_POINT('Ctrl Pts',(1.71754645763939,1.74785137121278,94.5934358288301));
#11768=CARTESIAN_POINT('Ctrl Pts',(1.65927487389282,1.80511262001994,94.5976818077557));
#11769=CARTESIAN_POINT('Ctrl Pts',(1.59807075486495,1.85952135251601,94.6019277866813));
#11770=CARTESIAN_POINT('Ctrl Pts',(1.53424793998413,1.91076777988704,94.6061737656069));
#11771=CARTESIAN_POINT('Ctrl Pts',(1.47086822472033,1.96165842112761,94.6103902661769));
#11772=CARTESIAN_POINT('Ctrl Pts',(1.40490642735054,2.00943023267578,94.6146067667468));
#11773=CARTESIAN_POINT('Ctrl Pts',(1.3367053290778,2.05381817920064,94.6188232673168));
#11774=CARTESIAN_POINT('Ctrl Pts',(1.26852692375421,2.09819135626519,94.6230383649059));
#11775=CARTESIAN_POINT('Ctrl Pts',(1.19811108671214,2.13918265064091,94.627253462495));
#11776=CARTESIAN_POINT('Ctrl Pts',(1.12583017537303,2.17656993138735,94.6314685600842));
#11777=CARTESIAN_POINT('Ctrl Pts',(1.05355114107204,2.21395624123636,94.6356835482129));
#11778=CARTESIAN_POINT('Ctrl Pts',(0.979407542444483,2.24773851076299,94.6398985363416));
#11779=CARTESIAN_POINT('Ctrl Pts',(0.903795681637717,2.27774090182642,94.6441135244703));
#11780=CARTESIAN_POINT('Ctrl Pts',(0.827218203179831,2.30812644492548,94.6483823410182));
#11781=CARTESIAN_POINT('Ctrl Pts',(0.749135142350709,2.33463468329617,94.652651157566));
#11782=CARTESIAN_POINT('Ctrl Pts',(0.669976523004302,2.35713421523321,94.6569199741139));
#11783=CARTESIAN_POINT('Ctrl Pts',(0.591702071884836,2.37938243693487,94.6611411097902));
#11784=CARTESIAN_POINT('Ctrl Pts',(0.512376442463163,2.39771101188027,94.6653622454666));
#11785=CARTESIAN_POINT('Ctrl Pts',(0.432426320493267,2.41204430459821,94.6695833811429));
#11786=CARTESIAN_POINT('Ctrl Pts',(0.351121554257427,2.42662045514192,94.6738760381266));
#11787=CARTESIAN_POINT('Ctrl Pts',(0.269171435538037,2.43706461483055,94.6781686951102));
#11788=CARTESIAN_POINT('Ctrl Pts',(0.187028794132821,2.44335230373461,94.6824613520938));
#11789=CARTESIAN_POINT('Ctrl Pts',(0.104886152727603,2.44963999263867,94.6867540090774));
#11790=CARTESIAN_POINT('Ctrl Pts',(0.0225514888198296,2.45177126446202,
94.691046666061));
#11791=CARTESIAN_POINT('Ctrl Pts',(-0.0595257641802243,2.44977691502691,
94.6953393230447));
#11792=CARTESIAN_POINT('Ctrl Pts',(-0.140409474789221,2.44781156681328,
94.6995695575191));
#11793=CARTESIAN_POINT('Ctrl Pts',(-0.221348271614469,2.4418324280466,94.7037997919935));
#11794=CARTESIAN_POINT('Ctrl Pts',(-0.301911146407717,2.43183056763311,
94.7080300264679));
#11795=CARTESIAN_POINT('Ctrl Pts',(-0.382358071494822,2.42184310234614,
94.712254172599));
#11796=CARTESIAN_POINT('Ctrl Pts',(-0.462429691378725,2.4078444707579,94.71647831873));
#11797=CARTESIAN_POINT('Ctrl Pts',(-0.541696086056398,2.38987773753202,
94.7207024648611));
#11798=CARTESIAN_POINT('Ctrl Pts',(-0.62137217342591,2.3718181422638,94.7249484437222));
#11799=CARTESIAN_POINT('Ctrl Pts',(-0.700234211369373,2.34974931577968,
94.7291944225834));
#11800=CARTESIAN_POINT('Ctrl Pts',(-0.77785190998881,2.32376777155695,94.7334404014445));
#11801=CARTESIAN_POINT('Ctrl Pts',(-0.854930741895584,2.29796660615985,
94.7376569022779));
#11802=CARTESIAN_POINT('Ctrl Pts',(-0.930782010665086,2.26830702926195,
94.7418734031114));
#11803=CARTESIAN_POINT('Ctrl Pts',(-1.00499742590154,2.23493409834189,94.7460899039448));
#11804=CARTESIAN_POINT('Ctrl Pts',(-1.07918814702948,2.20157227178303,94.7503050017984));
#11805=CARTESIAN_POINT('Ctrl Pts',(-1.15174367158573,2.16449973542075,94.754520099652));
#11806=CARTESIAN_POINT('Ctrl Pts',(-1.22227581023555,2.12390962465756,94.7587351975056));
#11807=CARTESIAN_POINT('Ctrl Pts',(-1.29280611727141,2.08332056795873,94.7629501858995));
#11808=CARTESIAN_POINT('Ctrl Pts',(-1.36131274021397,2.03921435142673,94.7671651742933));
#11809=CARTESIAN_POINT('Ctrl Pts',(-1.42743348605354,1.99182928306947,94.7713801626871));
#11810=CARTESIAN_POINT('Ctrl Pts',(-1.49439863211182,1.94383907994586,94.7756489789239));
#11811=CARTESIAN_POINT('Ctrl Pts',(-1.55891612237586,1.89248595458735,94.7799177951607));
#11812=CARTESIAN_POINT('Ctrl Pts',(-1.6206429124431,1.83806060845337,94.7841866113974));
#11813=CARTESIAN_POINT('Ctrl Pts',(-1.6816802486939,1.78424316307952,94.7884077473378));
#11814=CARTESIAN_POINT('Ctrl Pts',(-1.73998862154228,1.72742215829781,94.7926288832782));
#11815=CARTESIAN_POINT('Ctrl Pts',(-1.79527370339053,1.66791563932786,94.7968500192185));
#11816=CARTESIAN_POINT('Ctrl Pts',(-1.85149550314817,1.60740087690087,94.8011426756035));
#11817=CARTESIAN_POINT('Ctrl Pts',(-1.90459028865089,1.54410913767614,94.8054353319885));
#11818=CARTESIAN_POINT('Ctrl Pts',(-1.95429263032105,1.47840811857648,94.8097279883734));
#11819=CARTESIAN_POINT('Ctrl Pts',(-2.00399497199121,1.41270709947681,94.8140206447584));
#11820=CARTESIAN_POINT('Ctrl Pts',(-2.05030464456659,1.34459725030632,94.8183133011434));
#11821=CARTESIAN_POINT('Ctrl Pts',(-2.09300455428211,1.27447329738773,94.8226059575283));
#11822=CARTESIAN_POINT('Ctrl Pts',(-2.13642069144977,1.2031731194966,94.8269706168371));
#11823=CARTESIAN_POINT('Ctrl Pts',(-2.17626044123707,1.12953615291983,94.8313352761459));
#11824=CARTESIAN_POINT('Ctrl Pts',(-2.2122733453413,1.05394349729595,94.8356999354546));
#11825=CARTESIAN_POINT('Ctrl Pts',(-2.24822307132856,0.978483455293714,
94.8400569377592));
#11826=CARTESIAN_POINT('Ctrl Pts',(-2.28035912062873,0.901074927510781,
94.8444139400638));
#11827=CARTESIAN_POINT('Ctrl Pts',(-2.30847555175356,0.822125827933955,
94.8487709423684));
#11828=CARTESIAN_POINT('Ctrl Pts',(-2.33653701668684,0.743331069827807,
94.8531194269553));
#11829=CARTESIAN_POINT('Ctrl Pts',(-2.36059436775562,0.663002134486998,
94.8574679115423));
#11830=CARTESIAN_POINT('Ctrl Pts',(-2.3804892538109,0.581567848570437,94.8618163961292));
#11831=CARTESIAN_POINT('Ctrl Pts',(-2.40036100275622,0.500228268098339,
94.8661598235689));
#11832=CARTESIAN_POINT('Ctrl Pts',(-2.41607981075422,0.417786303621603,
94.8705032510087));
#11833=CARTESIAN_POINT('Ctrl Pts',(-2.42753682224339,0.334686759003764,
94.8748466784485));
#11834=CARTESIAN_POINT('Ctrl Pts',(-2.43898051632255,0.25168380769989,94.8791850571716));
#11835=CARTESIAN_POINT('Ctrl Pts',(-2.4461722172272,0.168025217525998,94.8835234358948));
#11836=CARTESIAN_POINT('Ctrl Pts',(-2.44905418491344,0.0841656067402018,
94.887861814618));
#11837=CARTESIAN_POINT('Ctrl Pts',(-2.45002501882,0.0559162429704074,94.8893232623587));
#11838=CARTESIAN_POINT('Ctrl Pts',(-2.45050722465988,0.0276441353787134,
94.8907847100995));
#11839=CARTESIAN_POINT('Ctrl Pts',(-2.45049991819823,-0.00063317491965548,
94.8922461578402));
#11840=CARTESIAN_POINT('',(-2.45049916761641,-0.00201978001007516,95.6922461577976));
#11841=CARTESIAN_POINT('Ctrl Pts',(-2.45049991819808,-0.000633175507850709,
94.8922461578706));
#11842=CARTESIAN_POINT('Ctrl Pts',(-2.45047735789977,-0.0879454743182435,
94.8967586932033));
#11843=CARTESIAN_POINT('Ctrl Pts',(-2.44578411198309,-0.175130467335658,
94.901271228536));
#11844=CARTESIAN_POINT('Ctrl Pts',(-2.43648610108198,-0.261697782249549,
94.9057837638687));
#11845=CARTESIAN_POINT('Ctrl Pts',(-2.42715182304631,-0.348602755238054,
94.9103139004635));
#11846=CARTESIAN_POINT('Ctrl Pts',(-2.41317689096561,-0.434884875770232,
94.9148440370582));
#11847=CARTESIAN_POINT('Ctrl Pts',(-2.3946786543609,-0.520061912033822,
94.919374173653));
#11848=CARTESIAN_POINT('Ctrl Pts',(-2.37614175994702,-0.605416952162517,
94.9239137773747));
#11849=CARTESIAN_POINT('Ctrl Pts',(-2.35306278731216,-0.689661956551622,
94.9284533810965));
#11850=CARTESIAN_POINT('Ctrl Pts',(-2.32560864957564,-0.772330666890149,
94.9329929848183));
#11851=CARTESIAN_POINT('Ctrl Pts',(-2.2980712145746,-0.855250198343442,
94.937546361931));
#11852=CARTESIAN_POINT('Ctrl Pts',(-2.26613220165545,-0.9365835419457,94.9420997390438));
#11853=CARTESIAN_POINT('Ctrl Pts',(-2.23000666024073,-1.0158841200068,94.9466531161565));
#11854=CARTESIAN_POINT('Ctrl Pts',(-2.22149244427397,-1.03457400592851,
94.947726274775));
#11855=CARTESIAN_POINT('Ctrl Pts',(-2.2127458756019,-1.05315109379866,94.9487994333934));
#11856=CARTESIAN_POINT('Ctrl Pts',(-2.20377012755118,-1.07160975868693,
94.9498725920119));
#11857=CARTESIAN_POINT('Ctrl Pts',(-2.16838903720358,-1.14437112480566,
94.9541028268427));
#11858=CARTESIAN_POINT('Ctrl Pts',(-2.12933383572574,-1.21551556172193,
94.9583330616736));
#11859=CARTESIAN_POINT('Ctrl Pts',(-2.08677540852799,-1.2846472840289,94.9625632965045));
#11860=CARTESIAN_POINT('Ctrl Pts',(-2.04427823340945,-1.35367950872731,
94.9667874429835));
#11861=CARTESIAN_POINT('Ctrl Pts',(-1.99828808797043,-1.42070437919437,
94.9710115894625));
#11862=CARTESIAN_POINT('Ctrl Pts',(-1.94902270471539,-1.48534869525776,
94.9752357359415));
#11863=CARTESIAN_POINT('Ctrl Pts',(-1.89950269574123,-1.55032712230084,
94.9794817147146));
#11864=CARTESIAN_POINT('Ctrl Pts',(-1.84667370015972,-1.61289988602724,
94.9837276934877));
#11865=CARTESIAN_POINT('Ctrl Pts',(-1.790802224898,-1.67271564866846,94.9879736722608));
#11866=CARTESIAN_POINT('Ctrl Pts',(-1.73531863612909,-1.73211614168818,
94.9921901734192));
#11867=CARTESIAN_POINT('Ctrl Pts',(-1.67683500032028,-1.7887974488079,94.9964066745777));
#11868=CARTESIAN_POINT('Ctrl Pts',(-1.61565284657833,-1.84244840615507,
95.0006231757362));
#11869=CARTESIAN_POINT('Ctrl Pts',(-1.55449105044771,-1.89608151180413,
95.0048382739057));
#11870=CARTESIAN_POINT('Ctrl Pts',(-1.49063286891244,-1.94668596353109,
95.0090533720751));
#11871=CARTESIAN_POINT('Ctrl Pts',(-1.4244152176806,-1.9939888509317,95.0132684702445));
#11872=CARTESIAN_POINT('Ctrl Pts',(-1.35819928617254,-2.04129050983962,
95.0174834589446));
#11873=CARTESIAN_POINT('Ctrl Pts',(-1.28962438594445,-2.08529050536559,
95.0216984476447));
#11874=CARTESIAN_POINT('Ctrl Pts',(-1.21905772795312,-2.12575833666901,
95.0259134363447));
#11875=CARTESIAN_POINT('Ctrl Pts',(-1.14758990460616,-2.1667429588851,95.0301822521906));
#11876=CARTESIAN_POINT('Ctrl Pts',(-1.07407950609926,-2.20410430293818,
95.0344510680365));
#11877=CARTESIAN_POINT('Ctrl Pts',(-0.998933451089233,-2.23765104748148,
95.0387198838824));
#11878=CARTESIAN_POINT('Ctrl Pts',(-0.924626723872426,-2.27082309883478,
95.0429410201025));
#11879=CARTESIAN_POINT('Ctrl Pts',(-0.848721157933712,-2.30026522668508,
95.0471621563226));
#11880=CARTESIAN_POINT('Ctrl Pts',(-0.771628312528639,-2.32584178251751,
95.0513832925427));
#11881=CARTESIAN_POINT('Ctrl Pts',(-0.693229269752938,-2.35185168634484,
95.0556759482015));
#11882=CARTESIAN_POINT('Ctrl Pts',(-0.613602826292481,-2.37386367892888,
95.0599686038603));
#11883=CARTESIAN_POINT('Ctrl Pts',(-0.533193705700807,-2.39178902125606,
95.0642612595191));
#11884=CARTESIAN_POINT('Ctrl Pts',(-0.452784585109126,-2.40971436358325,
95.0685539151779));
#11885=CARTESIAN_POINT('Ctrl Pts',(-0.371593290117368,-2.42355303755492,
95.0728465708367));
#11886=CARTESIAN_POINT('Ctrl Pts',(-0.290069056961055,-2.43327149989345,
95.0771392264955));
#11887=CARTESIAN_POINT('Ctrl Pts',(-0.209730264145545,-2.44284864649234,
95.0813694628345));
#11888=CARTESIAN_POINT('Ctrl Pts',(-0.128765155128878,-2.4484607827584,
95.0855996991734));
#11889=CARTESIAN_POINT('Ctrl Pts',(-0.0475990703908773,-2.45003766879163,
95.0898299355123));
#11890=CARTESIAN_POINT('Ctrl Pts',(0.0334501967872597,-2.45161228530577,
95.0940540835215));
#11891=CARTESIAN_POINT('Ctrl Pts',(0.114699404089822,-2.44916317693098,
95.0982782315307));
#11892=CARTESIAN_POINT('Ctrl Pts',(0.19571688106442,-2.44267172425326,95.1025023795399));
#11893=CARTESIAN_POINT('Ctrl Pts',(0.277153056114405,-2.43614672376779,
95.1067483579332));
#11894=CARTESIAN_POINT('Ctrl Pts',(0.35835462605696,-2.42553741631223,95.1109943363265));
#11895=CARTESIAN_POINT('Ctrl Pts',(0.438881940923745,-2.41087803340007,
95.1152403147198));
#11896=CARTESIAN_POINT('Ctrl Pts',(0.518850233643703,-2.39632041620208,
95.1194568174506));
#11897=CARTESIAN_POINT('Ctrl Pts',(0.598153139337098,-2.37776886130359,
95.1236733201814));
#11898=CARTESIAN_POINT('Ctrl Pts',(0.676365867025972,-2.35530878313698,
95.1278898229122));
#11899=CARTESIAN_POINT('Ctrl Pts',(0.754552570625387,-2.33285617821802,
95.1321049226661));
#11900=CARTESIAN_POINT('Ctrl Pts',(0.831649369793658,-2.30649776086538,
95.1363200224201));
#11901=CARTESIAN_POINT('Ctrl Pts',(0.907244520584572,-2.27636939662026,
95.140535122174));
#11902=CARTESIAN_POINT('Ctrl Pts',(0.982837708291136,-2.24624181476024,
95.1447501124686));
#11903=CARTESIAN_POINT('Ctrl Pts',(1.05692889341685,-2.21234465386775,95.1489651027632));
#11904=CARTESIAN_POINT('Ctrl Pts',(1.12912562806165,-2.17486219472738,95.1531800930578));
#11905=CARTESIAN_POINT('Ctrl Pts',(1.20224428542304,-2.13690109994337,95.1574489070513));
#11906=CARTESIAN_POINT('Ctrl Pts',(1.27341932385271,-2.09526270025244,95.1617177210447));
#11907=CARTESIAN_POINT('Ctrl Pts',(1.34226978604317,-2.05018586266602,95.1659865350381));
#11908=CARTESIAN_POINT('Ctrl Pts',(1.41035129310837,-2.00561246491414,95.1702076728607));
#11909=CARTESIAN_POINT('Ctrl Pts',(1.47615954531245,-1.95767737856541,95.1744288106833));
#11910=CARTESIAN_POINT('Ctrl Pts',(1.53935790885744,-1.90665347623475,95.1786499485059));
#11911=CARTESIAN_POINT('Ctrl Pts',(1.60362697517438,-1.85476513010211,95.1829426005848));
#11912=CARTESIAN_POINT('Ctrl Pts',(1.66519652468833,-1.7996826712849,95.1872352526637));
#11913=CARTESIAN_POINT('Ctrl Pts',(1.72375145497051,-1.74173223300456,95.1915279047425));
#11914=CARTESIAN_POINT('Ctrl Pts',(1.7823063852527,-1.68378179472421,95.1958205568214));
#11915=CARTESIAN_POINT('Ctrl Pts',(1.83784640926265,-1.62296379010353,95.2001132089003));
#11916=CARTESIAN_POINT('Ctrl Pts',(1.89010041660449,-1.55963799169921,95.2044058609792));
#11917=CARTESIAN_POINT('Ctrl Pts',(1.94159452572965,-1.4972331018285,95.2086360876322));
#11918=CARTESIAN_POINT('Ctrl Pts',(1.99009181235062,-1.43215754003063,95.2128663142852));
#11919=CARTESIAN_POINT('Ctrl Pts',(2.03530321545965,-1.36473113511035,95.2170965409383));
#11920=CARTESIAN_POINT('Ctrl Pts',(2.08044954808959,-1.2974017735944,95.2213206792407));
#11921=CARTESIAN_POINT('Ctrl Pts',(2.12231913272111,-1.22772867168445,95.2255448175431));
#11922=CARTESIAN_POINT('Ctrl Pts',(2.16066291033438,-1.15606489346635,95.2297689558455));
#11923=CARTESIAN_POINT('Ctrl Pts',(2.19920495904508,-1.08403055040467,95.2340149366629));
#11924=CARTESIAN_POINT('Ctrl Pts',(2.23418432595282,-1.00998524945895,95.2382609174803));
#11925=CARTESIAN_POINT('Ctrl Pts',(2.26539209553103,-0.934317346251,95.2425068982977));
#11926=CARTESIAN_POINT('Ctrl Pts',(2.29638313128798,-0.859174946596514,
95.2467233913414));
#11927=CARTESIAN_POINT('Ctrl Pts',(2.32365461055945,-0.782432846519269,
95.250939884385));
#11928=CARTESIAN_POINT('Ctrl Pts',(2.34704871011201,-0.704494572272601,
95.2551563774287));
#11929=CARTESIAN_POINT('Ctrl Pts',(2.37043502577665,-0.626582230325246,
95.2593714675242));
#11930=CARTESIAN_POINT('Ctrl Pts',(2.38994639000836,-0.547474949753931,
95.2635865576197));
#11931=CARTESIAN_POINT('Ctrl Pts',(2.40547447471462,-0.467592559282576,
95.2678016477152));
#11932=CARTESIAN_POINT('Ctrl Pts',(2.42100215633336,-0.387712242447165,
95.2720166283928));
#11933=CARTESIAN_POINT('Ctrl Pts',(2.43254667629042,-0.307057312559571,
95.2762316090704));
#11934=CARTESIAN_POINT('Ctrl Pts',(2.44005086774202,-0.226057543186284,
95.280446589748));
#11935=CARTESIAN_POINT('Ctrl Pts',(2.44765092242728,-0.144023032113256,
95.2847154152243));
#11936=CARTESIAN_POINT('Ctrl Pts',(2.45110662479623,-0.0616352936289753,
95.2889842407005));
#11937=CARTESIAN_POINT('Ctrl Pts',(2.45041294026594,0.0206560445693769,
95.2932530661767));
#11938=CARTESIAN_POINT('Ctrl Pts',(2.44972700651406,0.102027913037481,95.2974741945819));
#11939=CARTESIAN_POINT('Ctrl Pts',(2.44498403849069,0.18330505823126,95.301695322987));
#11940=CARTESIAN_POINT('Ctrl Pts',(2.43623157313892,0.264056759127766,95.3059164513921));
#11941=CARTESIAN_POINT('Ctrl Pts',(2.42733075872425,0.34617715314952,95.3102091254039));
#11942=CARTESIAN_POINT('Ctrl Pts',(2.41428334790203,0.427753629191953,95.3145017994157));
#11943=CARTESIAN_POINT('Ctrl Pts',(2.39719332599091,0.50834477259496,95.3187944734275));
#11944=CARTESIAN_POINT('Ctrl Pts',(2.3801033040798,0.588935915997967,95.3230871474393));
#11945=CARTESIAN_POINT('Ctrl Pts',(2.35897086342322,0.668541261909216,95.3273798214511));
#11946=CARTESIAN_POINT('Ctrl Pts',(2.3339520747727,0.746738215617897,95.3316724954629));
#11947=CARTESIAN_POINT('Ctrl Pts',(2.30929715729089,0.823797879374917,95.335902737183));
#11948=CARTESIAN_POINT('Ctrl Pts',(2.28077524768402,0.899780502572685,95.3401329789031));
#11949=CARTESIAN_POINT('Ctrl Pts',(2.24849910680534,0.974269991683817,95.3443632206233));
#11950=CARTESIAN_POINT('Ctrl Pts',(2.21626941952085,1.04865227143212,95.3485873739473));
#11951=CARTESIAN_POINT('Ctrl Pts',(2.18029641548116,1.12154526189137,95.3528115272713));
#11952=CARTESIAN_POINT('Ctrl Pts',(2.14074244224802,1.19254855077602,95.3570356805952));
#11953=CARTESIAN_POINT('Ctrl Pts',(2.1009841167441,1.26391867217156,95.3612816576515));
#11954=CARTESIAN_POINT('Ctrl Pts',(2.0576078550931,1.33337905458774,95.3655276347078));
#11955=CARTESIAN_POINT('Ctrl Pts',(2.01082739494091,1.40054397922919,95.3697736117641));
#11956=CARTESIAN_POINT('Ctrl Pts',(1.96437161462644,1.46724274563359,95.3739901196118));
#11957=CARTESIAN_POINT('Ctrl Pts',(1.91455900926562,1.53167742989576,95.3782066274594));
#11958=CARTESIAN_POINT('Ctrl Pts',(1.86164370577044,1.59349708589796,95.3824231353071));
#11959=CARTESIAN_POINT('Ctrl Pts',(1.80874601007896,1.65529617113339,95.3866382400929));
#11960=CARTESIAN_POINT('Ctrl Pts',(1.75274796872534,1.71448160296329,95.3908533448786));
#11961=CARTESIAN_POINT('Ctrl Pts',(1.69394418380189,1.77073525750287,95.3950684496645));
#11962=CARTESIAN_POINT('Ctrl Pts',(1.63514192718873,1.82698745001004,95.3992834448997));
#11963=CARTESIAN_POINT('Ctrl Pts',(1.57353440886822,1.88030769592763,95.4034984401349));
#11964=CARTESIAN_POINT('Ctrl Pts',(1.5094522587701,1.93041553259754,95.4077134353702));
#11965=CARTESIAN_POINT('Ctrl Pts',(1.44455197487279,1.98116309366373,95.4119822432515));
#11966=CARTESIAN_POINT('Ctrl Pts',(1.37711379745793,2.02861532240687,95.4162510511329));
#11967=CARTESIAN_POINT('Ctrl Pts',(1.30751323677533,2.0725248817945,95.4205198590142));
#11968=CARTESIAN_POINT('Ctrl Pts',(1.23868983402477,2.11594414825868,95.4247410015051));
#11969=CARTESIAN_POINT('Ctrl Pts',(1.16775253861468,2.1558992892507,95.4289621439959));
#11970=CARTESIAN_POINT('Ctrl Pts',(1.09508938887755,2.19219740907788,95.4331832864868));
#11971=CARTESIAN_POINT('Ctrl Pts',(1.02119546426745,2.2291103496771,95.4374759270634));
#11972=CARTESIAN_POINT('Ctrl Pts',(0.945517138300447,2.26224103266617,95.44176856764));
#11973=CARTESIAN_POINT('Ctrl Pts',(0.868481951697543,2.29143827095028,95.4460612082166));
#11974=CARTESIAN_POINT('Ctrl Pts',(0.79144676509464,2.3206355092344,95.4503538487932));
#11975=CARTESIAN_POINT('Ctrl Pts',(0.713055212866924,2.34589921328184,95.4546464893698));
#11976=CARTESIAN_POINT('Ctrl Pts',(0.633747165398412,2.36713218480707,95.4589391299464));
#11977=CARTESIAN_POINT('Ctrl Pts',(0.555591830508406,2.38805654309395,95.4631693786102));
#11978=CARTESIAN_POINT('Ctrl Pts',(0.476251723940673,2.40514552681904,95.4673996272739));
#11979=CARTESIAN_POINT('Ctrl Pts',(0.39613784477759,2.41826902100138,95.4716298759377));
#11980=CARTESIAN_POINT('Ctrl Pts',(0.316139266183492,2.43137362774046,95.4758540363919));
#11981=CARTESIAN_POINT('Ctrl Pts',(0.235369581833704,2.44052400502367,95.4800781968462));
#11982=CARTESIAN_POINT('Ctrl Pts',(0.154253409653161,2.4456402302077,95.4843023573005));
#11983=CARTESIAN_POINT('Ctrl Pts',(0.0727183290141794,2.45078287712672,
95.4885483325975));
#11984=CARTESIAN_POINT('Ctrl Pts',(-0.00916636924427454,2.45184945747314,
95.4927943078946));
#11985=CARTESIAN_POINT('Ctrl Pts',(-0.0909606451694004,2.44881122404941,
95.4970402831917));
#11986=CARTESIAN_POINT('Ctrl Pts',(-0.172187406493778,2.44579407085176,
95.5012567985669));
#11987=CARTESIAN_POINT('Ctrl Pts',(-0.253324525291851,2.43872890209282,
95.5054733139421));
#11988=CARTESIAN_POINT('Ctrl Pts',(-0.333939373021536,2.42763974780979,
95.5096898293174));
#11989=CARTESIAN_POINT('Ctrl Pts',(-0.414527398361621,2.41655428314009,
95.5139049417622));
#11990=CARTESIAN_POINT('Ctrl Pts',(-0.494593037235437,2.40144755502427,
95.5181200542071));
#11991=CARTESIAN_POINT('Ctrl Pts',(-0.573709388084008,2.38239538868431,
95.5223351666519));
#11992=CARTESIAN_POINT('Ctrl Pts',(-0.652823684959744,2.36334371696565,
95.5265501696665));
#11993=CARTESIAN_POINT('Ctrl Pts',(-0.730988290805646,2.3403469206185,95.530765172681));
#11994=CARTESIAN_POINT('Ctrl Pts',(-0.807788506305003,2.3135314951566,95.5349801756956));
#11995=CARTESIAN_POINT('Ctrl Pts',(-0.885568922283852,2.28637382465379,
95.5392489747568));
#11996=CARTESIAN_POINT('Ctrl Pts',(-0.961949405885977,2.25529950295276,
95.543517773818));
#11997=CARTESIAN_POINT('Ctrl Pts',(-1.03651886293772,2.22049068828813,95.5477865728792));
#11998=CARTESIAN_POINT('Ctrl Pts',(-1.11025597145398,2.18607041159942,95.5520077233617));
#11999=CARTESIAN_POINT('Ctrl Pts',(-1.18222189460279,2.14799887143268,95.5562288738441));
#12000=CARTESIAN_POINT('Ctrl Pts',(-1.25204455727057,2.10649820237501,95.5604500243266));
#12001=CARTESIAN_POINT('Ctrl Pts',(-1.32304946302162,2.06429484056588,95.5647426476771));
#12002=CARTESIAN_POINT('Ctrl Pts',(-1.39183743708825,2.01854542708319,95.5690352710277));
#12003=CARTESIAN_POINT('Ctrl Pts',(-1.45805013883951,1.96952787302695,95.5733278943783));
#12004=CARTESIAN_POINT('Ctrl Pts',(-1.52426284059078,1.92051031897071,95.5776205177289));
#12005=CARTESIAN_POINT('Ctrl Pts',(-1.58789992707878,1.86822499233759,95.5819131410795));
#12006=CARTESIAN_POINT('Ctrl Pts',(-1.64864180721736,1.81298936607336,95.58620576443));
#12007=CARTESIAN_POINT('Ctrl Pts',(-1.70760629626205,1.75937001032896,95.5903727797077));
#12008=CARTESIAN_POINT('Ctrl Pts',(-1.76407935781339,1.70275513819415,95.5945397949853));
#12009=CARTESIAN_POINT('Ctrl Pts',(-1.81773405989184,1.64340899885242,95.5987068102629));
#12010=CARTESIAN_POINT('Ctrl Pts',(-1.87129837357761,1.58416283587697,95.602866805656));
#12011=CARTESIAN_POINT('Ctrl Pts',(-1.92205344084515,1.52219489923289,95.607026801049));
#12012=CARTESIAN_POINT('Ctrl Pts',(-1.9697069062043,1.45780827053872,95.6111867964421));
#12013=CARTESIAN_POINT('Ctrl Pts',(-2.01731526164687,1.39348259177603,95.6153428538835));
#12014=CARTESIAN_POINT('Ctrl Pts',(-2.0618275538357,1.32674314536301,95.6194989113249));
#12015=CARTESIAN_POINT('Ctrl Pts',(-2.10299044589106,1.25792743609913,95.6236549687662));
#12016=CARTESIAN_POINT('Ctrl Pts',(-2.14412787968735,1.1891542876969,95.627808455786));
#12017=CARTESIAN_POINT('Ctrl Pts',(-2.18191977756558,1.11830783541453,95.6319619428058));
#12018=CARTESIAN_POINT('Ctrl Pts',(-2.21615600002487,1.04575467178195,95.6361154298256));
#12019=CARTESIAN_POINT('Ctrl Pts',(-2.25038227886981,0.97322258058748,95.640267710501));
#12020=CARTESIAN_POINT('Ctrl Pts',(-2.28105472888102,0.898985196785917,
95.6444199911764));
#12021=CARTESIAN_POINT('Ctrl Pts',(-2.30800983772869,0.823432352380932,
95.6485722718519));
#12022=CARTESIAN_POINT('Ctrl Pts',(-2.33497855028516,0.747841377953894,
95.652726648101));
#12023=CARTESIAN_POINT('Ctrl Pts',(-2.35822600958895,0.67093406872749,95.6568810243501));
#12024=CARTESIAN_POINT('Ctrl Pts',(-2.37763779980332,0.593117815401322,
95.6610354005993));
#12025=CARTESIAN_POINT('Ctrl Pts',(-2.39705492978061,0.5152801565098,95.6651909196273));
#12026=CARTESIAN_POINT('Ctrl Pts',(-2.41263419272981,0.436533526438097,
95.6693464386554));
#12027=CARTESIAN_POINT('Ctrl Pts',(-2.42431228652839,0.357295658226464,
95.6735019576834));
#12028=CARTESIAN_POINT('Ctrl Pts',(-2.43600468979453,0.277960697824659,
95.6776625685754));
#12029=CARTESIAN_POINT('Ctrl Pts',(-2.44378633365139,0.198133775714215,
95.6818231794673));
#12030=CARTESIAN_POINT('Ctrl Pts',(-2.44764586026056,0.118237019369414,
95.6859837903593));
#12031=CARTESIAN_POINT('Ctrl Pts',(-2.44958225649275,0.0781513317663674,
95.6880712461721));
#12032=CARTESIAN_POINT('Ctrl Pts',(-2.45053219281933,0.0380480649410048,
95.6901587019849));
#12033=CARTESIAN_POINT('Ctrl Pts',(-2.45049916761641,-0.00201978001007322,
95.6922461577976));
#12034=CARTESIAN_POINT('',(-2.4504995008409,0.00156409031575664,96.4922461578689));
#12035=CARTESIAN_POINT('Ctrl Pts',(-2.45049916761573,-0.00201978082743583,
95.6922461578402));
#12036=CARTESIAN_POINT('Ctrl Pts',(-2.45039286942341,-0.13098606680677,
95.6989650473549));
#12037=CARTESIAN_POINT('Ctrl Pts',(-2.44010274194984,-0.259545593344348,
95.7056839368697));
#12038=CARTESIAN_POINT('Ctrl Pts',(-2.41983633006845,-0.386448425641583,
95.7124028263845));
#12039=CARTESIAN_POINT('Ctrl Pts',(-2.41876093423285,-0.393182265759761,
95.7127593505609));
#12040=CARTESIAN_POINT('Ctrl Pts',(-2.41765745717425,-0.399911448803464,
95.7131158747373));
#12041=CARTESIAN_POINT('Ctrl Pts',(-2.41652593285027,-0.406635790188365,
95.7134723989137));
#12042=CARTESIAN_POINT('Ctrl Pts',(-2.40309990879575,-0.48642300047744,
95.7177027120113));
#12043=CARTESIAN_POINT('Ctrl Pts',(-2.38569278236315,-0.565694995452241,
95.721933025109));
#12044=CARTESIAN_POINT('Ctrl Pts',(-2.36435689547696,-0.644023851119309,
95.7261633382066));
#12045=CARTESIAN_POINT('Ctrl Pts',(-2.34305171746302,-0.722239967586223,
95.7303875625888));
#12046=CARTESIAN_POINT('Ctrl Pts',(-2.31782913063727,-0.799515195737968,
95.7346117869709));
#12047=CARTESIAN_POINT('Ctrl Pts',(-2.28879279169395,-0.875430069560003,
95.7388360113531));
#12048=CARTESIAN_POINT('Ctrl Pts',(-2.25960705229607,-0.951735547606572,
95.7430819706049));
#12049=CARTESIAN_POINT('Ctrl Pts',(-2.22656827742702,-1.02666616172602,
95.7473279298568));
#12050=CARTESIAN_POINT('Ctrl Pts',(-2.1898330725585,-1.09980969459675,95.7515738891086));
#12051=CARTESIAN_POINT('Ctrl Pts',(-2.15335207173773,-1.17244708132813,
95.7557904667351));
#12052=CARTESIAN_POINT('Ctrl Pts',(-2.11322584874696,-1.24332162042607,
95.7600070443615));
#12053=CARTESIAN_POINT('Ctrl Pts',(-2.06965594912513,-1.31204973314693,
95.7642236219879));
#12054=CARTESIAN_POINT('Ctrl Pts',(-2.02610055385468,-1.38075496638667,
95.7684387959223));
#12055=CARTESIAN_POINT('Ctrl Pts',(-1.97910400733192,-1.44731479963216,
95.7726539698566));
#12056=CARTESIAN_POINT('Ctrl Pts',(-1.92891259328625,-1.5113723755123,95.776869143791));
#12057=CARTESIAN_POINT('Ctrl Pts',(-1.87872249225802,-1.57542827563344,
95.7810842074555));
#12058=CARTESIAN_POINT('Ctrl Pts',(-1.82533797761367,-1.63698168303703,
95.7852992711201));
#12059=CARTESIAN_POINT('Ctrl Pts',(-1.76904635879676,-1.69570788475726,
95.7895143347847));
#12060=CARTESIAN_POINT('Ctrl Pts',(-1.7120381014728,-1.755181719223,95.793783059669));
#12061=CARTESIAN_POINT('Ctrl Pts',(-1.65204852131537,-1.81175548766543,
95.7980517845534));
#12062=CARTESIAN_POINT('Ctrl Pts',(-1.58941403354977,-1.86513090156027,
95.8023205094378));
#12063=CARTESIAN_POINT('Ctrl Pts',(-1.52747674843449,-1.91791217824163,
95.8065417179074));
#12064=CARTESIAN_POINT('Ctrl Pts',(-1.4629535570336,-1.96756571271323,95.8107629263769));
#12065=CARTESIAN_POINT('Ctrl Pts',(-1.39620106610138,-2.01384528527326,
95.8149841348465));
#12066=CARTESIAN_POINT('Ctrl Pts',(-1.32832146699419,-2.06090628312303,
95.8192766179382));
#12067=CARTESIAN_POINT('Ctrl Pts',(-1.25813701629652,-2.10447806251757,
95.82356910103));
#12068=CARTESIAN_POINT('Ctrl Pts',(-1.18604930007241,-2.14435008984022,
95.8278615841218));
#12069=CARTESIAN_POINT('Ctrl Pts',(-1.11396158384829,-2.18422211716287,
95.8321540672136));
#12070=CARTESIAN_POINT('Ctrl Pts',(-1.03997107915681,-2.22039423329967,
95.8364465503054));
#12071=CARTESIAN_POINT('Ctrl Pts',(-0.964499265121369,-2.25270757480423,
95.8407390333972));
#12072=CARTESIAN_POINT('Ctrl Pts',(-0.890120388998835,-2.28455297372023,
95.8449693553025));
#12073=CARTESIAN_POINT('Ctrl Pts',(-0.814022428920014,-2.31277072852657,
95.8491996772077));
#12074=CARTESIAN_POINT('Ctrl Pts',(-0.736593675473764,-2.33717350816152,
95.8534299991129));
#12075=CARTESIAN_POINT('Ctrl Pts',(-0.659276337203014,-2.3615411737096,
95.8576542338472));
#12076=CARTESIAN_POINT('Ctrl Pts',(-0.580632448559504,-2.38210462784626,
95.8618784685816));
#12077=CARTESIAN_POINT('Ctrl Pts',(-0.501070928541947,-2.39872428064797,
95.8661027033159));
#12078=CARTESIAN_POINT('Ctrl Pts',(-0.421100282328117,-2.41542939606192,
95.8703486601728));
#12079=CARTESIAN_POINT('Ctrl Pts',(-0.340202976699437,-2.42814984239434,
95.8745946170296));
#12080=CARTESIAN_POINT('Ctrl Pts',(-0.258810455535648,-2.43679449238245,
95.8788405738865));
#12081=CARTESIAN_POINT('Ctrl Pts',(-0.177980848947033,-2.44537935555715,
95.8830571655024));
#12082=CARTESIAN_POINT('Ctrl Pts',(-0.0966633236958435,-2.44994457149375,
95.8872737571182));
#12083=CARTESIAN_POINT('Ctrl Pts',(-0.0152895333809833,-2.45045230114136,
95.8914903487341));
#12084=CARTESIAN_POINT('Ctrl Pts',(0.0660571933746435,-2.4509598619266,
95.8957055379822));
#12085=CARTESIAN_POINT('Ctrl Pts',(0.147459683251942,-2.44741261327396,
95.8999207272304));
#12086=CARTESIAN_POINT('Ctrl Pts',(0.22848457369334,-2.43982479895262,95.9041359164785));
#12087=CARTESIAN_POINT('Ctrl Pts',(0.309507369405125,-2.4322371807984,95.9083509967517));
#12088=CARTESIAN_POINT('Ctrl Pts',(0.390152122053498,-2.42060924909943,
95.9125660770249));
#12089=CARTESIAN_POINT('Ctrl Pts',(0.469990329323206,-2.40500713935378,
95.9167811572982));
#12090=CARTESIAN_POINT('Ctrl Pts',(0.550844327114181,-2.38920652220506,
95.9210498665134));
#12091=CARTESIAN_POINT('Ctrl Pts',(0.630870627672605,-2.36932995950173,
95.9253185757286));
#12092=CARTESIAN_POINT('Ctrl Pts',(0.709636418486952,-2.34549918003759,
95.9295872849438));
#12093=CARTESIAN_POINT('Ctrl Pts',(0.787526091712351,-2.32193347205729,
95.9338085129977));
#12094=CARTESIAN_POINT('Ctrl Pts',(0.864182735228015,-2.29450129435288,
95.9380297410515));
#12095=CARTESIAN_POINT('Ctrl Pts',(0.939206411711731,-2.26336951605335,
95.9422509691054));
#12096=CARTESIAN_POINT('Ctrl Pts',(1.01549590867909,-2.23171247367039,95.9465434189013));
#12097=CARTESIAN_POINT('Ctrl Pts',(1.09009637187876,-2.19623005162782,95.9508358686972));
#12098=CARTESIAN_POINT('Ctrl Pts',(1.16261358044973,-2.15714624273689,95.9551283184931));
#12099=CARTESIAN_POINT('Ctrl Pts',(1.23513078902069,-2.11806243384596,95.959420768289));
#12100=CARTESIAN_POINT('Ctrl Pts',(1.30556435121456,-2.07537755338223,95.963713218085));
#12101=CARTESIAN_POINT('Ctrl Pts',(1.3735527561667,-2.02936026274953,95.9680056678809));
#12102=CARTESIAN_POINT('Ctrl Pts',(1.44054749437405,-1.98401552578859,95.9722353824998));
#12103=CARTESIAN_POINT('Ctrl Pts',(1.50542090464869,-1.93526406958689,95.9764650971188));
#12104=CARTESIAN_POINT('Ctrl Pts',(1.56780550832432,-1.88333112809933,95.9806948117378));
#12105=CARTESIAN_POINT('Ctrl Pts',(1.63010029878634,-1.8314729528857,95.9849184369654));
#12106=CARTESIAN_POINT('Ctrl Pts',(1.68991304412632,-1.77644268409849,95.9891420621931));
#12107=CARTESIAN_POINT('Ctrl Pts',(1.74690526492059,-1.71850872717968,95.9933656874208));
#12108=CARTESIAN_POINT('Ctrl Pts',(1.80420087380922,-1.66026636899938,95.9976117963768));
#12109=CARTESIAN_POINT('Ctrl Pts',(1.85864544215238,-1.5990895796545,96.0018579053327));
#12110=CARTESIAN_POINT('Ctrl Pts',(1.90992890972816,-1.53529209266009,96.0061040142887));
#12111=CARTESIAN_POINT('Ctrl Pts',(1.96084850111177,-1.47194727370347,96.0103199954466));
#12112=CARTESIAN_POINT('Ctrl Pts',(2.0086514099609,-1.40601919440417,96.0145359766045));
#12113=CARTESIAN_POINT('Ctrl Pts',(2.05307245712827,-1.33785041607098,96.0187519577623));
#12114=CARTESIAN_POINT('Ctrl Pts',(2.09747873885647,-1.26970429686029,96.0229665375392));
#12115=CARTESIAN_POINT('Ctrl Pts',(2.13850513733498,-1.19931934717004,96.027181117316));
#12116=CARTESIAN_POINT('Ctrl Pts',(2.1759293612013,-1.12706772869339,96.0313956970928));
#12117=CARTESIAN_POINT('Ctrl Pts',(2.21335263338379,-1.05481794754802,96.0356101696945));
#12118=CARTESIAN_POINT('Ctrl Pts',(2.24717370001357,-0.980702005661079,
96.0398246422961));
#12119=CARTESIAN_POINT('Ctrl Pts',(2.27721654987097,-0.905116033994397,
96.0440391148978));
#12120=CARTESIAN_POINT('Ctrl Pts',(2.30765117962308,-0.828544368088942,
96.0483085471867));
#12121=CARTESIAN_POINT('Ctrl Pts',(2.33420813985629,-0.750464502345619,
96.0525779794756));
#12122=CARTESIAN_POINT('Ctrl Pts',(2.35675574199825,-0.671306653146129,
96.0568474117645));
#12123=CARTESIAN_POINT('Ctrl Pts',(2.37904561615414,-0.593053609385728,
96.0610680427583));
#12124=CARTESIAN_POINT('Ctrl Pts',(2.39741727621602,-0.513747573025114,
96.0652886737521));
#12125=CARTESIAN_POINT('Ctrl Pts',(2.41179491259472,-0.433815109905383,
96.0695093047459));
#12126=CARTESIAN_POINT('Ctrl Pts',(2.4264219123778,-0.352496311048758,96.0738031376823));
#12127=CARTESIAN_POINT('Ctrl Pts',(2.43691496711382,-0.27052964985659,96.0780969706188));
#12128=CARTESIAN_POINT('Ctrl Pts',(2.44324939404552,-0.188368385076181,
96.0823908035552));
#12129=CARTESIAN_POINT('Ctrl Pts',(2.44958382097722,-0.106207120295777,
96.0866846364917));
#12130=CARTESIAN_POINT('Ctrl Pts',(2.45175967380902,-0.0238517532380541,
96.0909784694281));
#12131=CARTESIAN_POINT('Ctrl Pts',(2.44980763300449,0.058247843504729,96.0952723023645));
#12132=CARTESIAN_POINT('Ctrl Pts',(2.44788415030091,0.139146333914604,96.0995033170883));
#12133=CARTESIAN_POINT('Ctrl Pts',(2.44194554762611,0.220101762188912,96.103734331812));
#12134=CARTESIAN_POINT('Ctrl Pts',(2.43198272711111,0.300682997579212,96.1079653465357));
#12135=CARTESIAN_POINT('Ctrl Pts',(2.42203424890235,0.381148229599407,96.1121902703629));
#12136=CARTESIAN_POINT('Ctrl Pts',(2.40807311503856,0.461239881027298,96.1164151941901));
#12137=CARTESIAN_POINT('Ctrl Pts',(2.39014222383595,0.540527889971056,96.1206401180173));
#12138=CARTESIAN_POINT('Ctrl Pts',(2.37212280000661,0.620207378380073,96.1248859021352));
#12139=CARTESIAN_POINT('Ctrl Pts',(2.35009431810921,0.699074790646947,96.1291316862532));
#12140=CARTESIAN_POINT('Ctrl Pts',(2.32415305311903,0.776699965029916,96.1333774703711));
#12141=CARTESIAN_POINT('Ctrl Pts',(2.29838602586768,0.853803760256331,96.137594737151));
#12142=CARTESIAN_POINT('Ctrl Pts',(2.2687587642877,0.92968150691831,96.1418120039309));
#12143=CARTESIAN_POINT('Ctrl Pts',(2.23541615742505,1.00392472482903,96.1460292707107));
#12144=CARTESIAN_POINT('Ctrl Pts',(2.2020846907964,1.07814313703621,96.1502451284424));
#12145=CARTESIAN_POINT('Ctrl Pts',(2.16504053434128,1.15072768114341,96.1544609861741));
#12146=CARTESIAN_POINT('Ctrl Pts',(2.1244766657595,1.22128995191289,96.1586768439058));
#12147=CARTESIAN_POINT('Ctrl Pts',(2.08391391824573,1.2918502725453,96.1628925851234));
#12148=CARTESIAN_POINT('Ctrl Pts',(2.03983188467375,1.36038802835168,96.167108326341));
#12149=CARTESIAN_POINT('Ctrl Pts',(1.99246873056694,1.42654078375383,96.1713240675586));
#12150=CARTESIAN_POINT('Ctrl Pts',(1.94451951631013,1.49351209726268,96.1755919733327));
#12151=CARTESIAN_POINT('Ctrl Pts',(1.89320769161054,1.55803857359002,96.1798598791068));
#12152=CARTESIAN_POINT('Ctrl Pts',(1.83882348335499,1.61977728316649,96.184127784881));
#12153=CARTESIAN_POINT('Ctrl Pts',(1.78502596840533,1.68084995955457,96.1883496487649));
#12154=CARTESIAN_POINT('Ctrl Pts',(1.72822241336629,1.73919443460736,96.1925715126487));
#12155=CARTESIAN_POINT('Ctrl Pts',(1.66873075083071,1.79451607160036,96.1967933765326));
#12156=CARTESIAN_POINT('Ctrl Pts',(1.60826590133106,1.8507426807131,96.2010843032519));
#12157=CARTESIAN_POINT('Ctrl Pts',(1.54502459272168,1.90384634459835,96.2053752299711));
#12158=CARTESIAN_POINT('Ctrl Pts',(1.47937379800963,1.95356172560853,96.2096661566904));
#12159=CARTESIAN_POINT('Ctrl Pts',(1.41372300329758,2.0032771066187,96.2139570834096));
#12160=CARTESIAN_POINT('Ctrl Pts',(1.34566317058895,2.0496039797444,96.2182480101289));
#12161=CARTESIAN_POINT('Ctrl Pts',(1.27558828756782,2.09232520670659,96.2225389368481));
#12162=CARTESIAN_POINT('Ctrl Pts',(1.20649747055948,2.13444649677749,96.2267696058122));
#12163=CARTESIAN_POINT('Ctrl Pts',(1.13518812848537,2.17322115194946,96.2310002747762));
#12164=CARTESIAN_POINT('Ctrl Pts',(1.06201801927646,2.20840847144094,96.2352309437403));
#12165=CARTESIAN_POINT('Ctrl Pts',(0.988953036616486,2.24354523584231,96.2394555343257));
#12166=CARTESIAN_POINT('Ctrl Pts',(0.914033011978542,2.27510470098837,96.2436801249111));
#12167=CARTESIAN_POINT('Ctrl Pts',(0.837642911513598,2.30289048866659,96.2479047154965));
#12168=CARTESIAN_POINT('Ctrl Pts',(0.760868049573986,2.33081622773349,96.2521505844896));
#12169=CARTESIAN_POINT('Ctrl Pts',(0.682608666046283,2.35492991716484,96.2563964534828));
#12170=CARTESIAN_POINT('Ctrl Pts',(0.603278783409193,2.37507999012419,96.2606423224759));
#12171=CARTESIAN_POINT('Ctrl Pts',(0.524488924239545,2.39509289519791,96.2648592885031));
#12172=CARTESIAN_POINT('Ctrl Pts',(0.444643551593448,2.41119586310372,96.2690762545303));
#12173=CARTESIAN_POINT('Ctrl Pts',(0.364164608657989,2.42328999251038,96.2732932205575));
#12174=CARTESIAN_POINT('Ctrl Pts',(0.28371231307121,2.43538011743499,96.2775087903069));
#12175=CARTESIAN_POINT('Ctrl Pts',(0.20262732331826,2.44346397071098,96.2817243600562));
#12176=CARTESIAN_POINT('Ctrl Pts',(0.12134068543824,2.44749396078057,96.2859399298056));
#12177=CARTESIAN_POINT('Ctrl Pts',(0.0400560421298898,2.45152385196424,
96.2901553961154));
#12178=CARTESIAN_POINT('Ctrl Pts',(-0.0414297749209072,2.45150005576119,
96.2943708624251));
#12179=CARTESIAN_POINT('Ctrl Pts',(-0.122683145042565,2.44742703587307,
96.2985863287349));
#12180=CARTESIAN_POINT('Ctrl Pts',(-0.204954313683714,2.44330299639517,
96.3028545989513));
#12181=CARTESIAN_POINT('Ctrl Pts',(-0.28698668293458,2.43502758941941,96.3071228691677));
#12182=CARTESIAN_POINT('Ctrl Pts',(-0.368334710253303,2.42265965237022,
96.3113911393841));
#12183=CARTESIAN_POINT('Ctrl Pts',(-0.448793709332226,2.41042688080282,
96.315612762953));
#12184=CARTESIAN_POINT('Ctrl Pts',(-0.528582802708336,2.39419075039301,
96.3198343865219));
#12185=CARTESIAN_POINT('Ctrl Pts',(-0.607282300202502,2.3740594891158,96.3240560100907));
#12186=CARTESIAN_POINT('Ctrl Pts',(-0.687286177751075,2.35359456858387,
96.3283476036309));
#12187=CARTESIAN_POINT('Ctrl Pts',(-0.766163533826442,2.3291043757461,96.3326391971711));
#12188=CARTESIAN_POINT('Ctrl Pts',(-0.843492566232783,2.30075434166928,
96.3369307907112));
#12189=CARTESIAN_POINT('Ctrl Pts',(-0.920821598639124,2.27240430759245,
96.3412223842514));
#12190=CARTESIAN_POINT('Ctrl Pts',(-0.996601875438346,2.24019468810563,
96.3455139777916));
#12191=CARTESIAN_POINT('Ctrl Pts',(-1.07043757630683,2.20433972999408,96.3498055713318));
#12192=CARTESIAN_POINT('Ctrl Pts',(-1.14314574372558,2.16903230734483,96.3540316286176));
#12193=CARTESIAN_POINT('Ctrl Pts',(-1.21424392411789,2.13005630248263,96.3582576859035));
#12194=CARTESIAN_POINT('Ctrl Pts',(-1.28333670844218,2.08758164936483,96.3624837431893));
#12195=CARTESIAN_POINT('Ctrl Pts',(-1.35232977148203,2.04516829971029,96.366703701027));
#12196=CARTESIAN_POINT('Ctrl Pts',(-1.41932279274412,1.99926657190157,96.3709236588646));
#12197=CARTESIAN_POINT('Ctrl Pts',(-1.48394286364748,1.95009328685315,96.3751436167022));
#12198=CARTESIAN_POINT('Ctrl Pts',(-1.5489774061417,1.90060460552929,96.3793906412486));
#12199=CARTESIAN_POINT('Ctrl Pts',(-1.61160801401144,1.84780245084342,96.383637665795));
#12200=CARTESIAN_POINT('Ctrl Pts',(-1.67148228780926,1.79195346243699,96.3878846903414));
#12201=CARTESIAN_POINT('Ctrl Pts',(-1.73086723760558,1.73656090128643,96.3920970059733));
#12202=CARTESIAN_POINT('Ctrl Pts',(-1.78754039387152,1.6781714474271,96.3963093216053));
#12203=CARTESIAN_POINT('Ctrl Pts',(-1.84119080798415,1.6170858538107,96.4005216372372));
#12204=CARTESIAN_POINT('Ctrl Pts',(-1.89482348312035,1.55602045753896,96.4047325601089));
#12205=CARTESIAN_POINT('Ctrl Pts',(-1.94543509325173,1.4922610416411,96.4089434829805));
#12206=CARTESIAN_POINT('Ctrl Pts',(-1.99275291278564,1.4261437790715,96.4131544058522));
#12207=CARTESIAN_POINT('Ctrl Pts',(-2.04006967858883,1.36002798888147,96.4173652349498));
#12208=CARTESIAN_POINT('Ctrl Pts',(-2.08409252918242,1.29155483616462,96.4215760640475));
#12209=CARTESIAN_POINT('Ctrl Pts',(-2.12459113053335,1.2210908148287,96.4257868931452));
#12210=CARTESIAN_POINT('Ctrl Pts',(-2.16569513849314,1.14957343898717,96.4300606692011));
#12211=CARTESIAN_POINT('Ctrl Pts',(-2.20316839932188,1.07600560064285,96.4343344452569));
#12212=CARTESIAN_POINT('Ctrl Pts',(-2.23681857746337,1.00079613384282,96.4386082213128));
#12213=CARTESIAN_POINT('Ctrl Pts',(-2.27002217192328,0.926584799071467,
96.4428252785412));
#12214=CARTESIAN_POINT('Ctrl Pts',(-2.29950344177342,0.850775612650433,
96.4470423357697));
#12215=CARTESIAN_POINT('Ctrl Pts',(-2.32512700126326,0.77377947633453,96.4512593929982));
#12216=CARTESIAN_POINT('Ctrl Pts',(-2.35126751066703,0.695229959191192,
96.4555615284677));
#12217=CARTESIAN_POINT('Ctrl Pts',(-2.37339281243798,0.615445568424357,
96.4598636639372));
#12218=CARTESIAN_POINT('Ctrl Pts',(-2.39141369418015,0.534874558459875,
96.4641657994068));
#12219=CARTESIAN_POINT('Ctrl Pts',(-2.40943457592232,0.454303548495393,
96.4684679348763));
#12220=CARTESIAN_POINT('Ctrl Pts',(-2.42335102008677,0.372946431201083,
96.4727700703458));
#12221=CARTESIAN_POINT('Ctrl Pts',(-2.43312971698948,0.291255953248524,
96.4770722058154));
#12222=CARTESIAN_POINT('Ctrl Pts',(-2.44462644760282,0.195213154495219,
96.4821301898236));
#12223=CARTESIAN_POINT('Ctrl Pts',(-2.45043764111995,0.09848123134268,96.4871881738319));
#12224=CARTESIAN_POINT('Ctrl Pts',(-2.45049950084054,0.00156409086877713,
96.4922461578401));
#12225=CARTESIAN_POINT('',(0.587285094939578,-2.3790852164775,96.7230107090999));
#12226=CARTESIAN_POINT('Ctrl Pts',(-2.4504995008409,0.00156409031575633,
96.492246157869));
#12227=CARTESIAN_POINT('Ctrl Pts',(-2.45055056711173,-0.0784427161471055,
96.496421612754));
#12228=CARTESIAN_POINT('Ctrl Pts',(-2.44667918136308,-0.15860325583324,
96.5005970676391));
#12229=CARTESIAN_POINT('Ctrl Pts',(-2.43886659932268,-0.238495200597942,
96.5047725225241));
#12230=CARTESIAN_POINT('Ctrl Pts',(-2.43106488590343,-0.31827600217378,
96.5089421686462));
#12231=CARTESIAN_POINT('Ctrl Pts',(-2.41933291332766,-0.397788479137657,
96.5131118147683));
#12232=CARTESIAN_POINT('Ctrl Pts',(-2.40370395745537,-0.476610464544575,
96.5172814608903));
#12233=CARTESIAN_POINT('Ctrl Pts',(-2.38808705541766,-0.555371658483321,
96.5214478911722));
#12234=CARTESIAN_POINT('Ctrl Pts',(-2.3685792236406,-0.633442950428641,
96.525614321454));
#12235=CARTESIAN_POINT('Ctrl Pts',(-2.34526538839251,-0.710408690830951,
96.5297807517359));
#12236=CARTESIAN_POINT('Ctrl Pts',(-2.32196196211607,-0.787340068195104,
96.5339453218239));
#12237=CARTESIAN_POINT('Ctrl Pts',(-2.29485604239929,-0.86316641685313,
96.5381098919118));
#12238=CARTESIAN_POINT('Ctrl Pts',(-2.26408296841375,-0.937485233024396,
96.5422744619997));
#12239=CARTESIAN_POINT('Ctrl Pts',(-2.23331364036793,-1.01179500252692,
96.5464385251436));
#12240=CARTESIAN_POINT('Ctrl Pts',(-2.19887822823037,-1.08459716302059,
96.5506025882874));
#12241=CARTESIAN_POINT('Ctrl Pts',(-2.16096037609839,-1.15550876367629,
96.5547666514312));
#12242=CARTESIAN_POINT('Ctrl Pts',(-2.12300937877822,-1.22648235039439,
96.5589343545138));
#12243=CARTESIAN_POINT('Ctrl Pts',(-2.08157008507773,-1.29556165309398,
96.5631020575963));
#12244=CARTESIAN_POINT('Ctrl Pts',(-2.03687197920892,-1.36238863409584,
96.5672697606788));
#12245=CARTESIAN_POINT('Ctrl Pts',(-1.99215559824111,-1.42924293772516,
96.5714391677526));
#12246=CARTESIAN_POINT('Ctrl Pts',(-1.94417803708808,-1.49384270182766,
96.5756085748265));
#12247=CARTESIAN_POINT('Ctrl Pts',(-1.8932104343097,-1.55586133746581,96.5797779819004));
#12248=CARTESIAN_POINT('Ctrl Pts',(-1.84215338914959,-1.61798880879919,
96.5839547058124));
#12249=CARTESIAN_POINT('Ctrl Pts',(-1.78809614139987,-1.67752574799975,
96.5881314297244));
#12250=CARTESIAN_POINT('Ctrl Pts',(-1.73134796928215,-1.73418120715875,
96.5923081536364));
#12251=CARTESIAN_POINT('Ctrl Pts',(-1.67686192616905,-1.7885782330916,96.5963183825239));
#12252=CARTESIAN_POINT('Ctrl Pts',(-1.61989574806037,-1.84031894392783,
96.6003286114115));
#12253=CARTESIAN_POINT('Ctrl Pts',(-1.5607502269691,-1.88918209260407,96.604338840299));
#12254=CARTESIAN_POINT('Ctrl Pts',(-1.49897684234944,-1.94021625412997,
96.6085272455563));
#12255=CARTESIAN_POINT('Ctrl Pts',(-1.43457128275649,-1.98832161640094,
96.6127156508135));
#12256=CARTESIAN_POINT('Ctrl Pts',(-1.3678458339106,-2.03321125922847,96.6169040560708));
#12257=CARTESIAN_POINT('Ctrl Pts',(-1.30121544998754,-2.0780369469908,96.6210864940333));
#12258=CARTESIAN_POINT('Ctrl Pts',(-1.23227212844164,-2.1196557468126,96.6252689319957));
#12259=CARTESIAN_POINT('Ctrl Pts',(-1.16136171467528,-2.15782047855851,
96.6294513699582));
#12260=CARTESIAN_POINT('Ctrl Pts',(-1.09053096525414,-2.19594233411455,
96.6336291091584));
#12261=CARTESIAN_POINT('Ctrl Pts',(-1.01773792972895,-2.23061760584037,
96.6378068483585));
#12262=CARTESIAN_POINT('Ctrl Pts',(-0.943356620376197,-2.26164288445201,
96.6419845875587));
#12263=CARTESIAN_POINT('Ctrl Pts',(-0.869019872293292,-2.29264957605807,
96.6461598239074));
#12264=CARTESIAN_POINT('Ctrl Pts',(-0.793097175745001,-2.32001043058752,
96.6503350602562));
#12265=CARTESIAN_POINT('Ctrl Pts',(-0.715985096995049,-2.34356898573116,
96.6545102966049));
#12266=CARTESIAN_POINT('Ctrl Pts',(-0.638894427529492,-2.36712100011212,
96.6586843737471));
#12267=CARTESIAN_POINT('Ctrl Pts',(-0.560615485706379,-2.38687267232038,
96.6628584508894));
#12268=CARTESIAN_POINT('Ctrl Pts',(-0.481561179585564,-2.40271702044085,
96.6670325280317));
#12269=CARTESIAN_POINT('Ctrl Pts',(-0.402503410156221,-2.41856206269007,
96.671206788037));
#12270=CARTESIAN_POINT('Ctrl Pts',(-0.322670675394702,-2.43049935006043,
96.6753810480424));
#12271=CARTESIAN_POINT('Ctrl Pts',(-0.242485731844522,-2.43847307138132,
96.6795553080478));
#12272=CARTESIAN_POINT('Ctrl Pts',(-0.162222448688313,-2.44645458292015,
96.6837336462488));
#12273=CARTESIAN_POINT('Ctrl Pts',(-0.0816067436711042,-2.45046475337635,
96.6879119844498));
#12274=CARTESIAN_POINT('Ctrl Pts',(-0.00106534483579401,-2.45049976842284,
96.6920903226507));
#12275=CARTESIAN_POINT('Ctrl Pts',(0.0795205022898598,-2.45053480279304,
96.6962709667465));
#12276=CARTESIAN_POINT('Ctrl Pts',(0.160031487260103,-2.44659034078073,
96.7004516108422));
#12277=CARTESIAN_POINT('Ctrl Pts',(0.240044580309798,-2.43871458958688,
96.7046322549379));
#12278=CARTESIAN_POINT('Ctrl Pts',(0.320185460621495,-2.4308262601931,96.7088195758542));
#12279=CARTESIAN_POINT('Ctrl Pts',(0.399826393045886,-2.41899418310751,
96.7130068967705));
#12280=CARTESIAN_POINT('Ctrl Pts',(0.478553795723909,-2.40331781389775,
96.7171942176868));
#12281=CARTESIAN_POINT('Ctrl Pts',(0.515006479975092,-2.3960592772565,96.7191330481578));
#12282=CARTESIAN_POINT('Ctrl Pts',(0.551263515538092,-2.38797726310625,
96.7210718786289));
#12283=CARTESIAN_POINT('Ctrl Pts',(0.587285094939578,-2.3790852164775,96.7230107090999));
#12284=CARTESIAN_POINT('',(-1.51542342753571,-1.92573157144912,96.7230113585667));
#12285=CARTESIAN_POINT('Origin',(0.,0.,96.7230113585667));
#12286=CARTESIAN_POINT('',(-2.45326580686465,0.00155908382959414,96.6079011502643));
#12287=CARTESIAN_POINT('Ctrl Pts',(-1.51542342753571,-1.92573157144912,
96.7230113585667));
#12288=CARTESIAN_POINT('Ctrl Pts',(-2.09575769702644,-1.46904686999497,
96.6846412891326));
#12289=CARTESIAN_POINT('Ctrl Pts',(-2.44856389678248,-0.732572859810942,
96.6462712196984));
#12290=CARTESIAN_POINT('Ctrl Pts',(-2.45326580686465,0.00155908382959414,
96.6079011502643));
#12291=CARTESIAN_POINT('',(-2.45049904460346,-0.0021638848246924,95.8079011502643));
#12292=CARTESIAN_POINT('Ctrl Pts',(-2.45326580686465,0.00155908382959414,
96.6079011502643));
#12293=CARTESIAN_POINT('Ctrl Pts',(-2.45376236076432,0.0790884438376486,
96.6038490082039));
#12294=CARTESIAN_POINT('Ctrl Pts',(-2.41493050276558,0.96797952800282,96.5573746546489));
#12295=CARTESIAN_POINT('Ctrl Pts',(-1.32808179084826,2.5780765389172,96.4684780895995));
#12296=CARTESIAN_POINT('Ctrl Pts',(1.44992071634245,2.50904073301675,96.3412114551158));
#12297=CARTESIAN_POINT('Ctrl Pts',(2.89498768616649,0.137905795112437,96.2139448206323));
#12298=CARTESIAN_POINT('Ctrl Pts',(1.68109423068961,-2.3612860757178,96.0866781861487));
#12299=CARTESIAN_POINT('Ctrl Pts',(-1.07735437651229,-2.69063721300502,
95.9594115516649));
#12300=CARTESIAN_POINT('Ctrl Pts',(-2.36874873876448,-1.12659486130387,
95.8664858730369));
#12301=CARTESIAN_POINT('Ctrl Pts',(-2.45304861271184,-0.157484081137518,
95.8159824059033));
#12302=CARTESIAN_POINT('Ctrl Pts',(-2.45162076832419,-0.00216487534984322,
95.8079011502643));
#12303=CARTESIAN_POINT('',(-2.45049997932286,-0.000318337325309961,95.007901150296));
#12304=CARTESIAN_POINT('Ctrl Pts',(-2.45049904460346,-0.0021638848246924,
95.8079011502643));
#12305=CARTESIAN_POINT('Ctrl Pts',(-2.45057186376826,0.0803004366316179,
95.8036085307824));
#12306=CARTESIAN_POINT('Ctrl Pts',(-2.4464772602671,0.162905211040847,95.7993159113004));
#12307=CARTESIAN_POINT('Ctrl Pts',(-2.43820288991152,0.245187515235034,
95.7950232918185));
#12308=CARTESIAN_POINT('Ctrl Pts',(-2.43019164838499,0.324853203853163,
95.7908671796343));
#12309=CARTESIAN_POINT('Ctrl Pts',(-2.41826252366292,0.404216102305202,
95.7867110674501));
#12310=CARTESIAN_POINT('Ctrl Pts',(-2.40245714836581,0.48285598294523,95.7825549552659));
#12311=CARTESIAN_POINT('Ctrl Pts',(-2.38666006905027,0.561454586805206,
95.7784010245567));
#12312=CARTESIAN_POINT('Ctrl Pts',(-2.3669908693301,0.639330455758143,95.7742470938474));
#12313=CARTESIAN_POINT('Ctrl Pts',(-2.34354268285201,0.716071186161539,
95.7700931631382));
#12314=CARTESIAN_POINT('Ctrl Pts',(-2.32009911712784,0.792796793858927,
95.7659400510121));
#12315=CARTESIAN_POINT('Ctrl Pts',(-2.29287818369623,0.868387248078455,
95.7617869388861));
#12316=CARTESIAN_POINT('Ctrl Pts',(-2.26202308432463,0.942444595709725,
95.75763382676));
#12317=CARTESIAN_POINT('Ctrl Pts',(-2.23116395036688,1.01651162701583,95.7534801715766));
#12318=CARTESIAN_POINT('Ctrl Pts',(-2.19666989485624,1.08904471184014,95.7493265163932));
#12319=CARTESIAN_POINT('Ctrl Pts',(-2.15873188235456,1.15966672372107,95.7451728612098));
#12320=CARTESIAN_POINT('Ctrl Pts',(-2.12075375704251,1.23036340602312,95.7410148142628));
#12321=CARTESIAN_POINT('Ctrl Pts',(-2.07932464005412,1.29914456203895,95.7368567673158));
#12322=CARTESIAN_POINT('Ctrl Pts',(-2.03468055917747,1.36565928111856,95.7326987203687));
#12323=CARTESIAN_POINT('Ctrl Pts',(-1.99000792123275,1.43221654705597,95.7285380136821));
#12324=CARTESIAN_POINT('Ctrl Pts',(-1.94211651827156,1.49650411024708,95.7243773069955));
#12325=CARTESIAN_POINT('Ctrl Pts',(-1.89128306807474,1.55820364728549,95.7202166003089));
#12326=CARTESIAN_POINT('Ctrl Pts',(-1.84036955354491,1.62000036309615,95.7160493403743));
#12327=CARTESIAN_POINT('Ctrl Pts',(-1.786505075931,1.67920057315013,95.7118820804397));
#12328=CARTESIAN_POINT('Ctrl Pts',(-1.73000296549313,1.73552297287734,95.7077148205051));
#12329=CARTESIAN_POINT('Ctrl Pts',(-1.71718316103575,1.74830200264238,95.7067693079026));
#12330=CARTESIAN_POINT('Ctrl Pts',(-1.70422770338532,1.76093305184202,95.7058237953001));
#12331=CARTESIAN_POINT('Ctrl Pts',(-1.69114047383206,1.77341313510616,95.7048782826977));
#12332=CARTESIAN_POINT('Ctrl Pts',(-1.63258678848454,1.82925038206401,95.7006479567));
#12333=CARTESIAN_POINT('Ctrl Pts',(-1.57115433470712,1.8822898302454,95.6964176307023));
#12334=CARTESIAN_POINT('Ctrl Pts',(-1.50714141443661,1.93222022732659,95.6921873047047));
#12335=CARTESIAN_POINT('Ctrl Pts',(-1.44322061737361,1.98207876784644,95.6879630667155));
#12336=CARTESIAN_POINT('Ctrl Pts',(-1.37672709290479,2.02883685983672,95.6837388287262));
#12337=CARTESIAN_POINT('Ctrl Pts',(-1.30799515958366,2.07222076828356,95.679514590737));
#12338=CARTESIAN_POINT('Ctrl Pts',(-1.23890985681637,2.11582772512959,95.6752686347986));
#12339=CARTESIAN_POINT('Ctrl Pts',(-1.16756340468079,2.1560253719669,95.6710226788601));
#12340=CARTESIAN_POINT('Ctrl Pts',(-1.0943281665114,2.19257750466883,95.6667767229217));
#12341=CARTESIAN_POINT('Ctrl Pts',(-1.0215993904063,2.22887685921308,95.6625601301103));
#12342=CARTESIAN_POINT('Ctrl Pts',(-0.947008291469063,2.26158075152008,
95.658343537299));
#12343=CARTESIAN_POINT('Ctrl Pts',(-0.870946059288238,2.29050282947005,
95.6541269444877));
#12344=CARTESIAN_POINT('Ctrl Pts',(-0.79490913810909,2.31941528310657,95.6499117548194));
#12345=CARTESIAN_POINT('Ctrl Pts',(-0.717402490271032,2.34454825625696,
95.6456965651511));
#12346=CARTESIAN_POINT('Ctrl Pts',(-0.638837114124415,2.36576359588552,
95.6414813754828));
#12347=CARTESIAN_POINT('Ctrl Pts',(-0.560273783565406,2.38697838313544,
95.6372662955643));
#12348=CARTESIAN_POINT('Ctrl Pts',(-0.480652228859809,2.40427561942907,
95.6330512156458));
#12349=CARTESIAN_POINT('Ctrl Pts',(-0.400397035619176,2.41756746831756,
95.6288361357274));
#12350=CARTESIAN_POINT('Ctrl Pts',(-0.31912077626077,2.43102842597016,95.6245674284346));
#12351=CARTESIAN_POINT('Ctrl Pts',(-0.237195120187803,2.44038125826275,
95.6202987211419));
#12352=CARTESIAN_POINT('Ctrl Pts',(-0.155068125884885,2.44558870751698,
95.6160300138491));
#12353=CARTESIAN_POINT('Ctrl Pts',(-0.0738546428888111,2.45073823350476,
95.6118087880502));
#12354=CARTESIAN_POINT('Ctrl Pts',(0.00755524985231285,2.45183419442238,
95.6075875622513));
#12355=CARTESIAN_POINT('Ctrl Pts',(0.0887285139580289,2.44889311747385,
95.6033663364524));
#12356=CARTESIAN_POINT('Ctrl Pts',(0.171271366434522,2.44590241747725,95.5990738884127));
#12357=CARTESIAN_POINT('Ctrl Pts',(0.253569030853064,2.43873723534178,95.594781440373));
#12358=CARTESIAN_POINT('Ctrl Pts',(0.335173854290735,2.4274696161641,95.5904889923333));
#12359=CARTESIAN_POINT('Ctrl Pts',(0.4167786777284,2.41620199698643,95.5861965442936));
#12360=CARTESIAN_POINT('Ctrl Pts',(0.497690182935501,2.40083209919264,95.5819040962539));
#12361=CARTESIAN_POINT('Ctrl Pts',(0.577475747145409,2.38148525325244,95.5776116482142));
#12362=CARTESIAN_POINT('Ctrl Pts',(0.65610621664613,2.36241850108116,95.5733813440481));
#12363=CARTESIAN_POINT('Ctrl Pts',(0.733939585817066,2.3394173604224,95.569151039882));
#12364=CARTESIAN_POINT('Ctrl Pts',(0.810552738024953,2.31256448750738,95.5649207357159));
#12365=CARTESIAN_POINT('Ctrl Pts',(0.887055655155746,2.28575025193373,95.5606965183364));
#12366=CARTESIAN_POINT('Ctrl Pts',(0.962341406996425,2.25509544343965,95.5564723009569));
#12367=CARTESIAN_POINT('Ctrl Pts',(1.03599896479609,2.22073330117361,95.5522480835774));
#12368=CARTESIAN_POINT('Ctrl Pts',(1.11003566973322,2.18619428217874,95.5480021223338));
#12369=CARTESIAN_POINT('Ctrl Pts',(1.18242690642223,2.14790976166453,95.5437561610902));
#12370=CARTESIAN_POINT('Ctrl Pts',(1.25277264201465,2.10606527852762,95.5395101998465));
#12371=CARTESIAN_POINT('Ctrl Pts',(1.32263152168892,2.06451039694347,95.5352936244831));
#12372=CARTESIAN_POINT('Ctrl Pts',(1.39047271925249,2.01944491435982,95.5310770491197));
#12373=CARTESIAN_POINT('Ctrl Pts',(1.45592796740956,1.97109715735036,95.5268604737563));
#12374=CARTESIAN_POINT('Ctrl Pts',(1.52136145328513,1.92276547479677,95.5226453003019));
#12375=CARTESIAN_POINT('Ctrl Pts',(1.58441019116937,1.87115396103302,95.5184301268474));
#12376=CARTESIAN_POINT('Ctrl Pts',(1.64473575083004,1.81653366606335,95.514214953393));
#12377=CARTESIAN_POINT('Ctrl Pts',(1.7050597578607,1.76191477688434,95.5099998884267));
#12378=CARTESIAN_POINT('Ctrl Pts',(1.76266038190972,1.7042875734684,95.5057848234603));
#12379=CARTESIAN_POINT('Ctrl Pts',(1.8172341749178,1.64396174028194,95.501569758494));
#12380=CARTESIAN_POINT('Ctrl Pts',(1.87250276982559,1.5828678735543,95.4973010297637));
#12381=CARTESIAN_POINT('Ctrl Pts',(1.92466657495848,1.51900652598195,95.4930323010334));
#12382=CARTESIAN_POINT('Ctrl Pts',(1.97345199368759,1.45273448317663,95.4887635723031));
#12383=CARTESIAN_POINT('Ctrl Pts',(2.02169438905759,1.38720010478492,95.4845423581678));
#12384=CARTESIAN_POINT('Ctrl Pts',(2.06663302539075,1.31930885799789,95.4803211440326));
#12385=CARTESIAN_POINT('Ctrl Pts',(2.10804767972721,1.24943396383991,95.4760999298973));
#12386=CARTESIAN_POINT('Ctrl Pts',(2.15016158804585,1.17837928685443,95.4718074438695));
#12387=CARTESIAN_POINT('Ctrl Pts',(2.18863118070265,1.10527380325279,95.4675149578417));
#12388=CARTESIAN_POINT('Ctrl Pts',(2.2232750313747,1.0305330585992,95.4632224718139));
#12389=CARTESIAN_POINT('Ctrl Pts',(2.25791888204675,0.955792313945615,95.4589299857861));
#12390=CARTESIAN_POINT('Ctrl Pts',(2.28873686598192,0.879416795412588,95.4546374997582));
#12391=CARTESIAN_POINT('Ctrl Pts',(2.31560051147203,0.80183821390008,95.4503450137304));
#12392=CARTESIAN_POINT('Ctrl Pts',(2.34207419472043,0.725385790695685,95.446114838958));
#12393=CARTESIAN_POINT('Ctrl Pts',(2.3648074862182,0.647476656161797,95.4418846641855));
#12394=CARTESIAN_POINT('Ctrl Pts',(2.38364112932792,0.568511404086408,95.4376544894131));
#12395=CARTESIAN_POINT('Ctrl Pts',(2.402447661774,0.489659820958448,95.4334304038951));
#12396=CARTESIAN_POINT('Ctrl Pts',(2.4173655873715,0.409755588227427,95.4292063183771));
#12397=CARTESIAN_POINT('Ctrl Pts',(2.42828473548847,0.329216484085645,95.4249822328591));
#12398=CARTESIAN_POINT('Ctrl Pts',(2.43926051618846,0.248259660772587,95.4207362389586));
#12399=CARTESIAN_POINT('Ctrl Pts',(2.4461957597747,0.16666181039205,95.4164902450581));
#12400=CARTESIAN_POINT('Ctrl Pts',(2.44903022958949,0.0848597935236164,
95.4122442511576));
#12401=CARTESIAN_POINT('Ctrl Pts',(2.45184496926564,0.00362718301291821,
95.4080278127132));
#12402=CARTESIAN_POINT('Ctrl Pts',(2.45061582686108,-0.0778062896216502,
95.4038113742689));
#12403=CARTESIAN_POINT('Ctrl Pts',(2.44533574317124,-0.159007399730754,
95.3995949358245));
#12404=CARTESIAN_POINT('Ctrl Pts',(2.44005741704231,-0.240181480742424,
95.3953799008896));
#12405=CARTESIAN_POINT('Ctrl Pts',(2.43073085748668,-0.32112288897255,95.3911648659547));
#12406=CARTESIAN_POINT('Ctrl Pts',(2.41740107782973,-0.401400397244051,
95.3869498310197));
#12407=CARTESIAN_POINT('Ctrl Pts',(2.40407164574144,-0.481675812311703,
95.3827349059902));
#12408=CARTESIAN_POINT('Ctrl Pts',(2.38673927833838,-0.561286903095675,
95.3785199809606));
#12409=CARTESIAN_POINT('Ctrl Pts',(2.36550040385334,-0.639810979406937,
95.374305055931));
#12410=CARTESIAN_POINT('Ctrl Pts',(2.34398960297419,-0.719340418264053,
95.3700361662074));
#12411=CARTESIAN_POINT('Ctrl Pts',(2.31847166113447,-0.797754333226607,
95.3657672764837));
#12412=CARTESIAN_POINT('Ctrl Pts',(2.28909880358271,-0.874629588703803,
95.36149838676));
#12413=CARTESIAN_POINT('Ctrl Pts',(2.26005496356092,-0.950643732638566,
95.3572773146363));
#12414=CARTESIAN_POINT('Ctrl Pts',(2.22724238417466,-1.02515310930849,95.3530562425126));
#12415=CARTESIAN_POINT('Ctrl Pts',(2.19085594488886,-1.09777068586528,95.3488351703889));
#12416=CARTESIAN_POINT('Ctrl Pts',(2.15385121048255,-1.17162221369981,95.3445423718652));
#12417=CARTESIAN_POINT('Ctrl Pts',(2.11315027673689,-1.24351661304794,95.3402495733416));
#12418=CARTESIAN_POINT('Ctrl Pts',(2.06900468655941,-1.3130764855846,95.3359567748179));
#12419=CARTESIAN_POINT('Ctrl Pts',(2.02485909638192,-1.38263635812126,95.3316639762942));
#12420=CARTESIAN_POINT('Ctrl Pts',(1.97726919235437,-1.44986133527768,95.3273711777705));
#12421=CARTESIAN_POINT('Ctrl Pts',(1.92652876514865,-1.51440984117735,95.3230783792469));
#12422=CARTESIAN_POINT('Ctrl Pts',(1.87652766876007,-1.57801782090804,95.3188481304181));
#12423=CARTESIAN_POINT('Ctrl Pts',(1.82327869572507,-1.63926675901647,95.3146178815893));
#12424=CARTESIAN_POINT('Ctrl Pts',(1.7670327494766,-1.69780608794914,95.3103876327606));
#12425=CARTESIAN_POINT('Ctrl Pts',(1.71086775324413,-1.75626116619479,95.3061634721698));
#12426=CARTESIAN_POINT('Ctrl Pts',(1.65171466970017,-1.81201404765782,95.3019393115791));
#12427=CARTESIAN_POINT('Ctrl Pts',(1.58986539695636,-1.86474616759515,95.2977151509884));
#12428=CARTESIAN_POINT('Ctrl Pts',(1.52769671841289,-1.91775060997361,95.293469175729));
#12429=CARTESIAN_POINT('Ctrl Pts',(1.46280421402332,-1.96770262371319,95.2892232004696));
#12430=CARTESIAN_POINT('Ctrl Pts',(1.3955228091021,-2.01431535248972,95.2849772252102));
#12431=CARTESIAN_POINT('Ctrl Pts',(1.32870822224629,-2.06060466852098,95.2807607097691));
#12432=CARTESIAN_POINT('Ctrl Pts',(1.25953816713321,-2.10360062240015,95.2765441943279));
#12433=CARTESIAN_POINT('Ctrl Pts',(1.18837328327255,-2.14306303911108,95.2723276788867));
#12434=CARTESIAN_POINT('Ctrl Pts',(1.11723207803241,-2.18251232553163,95.2681125664024));
#12435=CARTESIAN_POINT('Ctrl Pts',(1.04409776859277,-2.21843018410425,95.2638974539182));
#12436=CARTESIAN_POINT('Ctrl Pts',(0.96935746782782,-2.25062132522698,95.259682341434));
#12437=CARTESIAN_POINT('Ctrl Pts',(0.894619107899231,-2.28281163041867,
95.2554673384067));
#12438=CARTESIAN_POINT('Ctrl Pts',(0.818275267222027,-2.31127522753333,
95.2512523353794));
#12439=CARTESIAN_POINT('Ctrl Pts',(0.740733675418833,-2.33586469473309,
95.2470373323521));
#12440=CARTESIAN_POINT('Ctrl Pts',(0.662202422950886,-2.36076799645557,
95.2427685333863));
#12441=CARTESIAN_POINT('Ctrl Pts',(0.582443089080039,-2.38169741057815,
95.2384997344206));
#12442=CARTESIAN_POINT('Ctrl Pts',(0.501893893863773,-2.39855222359286,
95.2342309354548));
#12443=CARTESIAN_POINT('Ctrl Pts',(0.422243792575454,-2.41521890238727,
95.2300097850251));
#12444=CARTESIAN_POINT('Ctrl Pts',(0.341821849958334,-2.42790147720855,
95.2257886345954));
#12445=CARTESIAN_POINT('Ctrl Pts',(0.261059029304541,-2.43655462348345,
95.2215674841657));
#12446=CARTESIAN_POINT('Ctrl Pts',(0.178928727119419,-2.44535428541522,
95.217274860932));
#12447=CARTESIAN_POINT('Ctrl Pts',(0.0964463982607014,-2.44998677244189,
95.2129822376982));
#12448=CARTESIAN_POINT('Ctrl Pts',(0.0140654582285057,-2.45045963298415,
95.2086896144645));
#12449=CARTESIAN_POINT('Ctrl Pts',(-0.0683154818036959,-2.45093249352641,
95.2043969912308));
#12450=CARTESIAN_POINT('Ctrl Pts',(-0.15059453789688,-2.44724581645714,
95.200104367997));
#12451=CARTESIAN_POINT('Ctrl Pts',(-0.232325584175832,-2.43946204580792,
95.1958117447633));
#12452=CARTESIAN_POINT('Ctrl Pts',(-0.312868874840373,-2.43179139272798,
95.1915815040338));
#12453=CARTESIAN_POINT('Ctrl Pts',(-0.393183743365405,-2.42011306134111,
95.1873512633044));
#12454=CARTESIAN_POINT('Ctrl Pts',(-0.472839625236135,-2.40444857270987,
95.183121022575));
#12455=CARTESIAN_POINT('Ctrl Pts',(-0.55238086599157,-2.38880662848346,
95.1788968700276));
#12456=CARTESIAN_POINT('Ctrl Pts',(-0.631264551134139,-2.36919000969627,
95.1746727174803));
#12457=CARTESIAN_POINT('Ctrl Pts',(-0.709064872687081,-2.34567202658881,
95.170448564933));
#12458=CARTESIAN_POINT('Ctrl Pts',(-0.787267161494991,-2.32203253422633,
95.1662025876558));
#12459=CARTESIAN_POINT('Ctrl Pts',(-0.86437438491763,-2.29445128838241,
95.1619566103786));
#12460=CARTESIAN_POINT('Ctrl Pts',(-0.939964141988851,-2.26305494006998,
95.1577106331013));
#12461=CARTESIAN_POINT('Ctrl Pts',(-1.01502925989475,-2.23187650162539,
95.1534941255044));
#12462=CARTESIAN_POINT('Ctrl Pts',(-1.08859747379438,-2.19693593212704,
95.1492776179075));
#12463=CARTESIAN_POINT('Ctrl Pts',(-1.16027175212964,-2.15840675295691,
95.1450611103106));
#12464=CARTESIAN_POINT('Ctrl Pts',(-1.23192218389073,-2.11989039273593,
95.1408460055776));
#12465=CARTESIAN_POINT('Ctrl Pts',(-1.30167952198786,-2.07778801388991,
95.1366309008446));
#12466=CARTESIAN_POINT('Ctrl Pts',(-1.36917018009721,-2.03231967660911,
95.1324157961116));
#12467=CARTESIAN_POINT('Ctrl Pts',(-1.43665908729011,-1.98685251891764,
95.1282008007315));
#12468=CARTESIAN_POINT('Ctrl Pts',(-1.50188104620748,-1.93801983720586,
95.1239858053514));
#12469=CARTESIAN_POINT('Ctrl Pts',(-1.5644915911768,-1.88608491620529,95.1197708099713));
#12470=CARTESIAN_POINT('Ctrl Pts',(-1.62790148618433,-1.83348694106412,
95.1155020016636));
#12471=CARTESIAN_POINT('Ctrl Pts',(-1.68863242610859,-1.7777072496585,95.111233193356));
#12472=CARTESIAN_POINT('Ctrl Pts',(-1.74636274837719,-1.71906003416997,
95.1069643850484));
#12473=CARTESIAN_POINT('Ctrl Pts',(-1.80344845827463,-1.66106766901229,
95.1027432419284));
#12474=CARTESIAN_POINT('Ctrl Pts',(-1.85759995945713,-1.60027189105454,
95.0985220988084));
#12475=CARTESIAN_POINT('Ctrl Pts',(-1.90854611158219,-1.53701073189633,
95.0943009556885));
#12476=CARTESIAN_POINT('Ctrl Pts',(-1.96035519034814,-1.47267805433499,
95.090008314787));
#12477=CARTESIAN_POINT('Ctrl Pts',(-2.00884903343694,-1.40579611070822,
95.0857156738855));
#12478=CARTESIAN_POINT('Ctrl Pts',(-2.05378883540593,-1.33675041408707,
95.081423032984));
#12479=CARTESIAN_POINT('Ctrl Pts',(-2.09872863737492,-1.26770471746592,
95.0771303920826));
#12480=CARTESIAN_POINT('Ctrl Pts',(-2.14011420528511,-1.19649573242134,
95.0728377511811));
#12481=CARTESIAN_POINT('Ctrl Pts',(-2.17775685604983,-1.12353252108159,
95.0685451102796));
#12482=CARTESIAN_POINT('Ctrl Pts',(-2.21719928527825,-1.0470807770869,95.0640472287139));
#12483=CARTESIAN_POINT('Ctrl Pts',(-2.25266677780864,-0.96844397721106,
95.0595493471482));
#12484=CARTESIAN_POINT('Ctrl Pts',(-2.28392751385978,-0.888045810436754,
95.0550514655825));
#12485=CARTESIAN_POINT('Ctrl Pts',(-2.31508961490446,-0.807901318869803,
95.0505677758956));
#12486=CARTESIAN_POINT('Ctrl Pts',(-2.34207126954516,-0.726006882702449,
95.0460840862087));
#12487=CARTESIAN_POINT('Ctrl Pts',(-2.36468776859533,-0.642807908364263,
95.0416003965217));
#12488=CARTESIAN_POINT('Ctrl Pts',(-2.38726029594484,-0.559770692058838,
95.0371254241637));
#12489=CARTESIAN_POINT('Ctrl Pts',(-2.40548445807782,-0.475434345746077,
95.0326504518057));
#12490=CARTESIAN_POINT('Ctrl Pts',(-2.41922415952532,-0.390262368117945,
95.0281754794477));
#12491=CARTESIAN_POINT('Ctrl Pts',(-2.43292775069282,-0.305314236981045,
95.0237122680807));
#12492=CARTESIAN_POINT('Ctrl Pts',(-2.44217029994478,-0.219535219633665,
95.0192490567136));
#12493=CARTESIAN_POINT('Ctrl Pts',(-2.44686627099133,-0.133400531801645,
95.0147858453466));
#12494=CARTESIAN_POINT('Ctrl Pts',(-2.44928084993937,-0.0891117144574003,
95.0124909469964));
#12495=CARTESIAN_POINT('Ctrl Pts',(-2.45049421005239,-0.0447290804429846,
95.0101960486462));
#12496=CARTESIAN_POINT('Ctrl Pts',(-2.45049997932286,-0.00031833732531135,
95.007901150296));
#12497=CARTESIAN_POINT('',(-2.45049895420016,0.00226394874618012,94.2079011502221));
#12498=CARTESIAN_POINT('Ctrl Pts',(-2.45049997932294,-0.000318336712990411,
95.0079011502643));
#12499=CARTESIAN_POINT('Ctrl Pts',(-2.45051097724511,0.0843417321286243,
95.0035263922964));
#12500=CARTESIAN_POINT('Ctrl Pts',(-2.44613038789473,0.168935422682587,
94.9991516343285));
#12501=CARTESIAN_POINT('Ctrl Pts',(-2.43740472998465,0.252998877958903,
94.9947768763606));
#12502=CARTESIAN_POINT('Ctrl Pts',(-2.42851264297302,0.338665720106336,
94.9903186763136));
#12503=CARTESIAN_POINT('Ctrl Pts',(-2.41510809386072,0.423781445560833,
94.9858604762665));
#12504=CARTESIAN_POINT('Ctrl Pts',(-2.39729475185905,0.507866244900213,
94.9814022762195));
#12505=CARTESIAN_POINT('Ctrl Pts',(-2.37975433706502,0.590662738570381,
94.9770123825065));
#12506=CARTESIAN_POINT('Ctrl Pts',(-2.35793947976719,0.67245930123738,94.9726224887935));
#12507=CARTESIAN_POINT('Ctrl Pts',(-2.33199926746043,0.752814496781243,
94.9682325950806));
#12508=CARTESIAN_POINT('Ctrl Pts',(-2.30545361425104,0.835045171274418,
94.9637402418665));
#12509=CARTESIAN_POINT('Ctrl Pts',(-2.27458781118937,0.915765926586604,
94.9592478886524));
#12510=CARTESIAN_POINT('Ctrl Pts',(-2.23961263170089,0.994527782380069,
94.9547555354383));
#12511=CARTESIAN_POINT('Ctrl Pts',(-2.20463745221241,1.07328963817353,94.9502631822242));
#12512=CARTESIAN_POINT('Ctrl Pts',(-2.16555316844435,1.15009222325543,94.9457708290101));
#12513=CARTESIAN_POINT('Ctrl Pts',(-2.12261843975362,1.22451672476038,94.941278475796));
#12514=CARTESIAN_POINT('Ctrl Pts',(-2.08218883859461,1.29459875401873,94.9370482394757));
#12515=CARTESIAN_POINT('Ctrl Pts',(-2.03820844252071,1.36280850261209,94.9328180031553));
#12516=CARTESIAN_POINT('Ctrl Pts',(-1.9908756524753,1.42876323664247,94.928587766835));
#12517=CARTESIAN_POINT('Ctrl Pts',(-1.94361098566699,1.49462304599208,94.9243636188393));
#12518=CARTESIAN_POINT('Ctrl Pts',(-1.89300377622801,1.55823391176525,94.9201394708436));
#12519=CARTESIAN_POINT('Ctrl Pts',(-1.83929756082253,1.61923893627601,94.9159153228479));
#12520=CARTESIAN_POINT('Ctrl Pts',(-1.78531379163511,1.68055923482244,94.9116693444506));
#12521=CARTESIAN_POINT('Ctrl Pts',(-1.72819912731434,1.73924626559179,94.9074233660533));
#12522=CARTESIAN_POINT('Ctrl Pts',(-1.66824421339529,1.79496838258314,94.903177387656));
#12523=CARTESIAN_POINT('Ctrl Pts',(-1.60870550769628,1.85030367551598,94.8989608849262));
#12524=CARTESIAN_POINT('Ctrl Pts',(-1.54636620690215,1.90271476844622,94.8947443821964));
#12525=CARTESIAN_POINT('Ctrl Pts',(-1.48154905552329,1.95191256107389,94.8905278794667));
#12526=CARTESIAN_POINT('Ctrl Pts',(-1.41675347098861,2.00109398394286,94.8863127797091));
#12527=CARTESIAN_POINT('Ctrl Pts',(-1.349482043334,2.04706394865548,94.8820976799514));
#12528=CARTESIAN_POINT('Ctrl Pts',(-1.28009011475513,2.08957401115783,94.8778825801938));
#12529=CARTESIAN_POINT('Ctrl Pts',(-1.21069998809592,2.13208296978946,94.8736675898909));
#12530=CARTESIAN_POINT('Ctrl Pts',(-1.1391898672171,2.17113196274648,94.8694525995879));
#12531=CARTESIAN_POINT('Ctrl Pts',(-1.06594231994289,2.20651698850355,94.865237609285));
#12532=CARTESIAN_POINT('Ctrl Pts',(-0.991759431577881,2.24235386650442,
94.8609687952873));
#12533=CARTESIAN_POINT('Ctrl Pts',(-0.915794861525792,2.27443230916632,
94.8566999812896));
#12534=CARTESIAN_POINT('Ctrl Pts',(-0.838468019221021,2.30259020034907,
94.8524311672918));
#12535=CARTESIAN_POINT('Ctrl Pts',(-0.762004800056656,2.33043361074241,
94.8482100294495));
#12536=CARTESIAN_POINT('Ctrl Pts',(-0.684210054419245,2.35444352728177,
94.8439888916072));
#12537=CARTESIAN_POINT('Ctrl Pts',(-0.605503891400048,2.3745136949488,94.8397677537649));
#12538=CARTESIAN_POINT('Ctrl Pts',(-0.525464293866478,2.39492389004507,
94.8354751016895));
#12539=CARTESIAN_POINT('Ctrl Pts',(-0.444482602954371,2.41125950463292,
94.831182449614));
#12540=CARTESIAN_POINT('Ctrl Pts',(-0.363008695972171,2.4234634176419,94.8268897975386));
#12541=CARTESIAN_POINT('Ctrl Pts',(-0.281534788989966,2.43566733065089,
94.8225971454632));
#12542=CARTESIAN_POINT('Ctrl Pts',(-0.199569168688666,2.44373955951889,
94.8183044933878));
#12543=CARTESIAN_POINT('Ctrl Pts',(-0.117562317125274,2.44767835950562,
94.8140118413124));
#12544=CARTESIAN_POINT('Ctrl Pts',(-0.0367478870311017,2.45155988733061,
94.8097816065886));
#12545=CARTESIAN_POINT('Ctrl Pts',(0.044411376960547,2.45144208469561,94.8055513718649));
#12546=CARTESIAN_POINT('Ctrl Pts',(0.125486237175565,2.44728491481468,94.8013211371412));
#12547=CARTESIAN_POINT('Ctrl Pts',(0.206444411099471,2.44313372810454,94.7970969907462));
#12548=CARTESIAN_POINT('Ctrl Pts',(0.287317961892368,2.43495474383967,94.7928728443511));
#12549=CARTESIAN_POINT('Ctrl Pts',(0.367674981959944,2.42275986380012,94.7886486979561));
#12550=CARTESIAN_POINT('Ctrl Pts',(0.448447325408579,2.41050195480795,94.7844027191592));
#12551=CARTESIAN_POINT('Ctrl Pts',(0.528697307574851,2.39418649118031,94.7801567403622));
#12552=CARTESIAN_POINT('Ctrl Pts',(0.607988791770718,2.373878657194,94.7759107615652));
#12553=CARTESIAN_POINT('Ctrl Pts',(0.686729795624061,2.3537118101437,94.7716942604339));
#12554=CARTESIAN_POINT('Ctrl Pts',(0.764525111512021,2.32960796811263,94.7674777593026));
#12555=CARTESIAN_POINT('Ctrl Pts',(0.840957038661839,2.30168232150423,94.7632612581713));
#12556=CARTESIAN_POINT('Ctrl Pts',(0.917363534412393,2.27376596667081,94.7590461600077));
#12557=CARTESIAN_POINT('Ctrl Pts',(0.992407105687038,2.24203049199986,94.7548310618441));
#12558=CARTESIAN_POINT('Ctrl Pts',(1.06568662791332,2.20664049203461,94.7506159636805));
#12559=CARTESIAN_POINT('Ctrl Pts',(1.13896424738483,2.17125141099581,94.7464009749649));
#12560=CARTESIAN_POINT('Ctrl Pts',(1.21047749044841,2.13220819659127,94.7421859862493));
#12561=CARTESIAN_POINT('Ctrl Pts',(1.27984789843215,2.08972237555107,94.7379709975337));
#12562=CARTESIAN_POINT('Ctrl Pts',(1.3501041956662,2.04669399272921,94.7337021816416));
#12563=CARTESIAN_POINT('Ctrl Pts',(1.41816211304461,2.00013469161971,94.7294333657496));
#12564=CARTESIAN_POINT('Ctrl Pts',(1.48365850661328,1.95030963843028,94.7251645498575));
#12565=CARTESIAN_POINT('Ctrl Pts',(1.54842335255914,1.90104109525967,94.7209434135695));
#12566=CARTESIAN_POINT('Ctrl Pts',(1.61068329043891,1.84857973987824,94.7167222772816));
#12567=CARTESIAN_POINT('Ctrl Pts',(1.6701217908313,1.79322152947996,94.7125011409937));
#12568=CARTESIAN_POINT('Ctrl Pts',(1.73056736750939,1.73692537582029,94.7082084852995));
#12569=CARTESIAN_POINT('Ctrl Pts',(1.78809466152267,1.67763365354351,94.7039158296054));
#12570=CARTESIAN_POINT('Ctrl Pts',(1.84241238017381,1.61569392874463,94.6996231739112));
#12571=CARTESIAN_POINT('Ctrl Pts',(1.89673009882495,1.55375420394576,94.6953305182171));
#12572=CARTESIAN_POINT('Ctrl Pts',(1.94783798495381,1.48916690898437,94.6910378625229));
#12573=CARTESIAN_POINT('Ctrl Pts',(1.99549100323293,1.42231005973256,94.6867452068288));
#12574=CARTESIAN_POINT('Ctrl Pts',(2.04245106751192,1.35642542006574,94.6825149734751));
#12575=CARTESIAN_POINT('Ctrl Pts',(2.0862332327142,1.28808833512064,94.6782847401215));
#12576=CARTESIAN_POINT('Ctrl Pts',(2.12657173800282,1.2176382439492,94.6740545067679));
#12577=CARTESIAN_POINT('Ctrl Pts',(2.16685218614249,1.14728954799325,94.669830361773));
#12578=CARTESIAN_POINT('Ctrl Pts',(2.20369858855441,1.07483428588162,94.665606216778));
#12579=CARTESIAN_POINT('Ctrl Pts',(2.23688743295657,1.00064222491406,94.661382071783));
#12580=CARTESIAN_POINT('Ctrl Pts',(2.27024782690328,0.926066673213479,94.6571360926398));
#12581=CARTESIAN_POINT('Ctrl Pts',(2.29991246275672,0.849736701875051,94.6528901134965));
#12582=CARTESIAN_POINT('Ctrl Pts',(2.32570036411272,0.772054445208349,94.6486441343533));
#12583=CARTESIAN_POINT('Ctrl Pts',(2.35130922224575,0.694911529894342,94.6444276346849));
#12584=CARTESIAN_POINT('Ctrl Pts',(2.3730948585931,0.616435494702253,94.6402111350166));
#12585=CARTESIAN_POINT('Ctrl Pts',(2.39092833146646,0.537040002039902,94.6359946353482));
#12586=CARTESIAN_POINT('Ctrl Pts',(2.40875587047224,0.457670927245963,94.631779538668));
#12587=CARTESIAN_POINT('Ctrl Pts',(2.42263375553616,0.377383456029156,94.6275644419878));
#12588=CARTESIAN_POINT('Ctrl Pts',(2.43248356752879,0.296604018351767,94.6233493453075));
#12589=CARTESIAN_POINT('Ctrl Pts',(2.44233312372074,0.215826678525057,94.6191343580938));
#12590=CARTESIAN_POINT('Ctrl Pts',(2.44815475958035,0.134557859534711,94.6149193708801));
#12591=CARTESIAN_POINT('Ctrl Pts',(2.4499217916521,0.0532302995309846,94.6107043836664));
#12592=CARTESIAN_POINT('Ctrl Pts',(2.45171139082359,-0.0291359100747253,
94.6064355660563));
#12593=CARTESIAN_POINT('Ctrl Pts',(2.44934205773973,-0.11156188344375,94.6021667484462));
#12594=CARTESIAN_POINT('Ctrl Pts',(2.44284051241173,-0.193598762702708,
94.5978979308361));
#12595=CARTESIAN_POINT('Ctrl Pts',(2.4364115895914,-0.274719286911727,94.5936767960804));
#12596=CARTESIAN_POINT('Ctrl Pts',(2.42594243090056,-0.355458907110871,
94.5894556613248));
#12597=CARTESIAN_POINT('Ctrl Pts',(2.41151086214071,-0.435391331766468,
94.5852345265692));
#12598=CARTESIAN_POINT('Ctrl Pts',(2.39683476018089,-0.516678157451295,
94.5809418675318));
#12599=CARTESIAN_POINT('Ctrl Pts',(2.37806083589897,-0.597129689449561,
94.5766492084945));
#12600=CARTESIAN_POINT('Ctrl Pts',(2.35532397543982,-0.676312960631674,
94.5723565494571));
#12601=CARTESIAN_POINT('Ctrl Pts',(2.33258711498066,-0.755496231813789,
94.5680638904198));
#12602=CARTESIAN_POINT('Ctrl Pts',(2.30588754301694,-0.833410792077988,
94.5637712313825));
#12603=CARTESIAN_POINT('Ctrl Pts',(2.27541077160263,-0.909646123761728,
94.5594785723451));
#12604=CARTESIAN_POINT('Ctrl Pts',(2.24537719852325,-0.984772828432255,
94.5552483378774));
#12605=CARTESIAN_POINT('Ctrl Pts',(2.21156232884268,-1.05855218561544,94.5510181034096));
#12606=CARTESIAN_POINT('Ctrl Pts',(2.17410801651075,-1.13057710154755,94.5467878689419));
#12607=CARTESIAN_POINT('Ctrl Pts',(2.13670761009236,-1.20249835601457,94.5425637228159));
#12608=CARTESIAN_POINT('Ctrl Pts',(2.09567837676965,-1.27266977491542,94.5383395766899));
#12609=CARTESIAN_POINT('Ctrl Pts',(2.05121052643643,-1.34070340725918,94.5341154305639));
#12610=CARTESIAN_POINT('Ctrl Pts',(2.00651284152022,-1.40908867525436,94.5298694517013));
#12611=CARTESIAN_POINT('Ctrl Pts',(1.95834106475029,-1.47531355037406,94.5256234728387));
#12612=CARTESIAN_POINT('Ctrl Pts',(1.90693563212919,-1.53900836414753,94.5213774939761));
#12613=CARTESIAN_POINT('Ctrl Pts',(1.85588708562321,-1.60226097184507,94.5171609931438));
#12614=CARTESIAN_POINT('Ctrl Pts',(1.80164993688566,-1.66301817046702,94.5129444923115));
#12615=CARTESIAN_POINT('Ctrl Pts',(1.74450245407991,-1.72094783119918,94.5087279914792));
#12616=CARTESIAN_POINT('Ctrl Pts',(1.68737398625447,-1.77885821669289,94.5045128936253));
#12617=CARTESIAN_POINT('Ctrl Pts',(1.62733743378636,-1.8339426016844,94.5002977957713));
#12618=CARTESIAN_POINT('Ctrl Pts',(1.56470912183818,-1.88590445517168,94.4960826979174));
#12619=CARTESIAN_POINT('Ctrl Pts',(1.50208243623128,-1.93786495930586,94.4918677095217));
#12620=CARTESIAN_POINT('Ctrl Pts',(1.4368644836448,-1.98670279694,94.487652721126));
#12621=CARTESIAN_POINT('Ctrl Pts',(1.36940486835244,-2.03216154784324,94.4834377327304));
#12622=CARTESIAN_POINT('Ctrl Pts',(1.30108375469578,-2.07820083332819,94.4791689164913));
#12623=CARTESIAN_POINT('Ctrl Pts',(1.23046371229256,-2.12077382519476,94.4749001002522));
#12624=CARTESIAN_POINT('Ctrl Pts',(1.15793677929927,-2.15966031244407,94.4706312840131));
#12625=CARTESIAN_POINT('Ctrl Pts',(1.08621993164186,-2.19811245934857,94.4664101480674));
#12626=CARTESIAN_POINT('Ctrl Pts',(1.01263903125177,-2.23295989853074,94.4621890121216));
#12627=CARTESIAN_POINT('Ctrl Pts',(0.937594765481311,-2.26403761137973,
94.4579678761758));
#12628=CARTESIAN_POINT('Ctrl Pts',(0.861278993895383,-2.29564188668107,
94.4536752197901));
#12629=CARTESIAN_POINT('Ctrl Pts',(0.78345028172949,-2.32334733793639,94.4493825634043));
#12630=CARTESIAN_POINT('Ctrl Pts',(0.704545782304668,-2.34703333820308,
94.4450899070186));
#12631=CARTESIAN_POINT('Ctrl Pts',(0.625641282879849,-2.37071933846978,
94.4407972506329));
#12632=CARTESIAN_POINT('Ctrl Pts',(0.545661496307845,-2.39038583338739,
94.4365045942472));
#12633=CARTESIAN_POINT('Ctrl Pts',(0.465052063249206,-2.40596692173181,
94.4322119378615));
#12634=CARTESIAN_POINT('Ctrl Pts',(0.385614821956653,-2.42132143580607,
94.4279817036549));
#12635=CARTESIAN_POINT('Ctrl Pts',(0.305266531096374,-2.43276653384473,
94.4237514694483));
#12636=CARTESIAN_POINT('Ctrl Pts',(0.224426346893148,-2.44020143939393,
94.4195212352417));
#12637=CARTESIAN_POINT('Ctrl Pts',(0.143702511522455,-2.44762564429233,
94.4152970893786));
#12638=CARTESIAN_POINT('Ctrl Pts',(0.0624886481135967,-2.45105107717047,
94.4110729435155));
#12639=CARTESIAN_POINT('Ctrl Pts',(-0.0187860453897214,-2.45042799006594,
94.4068487976525));
#12640=CARTESIAN_POINT('Ctrl Pts',(-0.100480818058492,-2.44980168245206,
94.4026028187244));
#12641=CARTESIAN_POINT('Ctrl Pts',(-0.182236584348602,-2.44508478899653,
94.3983568397963));
#12642=CARTESIAN_POINT('Ctrl Pts',(-0.263612369664805,-2.4362796983433,
94.3941108608681));
#12643=CARTESIAN_POINT('Ctrl Pts',(-0.344423191089381,-2.42753573838469,
94.3898943603011));
#12644=CARTESIAN_POINT('Ctrl Pts',(-0.424858822406461,-2.4147602180408,
94.385677859734));
#12645=CARTESIAN_POINT('Ctrl Pts',(-0.504489413384243,-2.39800764839965,
94.3814613591669));
#12646=CARTESIAN_POINT('Ctrl Pts',(-0.584093508453117,-2.38126065292986,
94.3772462615784));
#12647=CARTESIAN_POINT('Ctrl Pts',(-0.662892640253776,-2.36053933167851,
94.37303116399));
#12648=CARTESIAN_POINT('Ctrl Pts',(-0.740466327717361,-2.33594945739773,
94.3688160664015));
#12649=CARTESIAN_POINT('Ctrl Pts',(-0.818038000737844,-2.31136022166985,
94.3646010782712));
#12650=CARTESIAN_POINT('Ctrl Pts',(-0.894383849573194,-2.28290277422771,
94.3603860901409));
#12651=CARTESIAN_POINT('Ctrl Pts',(-0.969099142057992,-2.25073257026739,
94.3561711020106));
#12652=CARTESIAN_POINT('Ctrl Pts',(-1.04476860243158,-2.2181515297223,94.3519022854579));
#12653=CARTESIAN_POINT('Ctrl Pts',(-1.11876510782296,-2.18176240673814,
94.3476334689051));
#12654=CARTESIAN_POINT('Ctrl Pts',(-1.1906914429175,-2.14177593080206,94.3433646523524));
#12655=CARTESIAN_POINT('Ctrl Pts',(-1.26181439137251,-2.10223608683307,
94.339143516669));
#12656=CARTESIAN_POINT('Ctrl Pts',(-1.33091281827869,-2.05917915330359,
94.3349223809856));
#12657=CARTESIAN_POINT('Ctrl Pts',(-1.39763126139181,-2.01285297704038,
94.3307012453022));
#12658=CARTESIAN_POINT('Ctrl Pts',(-1.46548015621508,-1.96574186781505,
94.3264085883148));
#12659=CARTESIAN_POINT('Ctrl Pts',(-1.53086727006343,-1.91525000978067,
94.3221159313274));
#12660=CARTESIAN_POINT('Ctrl Pts',(-1.59345476753618,-1.86167992786521,
94.3178232743401));
#12661=CARTESIAN_POINT('Ctrl Pts',(-1.65604226500892,-1.80810984594975,
94.3135306173527));
#12662=CARTESIAN_POINT('Ctrl Pts',(-1.71582982997526,-1.75146193146986,
94.3092379603653));
#12663=CARTESIAN_POINT('Ctrl Pts',(-1.77252107491581,-1.69207543832399,
94.3049453033779));
#12664=CARTESIAN_POINT('Ctrl Pts',(-1.827670026992,-1.63430456262863,94.3007694286952));
#12665=CARTESIAN_POINT('Ctrl Pts',(-1.88010845724103,-1.57371206786479,
94.2965935540125));
#12666=CARTESIAN_POINT('Ctrl Pts',(-1.92952846367659,-1.51058603126796,
94.2924176793298));
#12667=CARTESIAN_POINT('Ctrl Pts',(-1.97888391947616,-1.44754244763103,
94.2882472590245));
#12668=CARTESIAN_POINT('Ctrl Pts',(-2.02522847865214,-1.38197225707019,
94.2840768387192));
#12669=CARTESIAN_POINT('Ctrl Pts',(-2.06829116509759,-1.31420010134654,
94.2799064184139));
#12670=CARTESIAN_POINT('Ctrl Pts',(-2.11131161439484,-1.24649441854461,
94.2757400885794));
#12671=CARTESIAN_POINT('Ctrl Pts',(-2.15105632215474,-1.17659145616965,
94.2715737587449));
#12672=CARTESIAN_POINT('Ctrl Pts',(-2.18729570921974,-1.10484737879442,
94.2674074289104));
#12673=CARTESIAN_POINT('Ctrl Pts',(-2.2235113347469,-1.03315034276697,94.2632438308662));
#12674=CARTESIAN_POINT('Ctrl Pts',(-2.25622598685222,-0.95961501333814,
94.2590802328219));
#12675=CARTESIAN_POINT('Ctrl Pts',(-2.2852552468919,-0.884623482931036,
94.2549166347776));
#12676=CARTESIAN_POINT('Ctrl Pts',(-2.31428442192048,-0.809632172133815,
94.2507530489263));
#12677=CARTESIAN_POINT('Ctrl Pts',(-2.33962803644342,-0.73318510766179,
94.246589463075));
#12678=CARTESIAN_POINT('Ctrl Pts',(-2.3611496936317,-0.655684660689062,
94.2424258772237));
#12679=CARTESIAN_POINT('Ctrl Pts',(-2.38267036229203,-0.578187773449548,
94.2382624826132));
#12680=CARTESIAN_POINT('Ctrl Pts',(-2.40036930237333,-0.499638062877898,
94.2340990880028));
#12681=CARTESIAN_POINT('Ctrl Pts',(-2.41416049745554,-0.420451355718133,
94.2299356933924));
#12682=CARTESIAN_POINT('Ctrl Pts',(-2.42796383302171,-0.341194939955018,
94.225768633717));
#12683=CARTESIAN_POINT('Ctrl Pts',(-2.43785248025489,-0.261300880884543,
94.2216015740417));
#12684=CARTESIAN_POINT('Ctrl Pts',(-2.44379203160573,-0.181192594386007,
94.2174345143663));
#12685=CARTESIAN_POINT('Ctrl Pts',(-2.44832151682569,-0.120102239532874,
94.2142567263323));
#12686=CARTESIAN_POINT('Ctrl Pts',(-2.45055545031336,-0.0588874867866859,
94.2110789382982));
#12687=CARTESIAN_POINT('Ctrl Pts',(-2.45049895420091,0.00226394793686294,
94.2079011502642));
#12688=CARTESIAN_POINT('',(-2.45049989228455,-0.000726576496363649,93.4079011502229));
#12689=CARTESIAN_POINT('Ctrl Pts',(-2.45049895420016,0.00226394874617963,
94.2079011502221));
#12690=CARTESIAN_POINT('Ctrl Pts',(-2.45039932002466,0.110108016892512,
94.2022969384674));
#12691=CARTESIAN_POINT('Ctrl Pts',(-2.44317684723875,0.21763439582928,94.1966927267126));
#12692=CARTESIAN_POINT('Ctrl Pts',(-2.4289785155877,0.324058051610146,94.1910885149578));
#12693=CARTESIAN_POINT('Ctrl Pts',(-2.41765385179736,0.408942117617231,
94.1866185662699));
#12694=CARTESIAN_POINT('Ctrl Pts',(-2.40189228346313,0.493125392929466,
94.1821486175821));
#12695=CARTESIAN_POINT('Ctrl Pts',(-2.38178925889044,0.576220596849957,
94.1776786688942));
#12696=CARTESIAN_POINT('Ctrl Pts',(-2.36276431963936,0.654859569852625,
94.1734484346857));
#12697=CARTESIAN_POINT('Ctrl Pts',(-2.33980471071961,0.732703609166421,
94.1692182004772));
#12698=CARTESIAN_POINT('Ctrl Pts',(-2.31299284592925,0.809329564936388,
94.1649879662687));
#12699=CARTESIAN_POINT('Ctrl Pts',(-2.28621956998838,0.885845237162166,
94.1607638204048));
#12700=CARTESIAN_POINT('Ctrl Pts',(-2.2556052017702,0.961145872269699,94.1565396745409));
#12701=CARTESIAN_POINT('Ctrl Pts',(-2.22128274485659,1.0348203792941,94.1523155286769));
#12702=CARTESIAN_POINT('Ctrl Pts',(-2.18678288772607,1.10887568287859,94.1480695497491));
#12703=CARTESIAN_POINT('Ctrl Pts',(-2.14853660786142,1.18128753600972,94.1438235708214));
#12704=CARTESIAN_POINT('Ctrl Pts',(-2.10672922721516,1.25165578862458,94.1395775918936));
#12705=CARTESIAN_POINT('Ctrl Pts',(-2.06521210074575,1.32153549881167,94.1353610913283));
#12706=CARTESIAN_POINT('Ctrl Pts',(-2.02018340462462,1.38939948945081,94.1311445907629));
#12707=CARTESIAN_POINT('Ctrl Pts',(-1.97187125486046,1.45487937790561,94.1269280901976));
#12708=CARTESIAN_POINT('Ctrl Pts',(-1.9235751802654,1.52033747887457,94.1227129926118));
#12709=CARTESIAN_POINT('Ctrl Pts',(-1.87199809752437,1.58341267892187,94.1184978950261));
#12710=CARTESIAN_POINT('Ctrl Pts',(-1.81741086265896,1.64376640867527,94.1142827974403));
#12711=CARTESIAN_POINT('Ctrl Pts',(-1.76282504533444,1.70411857114139,94.1100678093137));
#12712=CARTESIAN_POINT('Ctrl Pts',(-1.70522954413322,1.76174905953555,94.1058528211871));
#12713=CARTESIAN_POINT('Ctrl Pts',(-1.64493386883337,1.81635426532516,94.1016378330605));
#12714=CARTESIAN_POINT('Ctrl Pts',(-1.58386817442722,1.87165681883584,94.0973690165063));
#12715=CARTESIAN_POINT('Ctrl Pts',(-1.52003319995502,1.92385592937759,94.0931001999522));
#12716=CARTESIAN_POINT('Ctrl Pts',(-1.45378561469973,1.97267778324088,94.088831383398));
#12717=CARTESIAN_POINT('Ctrl Pts',(-1.38827798697457,2.02095431762932,94.0846102477207));
#12718=CARTESIAN_POINT('Ctrl Pts',(-1.32041180261381,2.06592845635766,94.0803891120434));
#12719=CARTESIAN_POINT('Ctrl Pts',(-1.25056015427761,2.10737978317463,94.0761679763661));
#12720=CARTESIAN_POINT('Ctrl Pts',(-1.17952496621542,2.14953344548621,94.0718753193735));
#12721=CARTESIAN_POINT('Ctrl Pts',(-1.10643685289585,2.1880435756916,94.0675826623809));
#12722=CARTESIAN_POINT('Ctrl Pts',(-1.03171132518651,2.22272850152282,94.0632900053883));
#12723=CARTESIAN_POINT('Ctrl Pts',(-0.95698579747717,2.25741342735405,94.0589973483957));
#12724=CARTESIAN_POINT('Ctrl Pts',(-0.88062334264572,2.28827302376057,94.0547046914031));
#12725=CARTESIAN_POINT('Ctrl Pts',(-0.803055668404255,2.31517857700951,
94.0504120344106));
#12726=CARTESIAN_POINT('Ctrl Pts',(-0.726615965300836,2.34169287594002,
94.0461818002409));
#12727=CARTESIAN_POINT('Ctrl Pts',(-0.648717580990793,2.3644674163922,94.0419515660712));
#12728=CARTESIAN_POINT('Ctrl Pts',(-0.569761040408466,2.38334273801161,
94.0377213319016));
#12729=CARTESIAN_POINT('Ctrl Pts',(-0.490918137661165,2.40219089341187,
94.0334971860768));
#12730=CARTESIAN_POINT('Ctrl Pts',(-0.411020551847942,2.417150868248,94.0292730402521));
#12731=CARTESIAN_POINT('Ctrl Pts',(-0.330486016570684,2.42811227970439,
94.0250488944273));
#12732=CARTESIAN_POINT('Ctrl Pts',(-0.249535226821358,2.43913034681196,
94.0208029154898));
#12733=CARTESIAN_POINT('Ctrl Pts',(-0.167941333160773,2.44610823691553,
94.0165569365523));
#12734=CARTESIAN_POINT('Ctrl Pts',(-0.0861411529701344,2.4489854943966,
94.0123109576148));
#12735=CARTESIAN_POINT('Ctrl Pts',(-0.00490888407719281,2.45184277604112,
94.0080944570892));
#12736=CARTESIAN_POINT('Ctrl Pts',(0.0765263450380388,2.45065616682677,
94.0038779565636));
#12737=CARTESIAN_POINT('Ctrl Pts',(0.157731302710592,2.44541838672756,93.999661456038));
#12738=CARTESIAN_POINT('Ctrl Pts',(0.238909240605338,2.44018234942409,93.9954463584922));
#12739=CARTESIAN_POINT('Ctrl Pts',(0.319856595358821,2.43089784795572,93.9912312609463));
#12740=CARTESIAN_POINT('Ctrl Pts',(0.400142106332113,2.41760967584515,93.9870161634004));
#12741=CARTESIAN_POINT('Ctrl Pts',(0.480425532421095,2.40432184880683,93.9828011753138));
#12742=CARTESIAN_POINT('Ctrl Pts',(0.560046690133499,2.38703063485041,93.9785861872272));
#12743=CARTESIAN_POINT('Ctrl Pts',(0.63858282950093,2.36583224677207,93.9743711991405));
#12744=CARTESIAN_POINT('Ctrl Pts',(0.718121933438913,2.34436313960355,93.9701023825394));
#12745=CARTESIAN_POINT('Ctrl Pts',(0.796547632615247,2.3188864644694,93.9658335659383));
#12746=CARTESIAN_POINT('Ctrl Pts',(0.873436743013434,2.28955421555247,93.9615647493371));
#12747=CARTESIAN_POINT('Ctrl Pts',(0.94946703299072,2.26054959605185,93.9573436136995));
#12748=CARTESIAN_POINT('Ctrl Pts',(1.02399448335681,2.22777535070441,93.953122478062));
#12749=CARTESIAN_POINT('Ctrl Pts',(1.09663194973094,2.19142616047845,93.9489013424244));
#12750=CARTESIAN_POINT('Ctrl Pts',(1.17050015992039,2.15446108229142,93.9446086853415));
#12751=CARTESIAN_POINT('Ctrl Pts',(1.24241330787115,2.11379903758172,93.9403160282586));
#12752=CARTESIAN_POINT('Ctrl Pts',(1.31199390695758,2.0696913388489,93.9360233711757));
#12753=CARTESIAN_POINT('Ctrl Pts',(1.38157450604402,2.02558364011609,93.9317307140928));
#12754=CARTESIAN_POINT('Ctrl Pts',(1.44882218761369,1.97803062965081,93.9274380570099));
#12755=CARTESIAN_POINT('Ctrl Pts',(1.51339525790319,1.92732587886848,93.923145399927));
#12756=CARTESIAN_POINT('Ctrl Pts',(1.57702932007514,1.87735846599449,93.9189151657679));
#12757=CARTESIAN_POINT('Ctrl Pts',(1.63830607531441,1.82414195352704,93.9146849316088));
#12758=CARTESIAN_POINT('Ctrl Pts',(1.69687482490868,1.76792705692037,93.9104546974497));
#12759=CARTESIAN_POINT('Ctrl Pts',(1.755359279697,1.71179306734748,93.9062305516358));
#12760=CARTESIAN_POINT('Ctrl Pts',(1.81114313664065,1.65266958357601,93.902006405822));
#12761=CARTESIAN_POINT('Ctrl Pts',(1.86390767800933,1.59084833276396,93.8977822600081));
#12762=CARTESIAN_POINT('Ctrl Pts',(1.91694494076326,1.52870754961595,93.8935362810679));
#12763=CARTESIAN_POINT('Ctrl Pts',(1.9669312089842,1.46384132241965,93.8892903021277));
#12764=CARTESIAN_POINT('Ctrl Pts',(2.01357944683973,1.39658442683018,93.8850443231875));
#12765=CARTESIAN_POINT('Ctrl Pts',(2.05990382142216,1.32979447360222,93.8808278226735));
#12766=CARTESIAN_POINT('Ctrl Pts',(2.10293609993088,1.26064732937696,93.8766113221595));
#12767=CARTESIAN_POINT('Ctrl Pts',(2.14243591804438,1.18950350443929,93.8723948216455));
#12768=CARTESIAN_POINT('Ctrl Pts',(2.18192259316115,1.11838335158676,93.8681797241115));
#12769=CARTESIAN_POINT('Ctrl Pts',(2.21787891632128,1.04526824370379,93.8639646265774));
#12770=CARTESIAN_POINT('Ctrl Pts',(2.25010939460911,0.970545188176116,93.8597495290434));
#12771=CARTESIAN_POINT('Ctrl Pts',(2.28233903592208,0.895824073088757,93.8555345409688));
#12772=CARTESIAN_POINT('Ctrl Pts',(2.31084284146848,0.819495520943343,93.8513195528942));
#12773=CARTESIAN_POINT('Ctrl Pts',(2.33547317520619,0.741967181142355,93.8471045648196));
#12774=CARTESIAN_POINT('Ctrl Pts',(2.36041805666823,0.663448746642874,93.8428357482049));
#12775=CARTESIAN_POINT('Ctrl Pts',(2.3813896641976,0.583700122860648,93.8385669315902));
#12776=CARTESIAN_POINT('Ctrl Pts',(2.39828705191424,0.503159484279612,93.8342981149755));
#12777=CARTESIAN_POINT('Ctrl Pts',(2.41499570250767,0.423518452707753,93.8300769793504));
#12778=CARTESIAN_POINT('Ctrl Pts',(2.42772068265479,0.34310348603632,93.8258558437253));
#12779=CARTESIAN_POINT('Ctrl Pts',(2.43641644173113,0.262345521140035,93.8216347081001));
#12780=CARTESIAN_POINT('Ctrl Pts',(2.44525953878754,0.180219220792155,93.8173420509907));
#12781=CARTESIAN_POINT('Ctrl Pts',(2.44993558013904,0.0977386930405679,
93.8130493938812));
#12782=CARTESIAN_POINT('Ctrl Pts',(2.45045187693754,0.0153573699988048,
93.8087567367717));
#12783=CARTESIAN_POINT('Ctrl Pts',(2.45096817373604,-0.0670239530429584,
93.8044640796623));
#12784=CARTESIAN_POINT('Ctrl Pts',(2.44732481460251,-0.149305576184179,
93.8001714225528));
#12785=CARTESIAN_POINT('Ctrl Pts',(2.43958401258297,-0.231041328661296,
93.7958787654433));
#12786=CARTESIAN_POINT('Ctrl Pts',(2.43195577571441,-0.311588496635811,
93.7916485312707));
#12787=CARTESIAN_POINT('Ctrl Pts',(2.42031975512473,-0.391909359454666,
93.7874182970981));
#12788=CARTESIAN_POINT('Ctrl Pts',(2.40469724343616,-0.471573342557164,
93.7831880629255));
#12789=CARTESIAN_POINT('Ctrl Pts',(2.38909721637532,-0.551122669640198,
93.7789639170979));
#12790=CARTESIAN_POINT('Ctrl Pts',(2.36952218193655,-0.630016542030731,
93.7747397712702));
#12791=CARTESIAN_POINT('Ctrl Pts',(2.34604522443331,-0.70782911420317,93.7705156254426));
#12792=CARTESIAN_POINT('Ctrl Pts',(2.32244692287695,-0.786043871918182,
93.7662696465058));
#12793=CARTESIAN_POINT('Ctrl Pts',(2.29490628741051,-0.863165644642283,
93.762023667569));
#12794=CARTESIAN_POINT('Ctrl Pts',(2.26354974573485,-0.93877196303666,93.7577776886322));
#12795=CARTESIAN_POINT('Ctrl Pts',(2.23241090201725,-1.01385337210587,93.7535611881039));
#12796=CARTESIAN_POINT('Ctrl Pts',(2.19750914997221,-1.08743986743532,93.7493446875756));
#12797=CARTESIAN_POINT('Ctrl Pts',(2.15901780038694,-1.15913432681995,93.7451281870473));
#12798=CARTESIAN_POINT('Ctrl Pts',(2.12053925824342,-1.23080493090663,93.7409130894988));
#12799=CARTESIAN_POINT('Ctrl Pts',(2.07847371024361,-1.30058433968162,93.7366979919503));
#12800=CARTESIAN_POINT('Ctrl Pts',(2.03304101838861,-1.36809885152696,93.7324828944018));
#12801=CARTESIAN_POINT('Ctrl Pts',(1.98760950634764,-1.43561161012888,93.7282679063126));
#12802=CARTESIAN_POINT('Ctrl Pts',(1.93881128489416,-1.50085920339646,93.7240529182234));
#12803=CARTESIAN_POINT('Ctrl Pts',(1.88690945597032,-1.56349702748991,93.7198379301341));
#12804=CARTESIAN_POINT('Ctrl Pts',(1.83434480238627,-1.62693478282533,93.7155691135363));
#12805=CARTESIAN_POINT('Ctrl Pts',(1.77859700556951,-1.68769525030285,93.7113002969384));
#12806=CARTESIAN_POINT('Ctrl Pts',(1.71998009048483,-1.74545659881184,93.7070314803405));
#12807=CARTESIAN_POINT('Ctrl Pts',(1.66201790267599,-1.80257277637822,93.7028103447006));
#12808=CARTESIAN_POINT('Ctrl Pts',(1.60125076402844,-1.85675623221234,93.6985892090606));
#12809=CARTESIAN_POINT('Ctrl Pts',(1.53801656220287,-1.90773564845595,93.6943680734207));
#12810=CARTESIAN_POINT('Ctrl Pts',(1.47371094231323,-1.9595788419891,93.6900754163439));
#12811=CARTESIAN_POINT('Ctrl Pts',(1.40685428842817,-2.00810811710232,93.685782759267));
#12812=CARTESIAN_POINT('Ctrl Pts',(1.33783199317452,-2.05308446198365,93.6814901021902));
#12813=CARTESIAN_POINT('Ctrl Pts',(1.26880969792087,-2.09806080686498,93.6771974451134));
#12814=CARTESIAN_POINT('Ctrl Pts',(1.19762222578243,-2.13948402832458,93.6729047880365));
#12815=CARTESIAN_POINT('Ctrl Pts',(1.12467854535163,-2.17716522561466,93.6686121309597));
#12816=CARTESIAN_POINT('Ctrl Pts',(1.05279559644858,-2.21429847092683,93.6643818967915));
#12817=CARTESIAN_POINT('Ctrl Pts',(0.97893608890089,-2.24793789881027,93.6601516626233));
#12818=CARTESIAN_POINT('Ctrl Pts',(0.903473746455619,-2.27786861769186,
93.6559214284551));
#12819=CARTESIAN_POINT('Ctrl Pts',(0.828120012839371,-2.30775625892408,
93.6516972826319));
#12820=CARTESIAN_POINT('Ctrl Pts',(0.751168454586691,-2.3339456220617,93.6474731368088));
#12821=CARTESIAN_POINT('Ctrl Pts',(0.673016820036839,-2.35626794103461,
93.6432489909857));
#12822=CARTESIAN_POINT('Ctrl Pts',(0.594461247347319,-2.37870563617401,
93.6390030120478));
#12823=CARTESIAN_POINT('Ctrl Pts',(0.514693578532129,-2.39723597468178,
93.6347570331099));
#12824=CARTESIAN_POINT('Ctrl Pts',(0.434137563550564,-2.41173688986058,
93.630511054172));
#12825=CARTESIAN_POINT('Ctrl Pts',(0.354140822087412,-2.42613713002641,
93.6262945536483));
#12826=CARTESIAN_POINT('Ctrl Pts',(0.273367110099192,-2.43656363606648,
93.6220780531247));
#12827=CARTESIAN_POINT('Ctrl Pts',(0.192244203631005,-2.44294748534844,
93.617861552601));
#12828=CARTESIAN_POINT('Ctrl Pts',(0.111148289641529,-2.4493292104965,93.6136464550572));
#12829=CARTESIAN_POINT('Ctrl Pts',(0.0297038752827075,-2.45167091359718,
93.6094313575134));
#12830=CARTESIAN_POINT('Ctrl Pts',(-0.0516557960857132,-2.44995549525512,
93.6052162599696));
#12831=CARTESIAN_POINT('Ctrl Pts',(-0.133013354673379,-2.44824012145973,
93.6010012718851));
#12832=CARTESIAN_POINT('Ctrl Pts',(-0.214285709586253,-2.44246784656551,
93.5967862838006));
#12833=CARTESIAN_POINT('Ctrl Pts',(-0.29504071630266,-2.43267367842948,
93.5925712957161));
#12834=CARTESIAN_POINT('Ctrl Pts',(-0.376827024250353,-2.4227544315142,
93.5883024791128));
#12835=CARTESIAN_POINT('Ctrl Pts',(-0.458082188896049,-2.40870987757979,
93.5840336625095));
#12836=CARTESIAN_POINT('Ctrl Pts',(-0.538365689650037,-2.39063017512279,
93.5797648459061));
#12837=CARTESIAN_POINT('Ctrl Pts',(-0.617752455922586,-2.37275241568591,
93.575543710271));
#12838=CARTESIAN_POINT('Ctrl Pts',(-0.696188719385308,-2.35092938689105,
93.5713225746358));
#12839=CARTESIAN_POINT('Ctrl Pts',(-0.773263550488758,-2.32529863275355,
93.5671014390006));
#12840=CARTESIAN_POINT('Ctrl Pts',(-0.851644310689964,-2.29923360004357,
93.5628087819132));
#12841=CARTESIAN_POINT('Ctrl Pts',(-0.928616606842926,-2.26923079398519,
93.5585161248258));
#12842=CARTESIAN_POINT('Ctrl Pts',(-1.00377100109754,-2.23548518835524,
93.5542234677384));
#12843=CARTESIAN_POINT('Ctrl Pts',(-1.07892539535214,-2.20173958272529,
93.549930810651));
#12844=CARTESIAN_POINT('Ctrl Pts',(-1.15226147405417,-2.1642514638063,93.5456381535636));
#12845=CARTESIAN_POINT('Ctrl Pts',(-1.2233992070889,-2.12326273223411,93.5413454964762));
#12846=CARTESIAN_POINT('Ctrl Pts',(-1.29350247020591,-2.08287005015588,
93.5371152623032));
#12847=CARTESIAN_POINT('Ctrl Pts',(-1.36173532530319,-2.03892559130925,
93.5328850281303));
#12848=CARTESIAN_POINT('Ctrl Pts',(-1.42771493428827,-1.99162755464224,
93.5286547939573));
#12849=CARTESIAN_POINT('Ctrl Pts',(-1.49359958242498,-1.94439759145668,
93.5244306481294));
#12850=CARTESIAN_POINT('Ctrl Pts',(-1.55723705026384,-1.89382390501511,
93.5202065023015));
#12851=CARTESIAN_POINT('Ctrl Pts',(-1.61827031211913,-1.84014984360346,
93.5159823564736));
#12852=CARTESIAN_POINT('Ctrl Pts',(-1.67961903321785,-1.78619836004052,
93.5117363775369));
#12853=CARTESIAN_POINT('Ctrl Pts',(-1.73833613527186,-1.72911459391617,
93.5074903986002));
#12854=CARTESIAN_POINT('Ctrl Pts',(-1.79408981881717,-1.66918901626405,
93.5032444196635));
#12855=CARTESIAN_POINT('Ctrl Pts',(-1.84945642322856,-1.60967948180805,
93.4990279191351));
#12856=CARTESIAN_POINT('Ctrl Pts',(-1.90190030582722,-1.54736781541865,
93.4948114186067));
#12857=CARTESIAN_POINT('Ctrl Pts',(-1.95113219657686,-1.48257660897546,
93.4905949180783));
#12858=CARTESIAN_POINT('Ctrl Pts',(-2.00034770612371,-1.41780696087332,
93.4863798205298));
#12859=CARTESIAN_POINT('Ctrl Pts',(-2.04635306492065,-1.3505597811607,93.4821647229812));
#12860=CARTESIAN_POINT('Ctrl Pts',(-2.08889964199823,-1.2811902808169,93.4779496254327));
#12861=CARTESIAN_POINT('Ctrl Pts',(-2.13144511420883,-1.21182258188874,
93.4737346373435));
#12862=CARTESIAN_POINT('Ctrl Pts',(-2.17053174097621,-1.14033306900568,
93.4695196492544));
#12863=CARTESIAN_POINT('Ctrl Pts',(-2.20595531951388,-1.06710420217916,
93.4653046611652));
#12864=CARTESIAN_POINT('Ctrl Pts',(-2.24183128329213,-0.992940148680246,
93.4610358445675));
#12865=CARTESIAN_POINT('Ctrl Pts',(-2.27394974557627,-0.91699243219872,
93.4567670279697));
#12866=CARTESIAN_POINT('Ctrl Pts',(-2.30214836904294,-0.839680377830114,
93.452498211372));
#12867=CARTESIAN_POINT('Ctrl Pts',(-2.33003202526981,-0.763231867896459,
93.4482770757323));
#12868=CARTESIAN_POINT('Ctrl Pts',(-2.35408289289647,-0.685449814745013,
93.4440559400925));
#12869=CARTESIAN_POINT('Ctrl Pts',(-2.37419449592288,-0.606754271125895,
93.4398348044528));
#12870=CARTESIAN_POINT('Ctrl Pts',(-2.3946468628743,-0.526725337906243,
93.4355421473761));
#12871=CARTESIAN_POINT('Ctrl Pts',(-2.41102513613057,-0.445752164087972,
93.4312494902994));
#12872=CARTESIAN_POINT('Ctrl Pts',(-2.42327195772963,-0.364284598742836,
93.4269568332226));
#12873=CARTESIAN_POINT('Ctrl Pts',(-2.43551877932868,-0.282817033397704,
93.4226641761459));
#12874=CARTESIAN_POINT('Ctrl Pts',(-2.44363416644429,-0.200855579290618,
93.4183715190692));
#12875=CARTESIAN_POINT('Ctrl Pts',(-2.44761613749138,-0.118850719357496,
93.4140788619925));
#12876=CARTESIAN_POINT('Ctrl Pts',(-2.44952633505272,-0.0795120396909347,
93.4120196247498));
#12877=CARTESIAN_POINT('Ctrl Pts',(-2.45048821001178,-0.0401269385891838,
93.409960387507));
#12878=CARTESIAN_POINT('Ctrl Pts',(-2.45049989228432,-0.000726577286486693,
93.4079011502642));
#12879=CARTESIAN_POINT('',(-2.45049926108039,-0.00190300932191417,92.6079011502917));
#12880=CARTESIAN_POINT('Ctrl Pts',(-2.45049989228455,-0.000726576496358752,
93.4079011502229));
#12881=CARTESIAN_POINT('Ctrl Pts',(-2.45052370789507,0.0795955249073371,
93.4037031617488));
#12882=CARTESIAN_POINT('Ctrl Pts',(-2.446594086483,0.160078074458993,93.3995051732748));
#12883=CARTESIAN_POINT('Ctrl Pts',(-2.43868984666028,0.240295821428641,
93.3953071848007));
#12884=CARTESIAN_POINT('Ctrl Pts',(-2.43079672481322,0.320400735415266,
93.3911151011492));
#12885=CARTESIAN_POINT('Ctrl Pts',(-2.41894012952624,0.400241119723056,
93.3869230174977));
#12886=CARTESIAN_POINT('Ctrl Pts',(-2.40315089260997,0.479391319641781,
93.3827309338461));
#12887=CARTESIAN_POINT('Ctrl Pts',(-2.38737900061532,0.558454570835878,
93.3785434553166));
#12888=CARTESIAN_POINT('Ctrl Pts',(-2.36768314111001,0.63682868239816,93.3743559767871));
#12889=CARTESIAN_POINT('Ctrl Pts',(-2.34414581799513,0.714094275271782,
93.3701684982576));
#12890=CARTESIAN_POINT('Ctrl Pts',(-2.3206223320979,0.791314444933099,93.3659834814801));
#12891=CARTESIAN_POINT('Ctrl Pts',(-2.2932620011617,0.867426937712915,93.3617984647026));
#12892=CARTESIAN_POINT('Ctrl Pts',(-2.26219786679023,0.942024979228125,
93.357613447925));
#12893=CARTESIAN_POINT('Ctrl Pts',(-2.23114210675983,1.01660291043104,93.353429559354));
#12894=CARTESIAN_POINT('Ctrl Pts',(-2.19638470745337,1.08966676464385,93.349245670783));
#12895=CARTESIAN_POINT('Ctrl Pts',(-2.15810724529095,1.16082874181454,93.3450617822119));
#12896=CARTESIAN_POINT('Ctrl Pts',(-2.1198279183326,1.23199418584424,93.3408776898108));
#12897=CARTESIAN_POINT('Ctrl Pts',(-2.07802841388237,1.30125715337313,93.3366935974097));
#12898=CARTESIAN_POINT('Ctrl Pts',(-2.03293601957873,1.36825487037298,93.3325095050085));
#12899=CARTESIAN_POINT('Ctrl Pts',(-1.98779748611528,1.43532114036097,93.3283211313863));
#12900=CARTESIAN_POINT('Ctrl Pts',(-1.93935960138974,1.50011713980379,93.3241327577642));
#12901=CARTESIAN_POINT('Ctrl Pts',(-1.88789231328252,1.56231010476434,93.319944384142));
#12902=CARTESIAN_POINT('Ctrl Pts',(-1.83639677584122,1.62453720616201,93.3157537116078));
#12903=CARTESIAN_POINT('Ctrl Pts',(-1.78186884546537,1.68415808109405,93.3115630390736));
#12904=CARTESIAN_POINT('Ctrl Pts',(-1.7246162531268,1.74087593740934,93.3073723665395));
#12905=CARTESIAN_POINT('Ctrl Pts',(-1.66726590097464,1.79769064046703,93.3031745383579));
#12906=CARTESIAN_POINT('Ctrl Pts',(-1.60718195106043,1.85159211357102,93.2989767101762));
#12907=CARTESIAN_POINT('Ctrl Pts',(-1.54470580952404,1.90232337209599,93.2947788819946));
#12908=CARTESIAN_POINT('Ctrl Pts',(-1.50518332220491,1.93441603134848,93.2921233304994));
#12909=CARTESIAN_POINT('Ctrl Pts',(-1.46470414331117,1.96524086620808,93.2894677790041));
#12910=CARTESIAN_POINT('Ctrl Pts',(-1.42336023198326,1.99474206352815,93.2868122275088));
#12911=CARTESIAN_POINT('Ctrl Pts',(-1.35750030542381,2.0417368114006,93.282581993338));
#12912=CARTESIAN_POINT('Ctrl Pts',(-1.28918626061932,2.08555494976627,93.2783517591672));
#12913=CARTESIAN_POINT('Ctrl Pts',(-1.21875739691421,2.12593053919146,93.2741215249964));
#12914=CARTESIAN_POINT('Ctrl Pts',(-1.14842989762866,2.16624801823447,93.2698973791708));
#12915=CARTESIAN_POINT('Ctrl Pts',(-1.07599402455916,2.20313255911316,93.2656732333452));
#12916=CARTESIAN_POINT('Ctrl Pts',(-1.0018194275133,2.2363604549931,93.2614490875196));
#12917=CARTESIAN_POINT('Ctrl Pts',(-0.927261448282132,2.2697600940822,93.2572031085823));
#12918=CARTESIAN_POINT('Ctrl Pts',(-0.850947105048476,2.29946489916578,
93.252957129645));
#12919=CARTESIAN_POINT('Ctrl Pts',(-0.773278436698099,2.3252936823846,93.2487111507078));
#12920=CARTESIAN_POINT('Ctrl Pts',(-0.696148995930408,2.35094314500176,
93.2444946501819));
#12921=CARTESIAN_POINT('Ctrl Pts',(-0.617684422978472,2.37277008643907,
93.240278149656));
#12922=CARTESIAN_POINT('Ctrl Pts',(-0.538298312493276,2.39064534734178,
93.2360616491302));
#12923=CARTESIAN_POINT('Ctrl Pts',(-0.458938616594858,2.40851466050845,
93.2318465515842));
#12924=CARTESIAN_POINT('Ctrl Pts',(-0.378658445527426,2.42243480209917,
93.2276314540383));
#12925=CARTESIAN_POINT('Ctrl Pts',(-0.297884188074977,2.43232712859412,
93.2234163564924));
#12926=CARTESIAN_POINT('Ctrl Pts',(-0.217112028203139,2.44221919820089,
93.2192013684059));
#12927=CARTESIAN_POINT('Ctrl Pts',(-0.135846269321706,2.44808360518105,
93.2149863803194));
#12928=CARTESIAN_POINT('Ctrl Pts',(-0.0545196356231395,2.44989343836248,
93.2107713922329));
#12929=CARTESIAN_POINT('Ctrl Pts',(0.0278455993155291,2.4517263844517,93.2065025756323));
#12930=CARTESIAN_POINT('Ctrl Pts',(0.110272786671581,2.44940043248254,93.2022337590317));
#12931=CARTESIAN_POINT('Ctrl Pts',(0.192313055022356,2.44294206621196,93.197964942431));
#12932=CARTESIAN_POINT('Ctrl Pts',(0.273436966586778,2.43655583729393,93.1937438067941));
#12933=CARTESIAN_POINT('Ctrl Pts',(0.354182100494936,2.42612917109596,93.1895226711572));
#12934=CARTESIAN_POINT('Ctrl Pts',(0.434122124168227,2.41173966905793,93.1853015355204));
#12935=CARTESIAN_POINT('Ctrl Pts',(0.51541662363876,2.39710635633097,93.1810088784378));
#12936=CARTESIAN_POINT('Ctrl Pts',(0.595877987104331,2.37837478613998,93.1767162213553));
#12937=CARTESIAN_POINT('Ctrl Pts',(0.675073177205928,2.35567961646254,93.1724235642728));
#12938=CARTESIAN_POINT('Ctrl Pts',(0.754268367307523,2.3329844467851,93.1681309071903));
#12939=CARTESIAN_POINT('Ctrl Pts',(0.83219693382685,2.30632590205602,93.1638382501078));
#12940=CARTESIAN_POINT('Ctrl Pts',(0.908448262154074,2.27588927784048,93.1595455930253));
#12941=CARTESIAN_POINT('Ctrl Pts',(0.983590760481222,2.24589525630179,93.1553153588153));
#12942=CARTESIAN_POINT('Ctrl Pts',(1.05738790226238,2.21211922990983,93.1510851246054));
#12943=CARTESIAN_POINT('Ctrl Pts',(1.12943251915137,2.17470283824788,93.1468548903955));
#12944=CARTESIAN_POINT('Ctrl Pts',(1.20137344616123,2.13734029795328,93.1426307445304));
#12945=CARTESIAN_POINT('Ctrl Pts',(1.27156644837697,2.09634801056346,93.1384065986654));
#12946=CARTESIAN_POINT('Ctrl Pts',(1.33962347476286,2.05191598167768,93.1341824528003));
#12947=CARTESIAN_POINT('Ctrl Pts',(1.40803226298435,2.00725429991298,93.1299364738729));
#12948=CARTESIAN_POINT('Ctrl Pts',(1.47428248740516,1.95911738938175,93.1256904949454));
#12949=CARTESIAN_POINT('Ctrl Pts',(1.53800435297943,1.90774549146796,93.121444516018));
#12950=CARTESIAN_POINT('Ctrl Pts',(1.60128381970143,1.85673025085651,93.1172280154523));
#12951=CARTESIAN_POINT('Ctrl Pts',(1.66206955651884,1.80252509522039,93.1130115148866));
#12952=CARTESIAN_POINT('Ctrl Pts',(1.72002928820667,1.74540811780834,93.1087950143208));
#12953=CARTESIAN_POINT('Ctrl Pts',(1.77796973462824,1.6883101452482,93.104579916735));
#12954=CARTESIAN_POINT('Ctrl Pts',(1.83308571212533,1.62830260114869,93.1003648191491));
#12955=CARTESIAN_POINT('Ctrl Pts',(1.88508052324529,1.56570165449273,93.0961497215633));
#12956=CARTESIAN_POINT('Ctrl Pts',(1.93707398414174,1.50310233348493,93.0919347334369));
#12957=CARTESIAN_POINT('Ctrl Pts',(1.98594614340768,1.43791010235155,93.0877197453105));
#12958=CARTESIAN_POINT('Ctrl Pts',(2.03144039683689,1.37047443029747,93.0835047571841));
#12959=CARTESIAN_POINT('Ctrl Pts',(2.07751564457341,1.3021775562537,93.0792359406306));
#12960=CARTESIAN_POINT('Ctrl Pts',(2.12012580879891,1.23157992872312,93.074967124077));
#12961=CARTESIAN_POINT('Ctrl Pts',(2.15905047210976,1.15907347001069,93.0706983075235));
#12962=CARTESIAN_POINT('Ctrl Pts',(2.19754036337891,1.08737687780473,93.0664771718471));
#12963=CARTESIAN_POINT('Ctrl Pts',(2.2324265290723,1.01381433584631,93.0622560361706));
#12964=CARTESIAN_POINT('Ctrl Pts',(2.26354373970752,0.938786444528733,93.0580349004942));
#12965=CARTESIAN_POINT('Ctrl Pts',(2.2951881885118,0.862487309187705,93.0537422435021));
#12966=CARTESIAN_POINT('Ctrl Pts',(2.32293460907364,0.784673180722974,93.04944958651));
#12967=CARTESIAN_POINT('Ctrl Pts',(2.3466621443104,0.705781149125222,93.0451569295179));
#12968=CARTESIAN_POINT('Ctrl Pts',(2.37038967954715,0.626889117527469,93.0408642725258));
#12969=CARTESIAN_POINT('Ctrl Pts',(2.39009827483509,0.546919682880347,93.0365716155337));
#12970=CARTESIAN_POINT('Ctrl Pts',(2.40572179438023,0.466318451322664,93.0322789585416));
#12971=CARTESIAN_POINT('Ctrl Pts',(2.42111811995924,0.386889306081384,93.0280487244731));
#12972=CARTESIAN_POINT('Ctrl Pts',(2.43260550988883,0.306547053535686,93.0238184904046));
#12973=CARTESIAN_POINT('Ctrl Pts',(2.44008296707689,0.225710796775996,93.0195882563361));
#12974=CARTESIAN_POINT('Ctrl Pts',(2.44754966236895,0.144990883228411,93.0153641106126));
#12975=CARTESIAN_POINT('Ctrl Pts',(2.4510178444076,0.0637788367834349,93.0111399648891));
#12976=CARTESIAN_POINT('Ctrl Pts',(2.4504375392987,-0.0174961708875144,
93.0069158191656));
#12977=CARTESIAN_POINT('Ctrl Pts',(2.44985423478089,-0.099191262715211,
93.0026698402028));
#12978=CARTESIAN_POINT('Ctrl Pts',(2.44518037701346,-0.180949501444377,
92.99842386124));
#12979=CARTESIAN_POINT('Ctrl Pts',(2.43641812250323,-0.262329911252715,
92.9941778822772));
#12980=CARTESIAN_POINT('Ctrl Pts',(2.42771670165569,-0.34314532167704,92.9899613818523));
#12981=CARTESIAN_POINT('Ctrl Pts',(2.41498352373129,-0.423587664264211,
92.9857448814274));
#12982=CARTESIAN_POINT('Ctrl Pts',(2.39827287353054,-0.503227060170226,
92.9815283810025));
#12983=CARTESIAN_POINT('Ctrl Pts',(2.38156778355595,-0.582839957223856,
92.977313283557));
#12984=CARTESIAN_POINT('Ctrl Pts',(2.36088794486213,-0.661649983233959,
92.9730981861114));
#12985=CARTESIAN_POINT('Ctrl Pts',(2.33633890883861,-0.739236601533515,
92.9688830886658));
#12986=CARTESIAN_POINT('Ctrl Pts',(2.31179051031042,-0.8168212050449,92.9646681006788));
#12987=CARTESIAN_POINT('Ctrl Pts',(2.28337325556862,-0.893182020818318,
92.9604531126919));
#12988=CARTESIAN_POINT('Ctrl Pts',(2.25124238673006,-0.967914234935082,
92.956238124705));
#12989=CARTESIAN_POINT('Ctrl Pts',(2.21870118125789,-1.04360083859284,92.9519693079844));
#12990=CARTESIAN_POINT('Ctrl Pts',(2.18235101290933,-1.11761649190415,92.9477004912638));
#12991=CARTESIAN_POINT('Ctrl Pts',(2.14240240208921,-1.1895638686184,92.9434316745432));
#12992=CARTESIAN_POINT('Ctrl Pts',(2.10290000319201,-1.26070761845669,92.939210539003));
#12993=CARTESIAN_POINT('Ctrl Pts',(2.05987944975525,-1.32982869849066,92.9349894034628));
#12994=CARTESIAN_POINT('Ctrl Pts',(2.01358840145199,-1.39657151608431,92.9307682679226));
#12995=CARTESIAN_POINT('Ctrl Pts',(1.96651301023838,-1.46444520579503,92.9264756106118));
#12996=CARTESIAN_POINT('Ctrl Pts',(1.91605557430884,-1.52985889405666,92.922182953301));
#12997=CARTESIAN_POINT('Ctrl Pts',(1.86251844080857,-1.59247458618592,92.9178902959903));
#12998=CARTESIAN_POINT('Ctrl Pts',(1.80898130730829,-1.65509027831519,92.9135976386795));
#12999=CARTESIAN_POINT('Ctrl Pts',(1.75236486738772,-1.71490765797517,92.9093049813687));
#13000=CARTESIAN_POINT('Ctrl Pts',(1.69300821898914,-1.77163015904427,92.9050123240579));
#13001=CARTESIAN_POINT('Ctrl Pts',(1.63451472488171,-1.82752781114492,92.9007820898401));
#13002=CARTESIAN_POINT('Ctrl Pts',(1.57313961198365,-1.88063085808535,92.8965518556222));
#13003=CARTESIAN_POINT('Ctrl Pts',(1.50918083421384,-1.93062773719887,92.8923216214044));
#13004=CARTESIAN_POINT('Ctrl Pts',(1.44531410883259,-1.98055265852483,92.8880974755325));
#13005=CARTESIAN_POINT('Ctrl Pts',(1.37887146708518,-2.02738000662939,92.8838733296605));
#13006=CARTESIAN_POINT('Ctrl Pts',(1.31018692013596,-2.07083569708092,92.8796491837886));
#13007=CARTESIAN_POINT('Ctrl Pts',(1.24114736806969,-2.11451599398559,92.875403204863));
#13008=CARTESIAN_POINT('Ctrl Pts',(1.16984301045906,-2.15478934675703,92.8711572259374));
#13009=CARTESIAN_POINT('Ctrl Pts',(1.09664597431824,-2.19141914224815,92.8669112470118));
#13010=CARTESIAN_POINT('Ctrl Pts',(1.02395711975321,-2.2277946298031,92.8626947464418));
#13011=CARTESIAN_POINT('Ctrl Pts',(0.949402205335669,-2.26057678084734,
92.8584782458718));
#13012=CARTESIAN_POINT('Ctrl Pts',(0.873372207824021,-2.28957883389076,
92.8542617453019));
#13013=CARTESIAN_POINT('Ctrl Pts',(0.797367508216987,-2.31857123691189,
92.8500466477127));
#13014=CARTESIAN_POINT('Ctrl Pts',(0.719889134464225,-2.34378587396247,
92.8458315501235));
#13015=CARTESIAN_POINT('Ctrl Pts',(0.641347923301296,-2.3650841615632,92.8416164525344));
#13016=CARTESIAN_POINT('Ctrl Pts',(0.562808751748022,-2.38638189607604,
92.8374014644057));
#13017=CARTESIAN_POINT('Ctrl Pts',(0.483207246910017,-2.40376336262492,
92.8331864762769));
#13018=CARTESIAN_POINT('Ctrl Pts',(0.402967885948781,-2.41714027993701,
92.8289714881482));
#13019=CARTESIAN_POINT('Ctrl Pts',(0.321703810844169,-2.4306880300698,92.8247026716004));
#13020=CARTESIAN_POINT('Ctrl Pts',(0.239785951321221,-2.44012812440312,
92.8204338550525));
#13021=CARTESIAN_POINT('Ctrl Pts',(0.157662373535208,-2.44542283173509,
92.8161650385047));
#13022=CARTESIAN_POINT('Ctrl Pts',(0.0764560813043814,-2.45065839943035,
92.8119439028283));
#13023=CARTESIAN_POINT('Ctrl Pts',(-0.00495088474896378,-2.45184077868515,
92.807722767152));
#13024=CARTESIAN_POINT('Ctrl Pts',(-0.0861254853411517,-2.44898604544304,
92.8035016314756));
#13025=CARTESIAN_POINT('Ctrl Pts',(-0.168675477295125,-2.44608294269357,
92.7992089744921));
#13026=CARTESIAN_POINT('Ctrl Pts',(-0.250984655618082,-2.43900469479108,
92.7949163175085));
#13027=CARTESIAN_POINT('Ctrl Pts',(-0.332605216569839,-2.42782289714685,
92.7906236605249));
#13028=CARTESIAN_POINT('Ctrl Pts',(-0.414225777521596,-2.41664109950263,
92.7863310035414));
#13029=CARTESIAN_POINT('Ctrl Pts',(-0.495157243503421,-2.40135591012571,
92.7820383465578));
#13030=CARTESIAN_POINT('Ctrl Pts',(-0.574966791155317,-2.38209223983215,
92.7777456895743));
#13031=CARTESIAN_POINT('Ctrl Pts',(-0.653615772711475,-2.36310869595555,
92.7735154550991));
#13032=CARTESIAN_POINT('Ctrl Pts',(-0.731471891581371,-2.34019006404083,
92.7692852206239));
#13033=CARTESIAN_POINT('Ctrl Pts',(-0.808111954547987,-2.31341853518049,
92.7650549861487));
#13034=CARTESIAN_POINT('Ctrl Pts',(-0.884641713695443,-2.28668553710631,
92.7608308400169));
#13035=CARTESIAN_POINT('Ctrl Pts',(-0.959958457488453,-2.25611080728024,
92.756606693885));
#13036=CARTESIAN_POINT('Ctrl Pts',(-1.03365102497352,-2.22182713291813,
92.7523825477532));
#13037=CARTESIAN_POINT('Ctrl Pts',(-1.10772447650297,-2.18736626151983,
92.7481365688922));
#13038=CARTESIAN_POINT('Ctrl Pts',(-1.18015644979191,-2.14915810302381,
92.7438905900313));
#13039=CARTESIAN_POINT('Ctrl Pts',(-1.25054669734552,-2.10738776872179,
92.7396446111704));
#13040=CARTESIAN_POINT('Ctrl Pts',(-1.32044825532549,-2.06590742809887,
92.7354281103362));
#13041=CARTESIAN_POINT('Ctrl Pts',(-1.38833594214196,-2.02091445690706,
92.731211609502));
#13042=CARTESIAN_POINT('Ctrl Pts',(-1.45384125510295,-1.97263677725036,
92.7269951086678));
#13043=CARTESIAN_POINT('Ctrl Pts',(-1.51932477211615,-1.92437516129503,
92.7227800108134));
#13044=CARTESIAN_POINT('Ctrl Pts',(-1.58242711524957,-1.87283128300427,
92.718564912959));
#13045=CARTESIAN_POINT('Ctrl Pts',(-1.64280957257505,-1.81827582018125,
92.7143498151046));
#13046=CARTESIAN_POINT('Ctrl Pts',(-1.70319046185879,-1.76372177408166,
92.71013482671));
#13047=CARTESIAN_POINT('Ctrl Pts',(-1.76085126131092,-1.70615661159099,
92.7059198383154));
#13048=CARTESIAN_POINT('Ctrl Pts',(-1.81548819949196,-1.64588968266571,
92.7017048499208));
#13049=CARTESIAN_POINT('Ctrl Pts',(-1.87082288299455,-1.58485311017875,
92.6974360336849));
#13050=CARTESIAN_POINT('Ctrl Pts',(-1.92305558209633,-1.5210456249169,92.6931672174491));
#13051=CARTESIAN_POINT('Ctrl Pts',(-1.97191229546202,-1.45482375187021,
92.6888984012133));
#13052=CARTESIAN_POINT('Ctrl Pts',(-2.0202233066089,-1.38934154018355,92.6846772652721));
#13053=CARTESIAN_POINT('Ctrl Pts',(-2.06523316365711,-1.32149903360087,
92.680456129331));
#13054=CARTESIAN_POINT('Ctrl Pts',(-2.10672125396135,-1.25166920873988,
92.6762349933899));
#13055=CARTESIAN_POINT('Ctrl Pts',(-2.14891229404025,-1.18065622844101,
92.6719423370067));
#13056=CARTESIAN_POINT('Ctrl Pts',(-2.18746088418393,-1.10758840587916,
92.6676496806235));
#13057=CARTESIAN_POINT('Ctrl Pts',(-2.22218513349975,-1.03288115601589,
92.6633570242403));
#13058=CARTESIAN_POINT('Ctrl Pts',(-2.25690938281556,-0.958173906152611,
92.6590643678571));
#13059=CARTESIAN_POINT('Ctrl Pts',(-2.28780916599659,-0.881827716189098,
92.6547717114739));
#13060=CARTESIAN_POINT('Ctrl Pts',(-2.31475554210733,-0.804274225798275,
92.6504790550907));
#13061=CARTESIAN_POINT('Ctrl Pts',(-2.34592638274948,-0.714562441167906,
92.6455134260391));
#13062=CARTESIAN_POINT('Ctrl Pts',(-2.37190502880027,-0.622958806512549,
92.6405477969874));
#13063=CARTESIAN_POINT('Ctrl Pts',(-2.39249357676296,-0.530023334531582,
92.6355821679358));
#13064=CARTESIAN_POINT('Ctrl Pts',(-2.41287918516334,-0.43800391957615,
92.6306654846664));
#13065=CARTESIAN_POINT('Ctrl Pts',(-2.4279803610644,-0.344678912633406,
92.6257488013971));
#13066=CARTESIAN_POINT('Ctrl Pts',(-2.43765120865071,-0.250612918589105,
92.6208321181277));
#13067=CARTESIAN_POINT('Ctrl Pts',(-2.44612937792563,-0.168147817841233,
92.6165217955157));
#13068=CARTESIAN_POINT('Ctrl Pts',(-2.45043464139583,-0.08511357872822,
92.6122114729037));
#13069=CARTESIAN_POINT('Ctrl Pts',(-2.45049926108039,-0.00190300932192698,
92.6079011502917));
#13070=CARTESIAN_POINT('',(-2.45049953842671,0.00150405135357228,91.8079011502354));
#13071=CARTESIAN_POINT('Ctrl Pts',(-2.4504992610808,-0.00190300879332999,
92.6079011502643));
#13072=CARTESIAN_POINT('Ctrl Pts',(-2.45056242607356,0.0794343810401948,
92.6036878586945));
#13073=CARTESIAN_POINT('Ctrl Pts',(-2.44657163267656,0.160818933598828,
92.5994745671246));
#13074=CARTESIAN_POINT('Ctrl Pts',(-2.43853945979514,0.241817189260865,
92.5952612755548));
#13075=CARTESIAN_POINT('Ctrl Pts',(-2.43050856615323,0.32280254478121,92.5910486550125));
#13076=CARTESIAN_POINT('Ctrl Pts',(-2.41843761755519,0.403401262967549,
92.5868360344702));
#13077=CARTESIAN_POINT('Ctrl Pts',(-2.40239111851131,0.483184399270065,
92.5826234139278));
#13078=CARTESIAN_POINT('Ctrl Pts',(-2.38634225763883,0.562979278576021,
92.5784101733445));
#13079=CARTESIAN_POINT('Ctrl Pts',(-2.36631677735233,0.641957882004794,
92.5741969327612));
#13080=CARTESIAN_POINT('Ctrl Pts',(-2.34243012355466,0.719702276127901,
92.5699836921778));
#13081=CARTESIAN_POINT('Ctrl Pts',(-2.3185158530207,0.797536555023019,92.5657655804244));
#13082=CARTESIAN_POINT('Ctrl Pts',(-2.29073163376794,0.874133330505025,
92.5615474686709));
#13083=CARTESIAN_POINT('Ctrl Pts',(-2.25924240106489,0.949091156438903,
92.5573293569174));
#13084=CARTESIAN_POINT('Ctrl Pts',(-2.22773386475762,1.02409493319728,92.5531086593671));
#13085=CARTESIAN_POINT('Ctrl Pts',(-2.19251599537294,1.09745734135112,92.5488879618168));
#13086=CARTESIAN_POINT('Ctrl Pts',(-2.15380026986483,1.16880051656824,92.5446672642665));
#13087=CARTESIAN_POINT('Ctrl Pts',(-2.11501406719797,1.24027356315465,92.5404388834616));
#13088=CARTESIAN_POINT('Ctrl Pts',(-2.0727175352075,1.30971963942041,92.5362105026568));
#13089=CARTESIAN_POINT('Ctrl Pts',(-2.02716597175543,1.37678915341342,92.531982121852));
#13090=CARTESIAN_POINT('Ctrl Pts',(-1.99567451587214,1.42315675270005,92.5290588881037));
#13091=CARTESIAN_POINT('Ctrl Pts',(-1.96262822674959,1.46838911902986,92.5261356543553));
#13092=CARTESIAN_POINT('Ctrl Pts',(-1.92812221977048,1.51238055912768,92.523212420607));
#13093=CARTESIAN_POINT('Ctrl Pts',(-1.87818830234013,1.57604092234551,92.5189821857755));
#13094=CARTESIAN_POINT('Ctrl Pts',(-1.82500404415984,1.63734568847151,92.514751950944));
#13095=CARTESIAN_POINT('Ctrl Pts',(-1.76881997612733,1.69594402680422,92.5105217161125));
#13096=CARTESIAN_POINT('Ctrl Pts',(-1.71271677083371,1.75445802766728,92.5062975696329));
#13097=CARTESIAN_POINT('Ctrl Pts',(-1.65362264953648,1.81027300386652,92.5020734231532));
#13098=CARTESIAN_POINT('Ctrl Pts',(-1.59182917166381,1.86307008409241,92.4978492766736));
#13099=CARTESIAN_POINT('Ctrl Pts',(-1.5297163172406,1.91614004343017,92.4936032979007));
#13100=CARTESIAN_POINT('Ctrl Pts',(-1.46487641363222,1.96616044360353,92.4893573191277));
#13101=CARTESIAN_POINT('Ctrl Pts',(-1.39764408523588,2.0128440727004,92.4851113403548));
#13102=CARTESIAN_POINT('Ctrl Pts',(-1.33087851579443,2.0592036017334,92.4808948391957));
#13103=CARTESIAN_POINT('Ctrl Pts',(-1.26175402222121,2.10227227508018,92.4766783380367));
#13104=CARTESIAN_POINT('Ctrl Pts',(-1.19063098829858,2.14180953861522,92.4724618368776));
#13105=CARTESIAN_POINT('Ctrl Pts',(-1.11953161969357,2.18133364661052,92.4682467387076));
#13106=CARTESIAN_POINT('Ctrl Pts',(-1.04643543753931,2.21732845233955,92.4640316405376));
#13107=CARTESIAN_POINT('Ctrl Pts',(-0.971729346338488,2.24959825912641,
92.4598165423676));
#13108=CARTESIAN_POINT('Ctrl Pts',(-0.89702519531303,2.28186722784126,92.455601553667));
#13109=CARTESIAN_POINT('Ctrl Pts',(-0.820711645839797,2.31041120646844,
92.4513865649663));
#13110=CARTESIAN_POINT('Ctrl Pts',(-0.743196269632219,2.33508234433066,
92.4471715762657));
#13111=CARTESIAN_POINT('Ctrl Pts',(-0.664690990092166,2.36006854280124,
92.4429027604205));
#13112=CARTESIAN_POINT('Ctrl Pts',(-0.584953430463237,2.38108211698799,
92.4386339445753));
#13113=CARTESIAN_POINT('Ctrl Pts',(-0.504421711694072,2.39802189038625,
92.4343651287302));
#13114=CARTESIAN_POINT('Ctrl Pts',(-0.424789474714928,2.41477245861253,
92.4301439925096));
#13115=CARTESIAN_POINT('Ctrl Pts',(-0.344381205452798,2.42753976328988,
92.4259228562889));
#13116=CARTESIAN_POINT('Ctrl Pts',(-0.263627816841055,2.43627802686549,
92.4217017200683));
#13117=CARTESIAN_POINT('Ctrl Pts',(-0.181506209679372,2.44516434434354,
92.4174090644109));
#13118=CARTESIAN_POINT('Ctrl Pts',(-0.0990281817692588,2.44988379597553,
92.4131164087534));
#13119=CARTESIAN_POINT('Ctrl Pts',(-0.0166471684788547,2.45044345410818,
92.4088237530959));
#13120=CARTESIAN_POINT('Ctrl Pts',(0.0657338448115509,2.45100311224084,
92.4045310974384));
#13121=CARTESIAN_POINT('Ctrl Pts',(0.148017348246232,2.44740306523394,92.400238441781));
#13122=CARTESIAN_POINT('Ctrl Pts',(0.229757138867459,2.43970529104223,92.3959457861235));
#13123=CARTESIAN_POINT('Ctrl Pts',(0.310308354856322,2.43211944984008,92.3917155497795));
#13124=CARTESIAN_POINT('Ctrl Pts',(0.390635373853221,2.42052570211332,92.3874853134356));
#13125=CARTESIAN_POINT('Ctrl Pts',(0.470307609770855,2.40494511417446,92.3832550770917));
#13126=CARTESIAN_POINT('Ctrl Pts',(0.54986517813793,2.38938695045698,92.3790309290774));
#13127=CARTESIAN_POINT('Ctrl Pts',(0.628769382404817,2.36985343097383,92.3748067810632));
#13128=CARTESIAN_POINT('Ctrl Pts',(0.706594338299834,2.34641741620766,92.370582633049));
#13129=CARTESIAN_POINT('Ctrl Pts',(0.784821493214441,2.32286028422331,92.3663366546569));
#13130=CARTESIAN_POINT('Ctrl Pts',(0.861957737646102,2.29536024502775,92.3620906762649));
#13131=CARTESIAN_POINT('Ctrl Pts',(0.937580536278816,2.26404350399703,92.3578446978728));
#13132=CARTESIAN_POINT('Ctrl Pts',(1.01267836012187,2.23294416432982,92.353628195137));
#13133=CARTESIAN_POINT('Ctrl Pts',(1.08628324891366,2.19808112658015,92.3494116924011));
#13134=CARTESIAN_POINT('Ctrl Pts',(1.15799798899147,2.15962749276159,92.3451951896653));
#13135=CARTESIAN_POINT('Ctrl Pts',(1.22968886708583,2.12118665380184,92.3409800899063));
#13136=CARTESIAN_POINT('Ctrl Pts',(1.29949043573397,2.07915781089497,92.3367649901472));
#13137=CARTESIAN_POINT('Ctrl Pts',(1.3670288773691,2.0337606295823,92.3325498903882));
#13138=CARTESIAN_POINT('Ctrl Pts',(1.43456556513953,1.9883646271614,92.3283349000886));
#13139=CARTESIAN_POINT('Ctrl Pts',(1.49983885726426,1.93960072063591,92.3241199097889));
#13140=CARTESIAN_POINT('Ctrl Pts',(1.56250401119836,1.88773183079299,92.3199049194892));
#13141=CARTESIAN_POINT('Ctrl Pts',(1.62596937330396,1.83520059661843,92.3156361055018));
#13142=CARTESIAN_POINT('Ctrl Pts',(1.68675912641859,1.77948481501085,92.3113672915143));
#13143=CARTESIAN_POINT('Ctrl Pts',(1.74455127498463,1.72089834067835,92.3070984775269));
#13144=CARTESIAN_POINT('Ctrl Pts',(1.80169797314627,1.66296618816099,92.3028773396993));
#13145=CARTESIAN_POINT('Ctrl Pts',(1.85591342349688,1.60222753885427,92.2986562018717));
#13146=CARTESIAN_POINT('Ctrl Pts',(1.90692613005042,1.53902013779253,92.2944350640442));
#13147=CARTESIAN_POINT('Ctrl Pts',(1.95880309052766,1.47474188109374,92.2901424119768));
#13148=CARTESIAN_POINT('Ctrl Pts',(2.00736748366151,1.40791085252572,92.2858497599094));
#13149=CARTESIAN_POINT('Ctrl Pts',(2.05238009564119,1.33891231714996,92.281557107842));
#13150=CARTESIAN_POINT('Ctrl Pts',(2.09739270762087,1.26991378177419,92.2772644557746));
#13151=CARTESIAN_POINT('Ctrl Pts',(2.13885334501351,1.19874820396808,92.2729718037073));
#13152=CARTESIAN_POINT('Ctrl Pts',(2.17657289230003,1.12582445101564,92.2686791516399));
#13153=CARTESIAN_POINT('Ctrl Pts',(2.21374390716426,1.0539611838253,92.2644489249992));
#13154=CARTESIAN_POINT('Ctrl Pts',(2.24742215915486,0.980119523096709,92.2602186983586));
#13155=CARTESIAN_POINT('Ctrl Pts',(2.27739255994902,0.904673077906526,92.255988471718));
#13156=CARTESIAN_POINT('Ctrl Pts',(2.30731982586546,0.829335218958139,92.251764333428));
#13157=CARTESIAN_POINT('Ctrl Pts',(2.33354966884192,0.752397591305803,92.247540195138));
#13158=CARTESIAN_POINT('Ctrl Pts',(2.35591311335638,0.674257852987607,92.243316056848));
#13159=CARTESIAN_POINT('Ctrl Pts',(2.37839219665573,0.595714063120693,92.2390700760275));
#13160=CARTESIAN_POINT('Ctrl Pts',(2.39696455807962,0.515956116139998,92.234824095207));
#13161=CARTESIAN_POINT('Ctrl Pts',(2.41150790699371,0.435407699181804,92.2305781143866));
#13162=CARTESIAN_POINT('Ctrl Pts',(2.42595025422533,0.355418680590661,92.2263616213552));
#13163=CARTESIAN_POINT('Ctrl Pts',(2.43641928988118,0.274650600485336,92.2221451283239));
#13164=CARTESIAN_POINT('Ctrl Pts',(2.44284586612902,0.193531197320604,92.2179286352926));
#13165=CARTESIAN_POINT('Ctrl Pts',(2.44927030407069,0.112438784907014,92.2137135452094));
#13166=CARTESIAN_POINT('Ctrl Pts',(2.45165491688449,0.0309957449287714,
92.2094984551262));
#13167=CARTESIAN_POINT('Ctrl Pts',(2.44998237708902,-0.0503646895478568,
92.205283365043));
#13168=CARTESIAN_POINT('Ctrl Pts',(2.44830988071032,-0.131723012022023,
92.2010683843776));
#13169=CARTESIAN_POINT('Ctrl Pts',(2.44258045174376,-0.212998268190724,
92.1968534037122));
#13170=CARTESIAN_POINT('Ctrl Pts',(2.43282887053207,-0.293758296403091,
92.1926384230469));
#13171=CARTESIAN_POINT('Ctrl Pts',(2.42295271646221,-0.375550004229518,
92.188369597556));
#13172=CARTESIAN_POINT('Ctrl Pts',(2.40895095771543,-0.456812739436458,
92.1841007720651));
#13173=CARTESIAN_POINT('Ctrl Pts',(2.39091352198649,-0.537105930317421,
92.1798319465742));
#13174=CARTESIAN_POINT('Ctrl Pts',(2.37307762490926,-0.616501976966011,
92.175610818181));
#13175=CARTESIAN_POINT('Ctrl Pts',(2.35129597153643,-0.694949600364978,
92.1713896897878));
#13176=CARTESIAN_POINT('Ctrl Pts',(2.3257058896982,-0.772037799996274,92.1671685613946));
#13177=CARTESIAN_POINT('Ctrl Pts',(2.29968207100601,-0.850432599324957,
92.1628758873549));
#13178=CARTESIAN_POINT('Ctrl Pts',(2.26971970688244,-0.927420995837426,
92.1585832133151));
#13179=CARTESIAN_POINT('Ctrl Pts',(2.23601355909546,-1.00259344379527,92.1542905392754));
#13180=CARTESIAN_POINT('Ctrl Pts',(2.20230741130847,-1.07776589175312,92.1499978652357));
#13181=CARTESIAN_POINT('Ctrl Pts',(2.16485776593381,-1.1511219773395,92.145705191196));
#13182=CARTESIAN_POINT('Ctrl Pts',(2.12390632801813,-1.2222815386827,92.1414125171563));
#13183=CARTESIAN_POINT('Ctrl Pts',(2.08355048458691,-1.29240616097591,92.1371822754293));
#13184=CARTESIAN_POINT('Ctrl Pts',(2.03964187030215,-1.3606622373627,92.1329520337024));
#13185=CARTESIAN_POINT('Ctrl Pts',(1.99237848348988,-1.42666682463936,92.1287217919755));
#13186=CARTESIAN_POINT('Ctrl Pts',(1.94518312073995,-1.49257641448858,92.1244976386448));
#13187=CARTESIAN_POINT('Ctrl Pts',(1.89464284330798,-1.55624057592302,92.1202734853141));
#13188=CARTESIAN_POINT('Ctrl Pts',(1.8410008124124,-1.61730215442164,92.1160493319835));
#13189=CARTESIAN_POINT('Ctrl Pts',(1.7870816445896,-1.67867920230041,92.1118033549288));
#13190=CARTESIAN_POINT('Ctrl Pts',(1.73002881512644,-1.73742628257337,92.1075573778742));
#13191=CARTESIAN_POINT('Ctrl Pts',(1.67013261929227,-1.79321144430208,92.1033114008196));
#13192=CARTESIAN_POINT('Ctrl Pts',(1.61065213296009,-1.8486094291579,92.0990948929655));
#13193=CARTESIAN_POINT('Ctrl Pts',(1.54836796895763,-1.90108615847223,92.0948783851115));
#13194=CARTESIAN_POINT('Ctrl Pts',(1.48360256763824,-1.95035219160469,92.0906618772574));
#13195=CARTESIAN_POINT('Ctrl Pts',(1.41885871729723,-1.9996018312432,92.0864467724652));
#13196=CARTESIAN_POINT('Ctrl Pts',(1.35163563914798,-2.04564261487001,92.0822316676731));
#13197=CARTESIAN_POINT('Ctrl Pts',(1.28228841405349,-2.0882257237148,92.078016562881));
#13198=CARTESIAN_POINT('Ctrl Pts',(1.2129429912952,-2.13080772582346,92.0738015676395));
#13199=CARTESIAN_POINT('Ctrl Pts',(1.14147392832452,-2.16993198930972,92.0695865723981));
#13200=CARTESIAN_POINT('Ctrl Pts',(1.06826357846448,-2.2053941092073,92.0653715771566));
#13201=CARTESIAN_POINT('Ctrl Pts',(0.994118555750534,-2.24130897220573,
92.0611027692829));
#13202=CARTESIAN_POINT('Ctrl Pts',(0.918187900633963,-2.27346728952869,
92.0568339614093));
#13203=CARTESIAN_POINT('Ctrl Pts',(0.840890848952885,-2.30170650391124,
92.0525651535356));
#13204=CARTESIAN_POINT('Ctrl Pts',(0.7644568937653,-2.32963040009752,92.0483440110389));
#13205=CARTESIAN_POINT('Ctrl Pts',(0.686687372585542,-2.35372219881254,
92.0441228685422));
#13206=CARTESIAN_POINT('Ctrl Pts',(0.608002283014224,-2.37387520182707,
92.0399017260455));
#13207=CARTESIAN_POINT('Ctrl Pts',(0.527984418799767,-2.39436955809603,
92.0356090854833));
#13208=CARTESIAN_POINT('Ctrl Pts',(0.447020175299165,-2.41079034997452,
92.0313164449212));
#13209=CARTESIAN_POINT('Ctrl Pts',(0.365559365136432,-2.42307998228722,
92.027023804359));
#13210=CARTESIAN_POINT('Ctrl Pts',(0.284098554973698,-2.43536961459993,
92.0227311637969));
#13211=CARTESIAN_POINT('Ctrl Pts',(0.202141680907314,-2.4435281042525,92.0184385232347));
#13212=CARTESIAN_POINT('Ctrl Pts',(0.120139218826632,-2.44755323090219,
92.0141458826726));
#13213=CARTESIAN_POINT('Ctrl Pts',(0.039328630761398,-2.45151985389551,
92.0099156339779));
#13214=CARTESIAN_POINT('Ctrl Pts',(-0.0418309954404525,-2.45148748266241,
92.0056853852831));
#13215=CARTESIAN_POINT('Ctrl Pts',(-0.122910461706396,-2.44741563049743,
92.0014551365884));
#13216=CARTESIAN_POINT('Ctrl Pts',(-0.203873237726811,-2.44334963857611,
91.997230976103));
#13217=CARTESIAN_POINT('Ctrl Pts',(-0.284755622299825,-2.43525573499196,
91.9930068156175));
#13218=CARTESIAN_POINT('Ctrl Pts',(-0.365125693053675,-2.42314536878663,
91.9887826551321));
#13219=CARTESIAN_POINT('Ctrl Pts',(-0.44591081842863,-2.41097246109775,
91.9845366798428));
#13220=CARTESIAN_POINT('Ctrl Pts',(-0.526177847492383,-2.3947414593674,
91.9802907045535));
#13221=CARTESIAN_POINT('Ctrl Pts',(-0.605490578364516,-2.37451708974937,
91.9760447292642));
#13222=CARTESIAN_POINT('Ctrl Pts',(-0.684253013112445,-2.35443304302896,
91.9718282138576));
#13223=CARTESIAN_POINT('Ctrl Pts',(-0.76207389349487,-2.33041098391699,
91.9676116984509));
#13224=CARTESIAN_POINT('Ctrl Pts',(-0.838535395610174,-2.30256566471163,
91.9633951830443));
#13225=CARTESIAN_POINT('Ctrl Pts',(-0.914971457248737,-2.2747296102758,
91.959180070568));
#13226=CARTESIAN_POINT('Ctrl Pts',(-0.990048602041579,-2.2430729809124,
91.9549649580918));
#13227=CARTESIAN_POINT('Ctrl Pts',(-1.06336553039165,-2.20775995044183,
91.9507498456155));
#13228=CARTESIAN_POINT('Ctrl Pts',(-1.1366805553295,-2.17244783674798,91.9465348425695));
#13229=CARTESIAN_POINT('Ctrl Pts',(-1.20823503604193,-2.13347971349964,
91.9423198395236));
#13230=CARTESIAN_POINT('Ctrl Pts',(-1.27765028948547,-2.09106671050392,
91.9381048364776));
#13231=CARTESIAN_POINT('Ctrl Pts',(-1.34795148806702,-2.04811239141515,
91.9338360374536));
#13232=CARTESIAN_POINT('Ctrl Pts',(-1.41605803946471,-2.00162487400772,
91.9295672384295));
#13233=CARTESIAN_POINT('Ctrl Pts',(-1.48160652672157,-1.95186893770459,
91.9252984394055));
#13234=CARTESIAN_POINT('Ctrl Pts',(-1.54642335906288,-1.90266837921256,
91.921077288892));
#13235=CARTESIAN_POINT('Ctrl Pts',(-1.60873862907606,-1.850272353781,91.9168561383785));
#13236=CARTESIAN_POINT('Ctrl Pts',(-1.66823549380769,-1.79497648653129,
91.9126349878651));
#13237=CARTESIAN_POINT('Ctrl Pts',(-1.72873976291179,-1.7387443464427,91.9083423645857));
#13238=CARTESIAN_POINT('Ctrl Pts',(-1.78632894863795,-1.6795136139708,91.9040497413064));
#13239=CARTESIAN_POINT('Ctrl Pts',(-1.84071139952382,-1.61763153828771,
91.899757118027));
#13240=CARTESIAN_POINT('Ctrl Pts',(-1.8950938504097,-1.55574946260462,91.8954644947477));
#13241=CARTESIAN_POINT('Ctrl Pts',(-1.94626930885375,-1.49121647577073,
91.8911718714683));
#13242=CARTESIAN_POINT('Ctrl Pts',(-1.99399234651966,-1.42441032431705,
91.886879248189));
#13243=CARTESIAN_POINT('Ctrl Pts',(-2.04145829217768,-1.35796406880582,
91.8826097499912));
#13244=CARTESIAN_POINT('Ctrl Pts',(-2.08568702951202,-1.28902010786886,
91.8783402517934));
#13245=CARTESIAN_POINT('Ctrl Pts',(-2.12640843309736,-1.21792340713709,
91.8740707535956));
#13246=CARTESIAN_POINT('Ctrl Pts',(-2.16706882103362,-1.14693323542842,
91.8698076526773));
#13247=CARTESIAN_POINT('Ctrl Pts',(-2.20423209025483,-1.07379712098361,
91.8655445517591));
#13248=CARTESIAN_POINT('Ctrl Pts',(-2.23767023184873,-0.998890476227515,
91.8612814508409));
#13249=CARTESIAN_POINT('Ctrl Pts',(-2.2725614624977,-0.920728685687057,
91.8568330924595));
#13250=CARTESIAN_POINT('Ctrl Pts',(-2.30339612314618,-0.840639372995289,
91.8523847340781));
#13251=CARTESIAN_POINT('Ctrl Pts',(-2.32996742028762,-0.759079752330567,
91.8479363756967));
#13252=CARTESIAN_POINT('Ctrl Pts',(-2.35537480837413,-0.681092707761914,
91.8436828698501));
#13253=CARTESIAN_POINT('Ctrl Pts',(-2.37688432399493,-0.601761941124336,
91.8394293640035));
#13254=CARTESIAN_POINT('Ctrl Pts',(-2.39436418876273,-0.521507796270208,
91.8351758581569));
#13255=CARTESIAN_POINT('Ctrl Pts',(-2.41183415697063,-0.441299088835756,
91.830924760514));
#13256=CARTESIAN_POINT('Ctrl Pts',(-2.42527891340726,-0.360168485131073,
91.826673662871));
#13257=CARTESIAN_POINT('Ctrl Pts',(-2.43461712473377,-0.278549288193404,
91.8224225652281));
#13258=CARTESIAN_POINT('Ctrl Pts',(-2.44395324096001,-0.196948403156809,
91.818172421352));
#13259=CARTESIAN_POINT('Ctrl Pts',(-2.44918459184153,-0.11485959340377,
91.8139222774759));
#13260=CARTESIAN_POINT('Ctrl Pts',(-2.45028150676759,-0.032722890959208,
91.8096721335998));
#13261=CARTESIAN_POINT('Ctrl Pts',(-2.45043386381017,-0.0213144355044843,
91.8090818058213));
#13262=CARTESIAN_POINT('Ctrl Pts',(-2.45050654103334,-0.0099050608674649,
91.8084914780428));
#13263=CARTESIAN_POINT('Ctrl Pts',(-2.45049953842705,0.00150405079498821,
91.8079011502643));
#13264=CARTESIAN_POINT('Ctrl Pts',(-2.45049953842671,0.00150405135356907,
91.8079011502354));
#13265=CARTESIAN_POINT('Ctrl Pts',(-2.45044342734625,0.0929239197229016,
91.8031709232553));
#13266=CARTESIAN_POINT('Ctrl Pts',(-2.44526737934698,0.184152685350111,
91.7984406962751));
#13267=CARTESIAN_POINT('Ctrl Pts',(-2.43505973922788,0.274653083710055,
91.793710469295));
#13268=CARTESIAN_POINT('Ctrl Pts',(-2.42480793863696,0.365545006481651,
91.7889597783239));
#13269=CARTESIAN_POINT('Ctrl Pts',(-2.40948104789849,0.455702014559125,
91.7842090873527));
#13270=CARTESIAN_POINT('Ctrl Pts',(-2.38921823372468,0.544597540976377,
91.7794583963816));
#13271=CARTESIAN_POINT('Ctrl Pts',(-2.3688459255397,0.633973431457541,91.7746820341387));
#13272=CARTESIAN_POINT('Ctrl Pts',(-2.34348433095867,0.722073944947803,
91.7699056718958));
#13273=CARTESIAN_POINT('Ctrl Pts',(-2.31332305585638,0.808385235666317,
91.7651293096528));
#13274=CARTESIAN_POINT('Ctrl Pts',(-2.30171097008438,0.841615067877205,
91.7632904110037));
#13275=CARTESIAN_POINT('Ctrl Pts',(-2.28938794702891,0.874579933837566,
91.7614515123545));
#13276=CARTESIAN_POINT('Ctrl Pts',(-2.27636663418872,0.907251451777459,
91.7596126137053));
#13277=CARTESIAN_POINT('Ctrl Pts',(-2.24641162225297,0.982410978459588,
91.7553823005517));
#13278=CARTESIAN_POINT('Ctrl Pts',(-2.21267377992271,1.05622707003952,91.7511519873981));
#13279=CARTESIAN_POINT('Ctrl Pts',(-2.17529454185354,1.12829247368853,91.7469216742446));
#13280=CARTESIAN_POINT('Ctrl Pts',(-2.13796910395373,1.20025415315478,91.742697449807));
#13281=CARTESIAN_POINT('Ctrl Pts',(-2.09701289166299,1.27046973965804,91.7384732253694));
#13282=CARTESIAN_POINT('Ctrl Pts',(-2.05261571545128,1.33855107287037,91.7342490009318));
#13283=CARTESIAN_POINT('Ctrl Pts',(-2.00799010351738,1.40698270332787,91.7300030416939));
#13284=CARTESIAN_POINT('Ctrl Pts',(-1.95988818922199,1.47325761065391,91.7257570824559));
#13285=CARTESIAN_POINT('Ctrl Pts',(-1.90855001117378,1.53700588965968,91.721511123218));
#13286=CARTESIAN_POINT('Ctrl Pts',(-1.85756708751065,1.6003130377855,91.7172945455378));
#13287=CARTESIAN_POINT('Ctrl Pts',(-1.80339284340111,1.66112804808693,91.7130779678575));
#13288=CARTESIAN_POINT('Ctrl Pts',(-1.74630520492977,1.71911848958563,91.7088613901772));
#13289=CARTESIAN_POINT('Ctrl Pts',(-1.68923657085335,1.77708962614755,91.7046462161897));
#13290=CARTESIAN_POINT('Ctrl Pts',(-1.62925679445037,1.83223772992246,91.7004310422023));
#13291=CARTESIAN_POINT('Ctrl Pts',(-1.56668189637093,1.88426592751224,91.6962158682148));
#13292=CARTESIAN_POINT('Ctrl Pts',(-1.50410863527495,1.93629276402433,91.6920008044979));
#13293=CARTESIAN_POINT('Ctrl Pts',(-1.43894074584348,1.98519956004807,91.687785740781));
#13294=CARTESIAN_POINT('Ctrl Pts',(-1.37152757036941,2.03072951761592,91.6835706770642));
#13295=CARTESIAN_POINT('Ctrl Pts',(-1.30325617171834,2.0768391076452,91.6793019522439));
#13296=CARTESIAN_POINT('Ctrl Pts',(-1.23268230853496,2.11948498222502,91.6750332274237));
#13297=CARTESIAN_POINT('Ctrl Pts',(-1.16019774959019,2.15844653207946,91.6707645026035));
#13298=CARTESIAN_POINT('Ctrl Pts',(-1.08852003537,2.19697439065649,91.6665432940841));
#13299=CARTESIAN_POINT('Ctrl Pts',(-1.01497440321775,2.23189939398055,91.6623220855646));
#13300=CARTESIAN_POINT('Ctrl Pts',(-0.939961375172089,2.26305608927057,
91.6581008770451));
#13301=CARTESIAN_POINT('Ctrl Pts',(-0.863681763782927,2.29473886052793,
91.6538083940745));
#13302=CARTESIAN_POINT('Ctrl Pts',(-0.785885218093811,2.32252472344326,
91.649515911104));
#13303=CARTESIAN_POINT('Ctrl Pts',(-0.707008699244591,2.34629259667086,
91.6452234281334));
#13304=CARTESIAN_POINT('Ctrl Pts',(-0.628132180395372,2.37006046989846,
91.6409309451628));
#13305=CARTESIAN_POINT('Ctrl Pts',(-0.548176188274773,2.38981029854057,
91.6366384621923));
#13306=CARTESIAN_POINT('Ctrl Pts',(-0.467586229601472,2.40547570511262,
91.6323459792217));
#13307=CARTESIAN_POINT('Ctrl Pts',(-0.388163321044419,2.42091425569838,
91.6281156571311));
#13308=CARTESIAN_POINT('Ctrl Pts',(-0.307825265043799,2.43244415440366,
91.6238853350405));
#13309=CARTESIAN_POINT('Ctrl Pts',(-0.226991131958893,2.43996419564141,
91.6196550129499));
#13310=CARTESIAN_POINT('Ctrl Pts',(-0.146273314150721,2.44747341600876,
91.615430778029));
#13311=CARTESIAN_POINT('Ctrl Pts',(-0.0650612961559804,2.45098419550811,
91.6112065431081));
#13312=CARTESIAN_POINT('Ctrl Pts',(0.0162157584592155,2.45044634692898,
91.6069823081872));
#13313=CARTESIAN_POINT('Ctrl Pts',(0.0979107564963627,2.44990573262124,
91.6027363513768));
#13314=CARTESIAN_POINT('Ctrl Pts',(0.179670994974369,2.44527463812407,91.5984903945665));
#13315=CARTESIAN_POINT('Ctrl Pts',(0.261055515603077,2.43655499994833,91.5942444377561));
#13316=CARTESIAN_POINT('Ctrl Pts',(0.341877181482125,2.42789566672647,91.590027845952));
#13317=CARTESIAN_POINT('Ctrl Pts',(0.422327841458038,2.41520421422521,91.5858112541478));
#13318=CARTESIAN_POINT('Ctrl Pts',(0.501977573320803,2.39853471225308,91.5815946623437));
#13319=CARTESIAN_POINT('Ctrl Pts',(0.581600815022473,2.38187075427692,91.5773794729071));
#13320=CARTESIAN_POINT('Ctrl Pts',(0.660423202646158,2.36123146932777,91.5731642834705));
#13321=CARTESIAN_POINT('Ctrl Pts',(0.738024130354673,2.33672219851103,91.5689490940339));
#13322=CARTESIAN_POINT('Ctrl Pts',(0.815623051852268,2.31221356133062,91.5647340135722));
#13323=CARTESIAN_POINT('Ctrl Pts',(0.892000132975834,2.2838352783163,91.5605189331106));
#13324=CARTESIAN_POINT('Ctrl Pts',(0.966750465322902,2.2517423893061,91.5563038526489));
#13325=CARTESIAN_POINT('Ctrl Pts',(1.04245184725185,2.21924118199528,91.5520351436564));
#13326=CARTESIAN_POINT('Ctrl Pts',(1.11648433699277,2.18293035398683,91.5477664346638));
#13327=CARTESIAN_POINT('Ctrl Pts',(1.18845054046122,2.14302019656312,91.5434977256712));
#13328=CARTESIAN_POINT('Ctrl Pts',(1.25961626549693,2.10355395890626,91.539276497431));
#13329=CARTESIAN_POINT('Ctrl Pts',(1.3287610757537,2.06056836668343,91.5350552691908));
#13330=CARTESIAN_POINT('Ctrl Pts',(1.39552923478034,2.01431090074829,91.5308340409505));
#13331=CARTESIAN_POINT('Ctrl Pts',(1.4634239151331,1.96727297264933,91.5265415915818));
#13332=CARTESIAN_POINT('Ctrl Pts',(1.52886060679971,1.91685205044352,91.522249142213));
#13333=CARTESIAN_POINT('Ctrl Pts',(1.59150121153463,1.86335024718484,91.5179566928443));
#13334=CARTESIAN_POINT('Ctrl Pts',(1.65414181626955,1.80984844392616,91.5136642434755));
#13335=CARTESIAN_POINT('Ctrl Pts',(1.7139860176476,1.75326615043448,91.5093717941068));
#13336=CARTESIAN_POINT('Ctrl Pts',(1.77073711415668,1.69394224297881,91.505079344738));
#13337=CARTESIAN_POINT('Ctrl Pts',(1.82665877833745,1.63548537016586,91.5008496306554));
#13338=CARTESIAN_POINT('Ctrl Pts',(1.87978820444791,1.57414593479859,91.4966199165727));
#13339=CARTESIAN_POINT('Ctrl Pts',(1.9298136963886,1.51022162189229,91.49239020249));
#13340=CARTESIAN_POINT('Ctrl Pts',(1.97976716813481,1.4463893388945,91.4881665777993));
#13341=CARTESIAN_POINT('Ctrl Pts',(2.02662529621523,1.37997993239357,91.4839429531086));
#13342=CARTESIAN_POINT('Ctrl Pts',(2.0701138382201,1.31132717001122,91.479719328418));
#13343=CARTESIAN_POINT('Ctrl Pts',(2.11383389079293,1.24230893573033,91.4754732193278));
#13344=CARTESIAN_POINT('Ctrl Pts',(2.15414804167968,1.1710237309849,91.4712271102377));
#13345=CARTESIAN_POINT('Ctrl Pts',(2.19081938999678,1.09784363659591,91.4669810011475));
#13346=CARTESIAN_POINT('Ctrl Pts',(2.22723053503344,1.02518279501591,91.4627650205246));
#13347=CARTESIAN_POINT('Ctrl Pts',(2.26005019472744,0.950654289210813,91.4585490399016));
#13348=CARTESIAN_POINT('Ctrl Pts',(2.28909142064245,0.874648911244454,91.4543330592786));
#13349=CARTESIAN_POINT('Ctrl Pts',(2.31812299334254,0.798668797233951,91.4501184800347));
#13350=CARTESIAN_POINT('Ctrl Pts',(2.34337846034257,0.721213220216567,91.4459039007909));
#13351=CARTESIAN_POINT('Ctrl Pts',(2.36471904008228,0.642692859359994,91.441689321547));
#13352=CARTESIAN_POINT('Ctrl Pts',(2.38605907715239,0.564174495197691,91.4374748494757));
#13353=CARTESIAN_POINT('Ctrl Pts',(2.40348430388506,0.484591850334117,91.4332603774044));
#13354=CARTESIAN_POINT('Ctrl Pts',(2.4169062337319,0.404369271023259,91.429045905333));
#13355=CARTESIAN_POINT('Ctrl Pts',(2.43050319871624,0.323100510547673,91.4247764724098));
#13356=CARTESIAN_POINT('Ctrl Pts',(2.43999159786059,0.241175483715299,91.4205070394866));
#13357=CARTESIAN_POINT('Ctrl Pts',(2.44533346016253,0.159042505669277,91.4162376065634));
#13358=CARTESIAN_POINT('Ctrl Pts',(2.45061426143794,0.0778483619974146,
91.4120169760881));
#13359=CARTESIAN_POINT('Ctrl Pts',(2.45184289289478,-0.00354853112366331,
91.4077963456128));
#13360=CARTESIAN_POINT('Ctrl Pts',(2.44903523501604,-0.084715214984909,
91.4035757151376));
#13361=CARTESIAN_POINT('Ctrl Pts',(2.44617888041592,-0.167289674137563,
91.3992818809904));
#13362=CARTESIAN_POINT('Ctrl Pts',(2.43914493860046,-0.249625360627648,
91.3949880468432));
#13363=CARTESIAN_POINT('Ctrl Pts',(2.42800489733757,-0.331274008193782,
91.390694212696));
#13364=CARTESIAN_POINT('Ctrl Pts',(2.41686485607468,-0.412922655759917,
91.3864003785488));
#13365=CARTESIAN_POINT('Ctrl Pts',(2.40161887361233,-0.493883785700159,
91.3821065444016));
#13366=CARTESIAN_POINT('Ctrl Pts',(2.38239184086457,-0.573724120620635,
91.3778127102544));
#13367=CARTESIAN_POINT('Ctrl Pts',(2.36344610079998,-0.65239638648284,91.3735816951674));
#13368=CARTESIAN_POINT('Ctrl Pts',(2.34056358204653,-0.730277318983722,
91.3693506800805));
#13369=CARTESIAN_POINT('Ctrl Pts',(2.3138263385451,-0.806943569932234,91.3651196649935));
#13370=CARTESIAN_POINT('Ctrl Pts',(2.28712758553652,-0.883499453415827,
91.3608947408058));
#13371=CARTESIAN_POINT('Ctrl Pts',(2.25658528062193,-0.958843692905802,
91.3566698166181));
#13372=CARTESIAN_POINT('Ctrl Pts',(2.2223320783732,-1.03256495361476,91.3524448924303));
#13373=CARTESIAN_POINT('Ctrl Pts',(2.18790975680346,-1.10665020042534,91.3481991084029));
#13374=CARTESIAN_POINT('Ctrl Pts',(2.1497399014367,-1.17909593443739,91.3439533243754));
#13375=CARTESIAN_POINT('Ctrl Pts',(2.10800736336254,-1.24950198319543,91.3397075403479));
#13376=CARTESIAN_POINT('Ctrl Pts',(2.06655512274216,-1.31943514827307,91.3354902732165));
#13377=CARTESIAN_POINT('Ctrl Pts',(2.0215881497874,-1.38735553784634,91.3312730060851));
#13378=CARTESIAN_POINT('Ctrl Pts',(1.97333424201925,-1.45289442812419,91.3270557389538));
#13379=CARTESIAN_POINT('Ctrl Pts',(1.92509645660628,-1.51841142087464,91.3228398808747));
#13380=CARTESIAN_POINT('Ctrl Pts',(1.873574192722,-1.58154812028761,91.3186240227956));
#13381=CARTESIAN_POINT('Ctrl Pts',(1.81903801958421,-1.64196557007361,91.3144081647165));
#13382=CARTESIAN_POINT('Ctrl Pts',(1.76450335372716,-1.70238135003107,91.310192423156));
#13383=CARTESIAN_POINT('Ctrl Pts',(1.70695525659306,-1.76007768531773,91.3059766815956));
#13384=CARTESIAN_POINT('Ctrl Pts',(1.64670299005559,-1.81475053727557,91.3017609400351));
#13385=CARTESIAN_POINT('Ctrl Pts',(1.58570518757162,-1.87009988787445,91.2974930346798));
#13386=CARTESIAN_POINT('Ctrl Pts',(1.5219361831133,-1.92235007568659,91.2932251293244));
#13387=CARTESIAN_POINT('Ctrl Pts',(1.45575201339009,-1.97122711160097,91.288957223969));
#13388=CARTESIAN_POINT('Ctrl Pts',(1.39028182267432,-2.01957687373168,91.2847353597568));
#13389=CARTESIAN_POINT('Ctrl Pts',(1.32244875105379,-2.06462570294899,91.2805134955446));
#13390=CARTESIAN_POINT('Ctrl Pts',(1.25262573029115,-2.10615266061427,91.2762916313323));
#13391=CARTESIAN_POINT('Ctrl Pts',(1.18166053694928,-2.14835892077643,91.2720007054054));
#13392=CARTESIAN_POINT('Ctrl Pts',(1.1086401497209,-2.18692681906497,91.2677097794785));
#13393=CARTESIAN_POINT('Ctrl Pts',(1.03397925625825,-2.22167440180321,91.2634188535516));
#13394=CARTESIAN_POINT('Ctrl Pts',(0.959318362795604,-2.25642198454144,
91.2591279276247));
#13395=CARTESIAN_POINT('Ctrl Pts',(0.883017448585974,-2.28734912631146,
91.2548370016978));
#13396=CARTESIAN_POINT('Ctrl Pts',(0.805507440379614,-2.31432668685583,
91.2505460757709));
#13397=CARTESIAN_POINT('Ctrl Pts',(0.72908587596123,-2.34092541170054,91.2463154056971));
#13398=CARTESIAN_POINT('Ctrl Pts',(0.651201682846937,-2.36378481128142,
91.2420847356233));
#13399=CARTESIAN_POINT('Ctrl Pts',(0.572255344369428,-2.38274507046822,
91.2378540655495));
#13400=CARTESIAN_POINT('Ctrl Pts',(0.493422431226035,-2.40167808869902,
91.2336294738471));
#13401=CARTESIAN_POINT('Ctrl Pts',(0.413530851853179,-2.4167229848221,91.2294048821447));
#13402=CARTESIAN_POINT('Ctrl Pts',(0.332998335664766,-2.42776900846116,
91.2251802904423));
#13403=CARTESIAN_POINT('Ctrl Pts',(0.252060220197776,-2.43887066502256,
91.2209344217275));
#13404=CARTESIAN_POINT('Ctrl Pts',(0.170475142269413,-2.44593289574067,
91.2166885530127));
#13405=CARTESIAN_POINT('Ctrl Pts',(0.0886797803512509,-2.4488948827087,
91.2124426842979));
#13406=CARTESIAN_POINT('Ctrl Pts',(0.00744119817062207,-2.45183670747819,
91.2082257171445));
#13407=CARTESIAN_POINT('Ctrl Pts',(-0.0740043433872743,-2.45073391836519,
91.204008749991));
#13408=CARTESIAN_POINT('Ctrl Pts',(-0.15522353275677,-2.44557884863247,
91.1997917828375));
#13409=CARTESIAN_POINT('Ctrl Pts',(-0.236415829701173,-2.44042548579103,
91.1955762119609));
#13410=CARTESIAN_POINT('Ctrl Pts',(-0.317381459527211,-2.43122253623513,
91.1913606410842));
#13411=CARTESIAN_POINT('Ctrl Pts',(-0.397689036467322,-2.41801440861582,
91.1871450702076));
#13412=CARTESIAN_POINT('Ctrl Pts',(-0.477994642849909,-2.40480660509264,
91.1829296027711));
#13413=CARTESIAN_POINT('Ctrl Pts',(-0.557641769726736,-2.38759389544172,
91.1787141353346));
#13414=CARTESIAN_POINT('Ctrl Pts',(-0.636207495698802,-2.36647211528398,
91.1744986678981));
#13415=CARTESIAN_POINT('Ctrl Pts',(-0.715757308046921,-2.3450857712107,
91.1702303990138));
#13416=CARTESIAN_POINT('Ctrl Pts',(-0.794197964003815,-2.31969185603068,
91.1659621301296));
#13417=CARTESIAN_POINT('Ctrl Pts',(-0.871106359442046,-2.29044187015074,
91.1616938612453));
#13418=CARTESIAN_POINT('Ctrl Pts',(-0.94717428986041,-2.26151153194806,
91.1574722365626));
#13419=CARTESIAN_POINT('Ctrl Pts',(-1.02174288005474,-2.22880923791292,
91.1532506118798));
#13420=CARTESIAN_POINT('Ctrl Pts',(-1.09442471470152,-2.19252931425112,
91.1490289871971));
#13421=CARTESIAN_POINT('Ctrl Pts',(-1.16831112805704,-2.15564811210192,
91.1447373962121));
#13422=CARTESIAN_POINT('Ctrl Pts',(-1.2402472411976,-2.11506986323518,91.1404458052271));
#13423=CARTESIAN_POINT('Ctrl Pts',(-1.30985564224241,-2.07104525457213,
91.1361542142421));
#13424=CARTESIAN_POINT('Ctrl Pts',(-1.37946404328721,-2.02702064590908,
91.1318626232571));
#13425=CARTESIAN_POINT('Ctrl Pts',(-1.44674436398691,-1.97955001863733,
91.1275710322721));
#13426=CARTESIAN_POINT('Ctrl Pts',(-1.51135488719631,-1.92892629588272,
91.1232794412872));
#13427=CARTESIAN_POINT('Ctrl Pts',(-1.57421989033043,-1.87967022533033,
91.1191037920691));
#13428=CARTESIAN_POINT('Ctrl Pts',(-1.63480814000601,-1.82723268945927,
91.1149281428509));
#13429=CARTESIAN_POINT('Ctrl Pts',(-1.69277337230466,-1.77185455385489,
91.1107524936328));
#13430=CARTESIAN_POINT('Ctrl Pts',(-1.75226314360995,-1.71501992227015,
91.1064670209937));
#13431=CARTESIAN_POINT('Ctrl Pts',(-1.80898952372527,-1.65508806093937,
91.1021815483546));
#13432=CARTESIAN_POINT('Ctrl Pts',(-1.86261122648677,-1.59236605997661,
91.0978960757154));
#13433=CARTESIAN_POINT('Ctrl Pts',(-1.91472175221152,-1.53141170238721,
91.0937313770822));
#13434=CARTESIAN_POINT('Ctrl Pts',(-1.9638999286895,-1.46782276849848,91.0895666784489));
#13435=CARTESIAN_POINT('Ctrl Pts',(-2.00986862981078,-1.40191952012323,
91.0854019798157));
#13436=CARTESIAN_POINT('Ctrl Pts',(-2.05580954463358,-1.33605610770776,
91.0812397985813));
#13437=CARTESIAN_POINT('Ctrl Pts',(-2.09854455984026,-1.26788154730045,
91.077077617347));
#13438=CARTESIAN_POINT('Ctrl Pts',(-2.13783760634789,-1.19774814501411,
91.0729154361127));
#13439=CARTESIAN_POINT('Ctrl Pts',(-2.17711968999981,-1.12763431011787,
91.0687544161371));
#13440=CARTESIAN_POINT('Ctrl Pts',(-2.2129614780551,-1.05556313547689,91.0645933961615));
#13441=CARTESIAN_POINT('Ctrl Pts',(-2.24517177871854,-0.981913404555533,
91.0604323761858));
#13442=CARTESIAN_POINT('Ctrl Pts',(-2.27905863398711,-0.904430185805758,
91.0560547740282));
#13443=CARTESIAN_POINT('Ctrl Pts',(-2.30892543008363,-0.825200132907421,
91.0516771718705));
#13444=CARTESIAN_POINT('Ctrl Pts',(-2.3346068648025,-0.744688550212115,
91.0472995697128));
#13445=CARTESIAN_POINT('Ctrl Pts',(-2.35904185950792,-0.668084570784174,
91.0431344330405));
#13446=CARTESIAN_POINT('Ctrl Pts',(-2.37968821884651,-0.590321058987381,
91.0389692963682));
#13447=CARTESIAN_POINT('Ctrl Pts',(-2.3964553324695,-0.511812553068496,
91.0348041596959));
#13448=CARTESIAN_POINT('Ctrl Pts',(-2.41323215421009,-0.433258590917541,
91.0306366114197));
#13449=CARTESIAN_POINT('Ctrl Pts',(-2.42612518745693,-0.353959248289263,
91.0264690631435));
#13450=CARTESIAN_POINT('Ctrl Pts',(-2.43509548030834,-0.274336019840476,
91.0223015148672));
#13451=CARTESIAN_POINT('Ctrl Pts',(-2.44407863856889,-0.194598593847754,
91.0181279893933));
#13452=CARTESIAN_POINT('Ctrl Pts',(-2.44912781095319,-0.114536831426669,
91.0139544639194));
#13453=CARTESIAN_POINT('Ctrl Pts',(-2.45025609890484,-0.0345731077519822,
91.0097809384455));
#13454=CARTESIAN_POINT('Ctrl Pts',(-2.45042549544473,-0.0225676812227585,
91.0091543423949));
#13455=CARTESIAN_POINT('Ctrl Pts',(-2.4505066074065,-0.0105644550898491,
91.0085277463443));
#13456=CARTESIAN_POINT('Ctrl Pts',(-2.45049957974585,0.00143515344103467,
91.0079011502937));
#13457=CARTESIAN_POINT('Origin',(0.,0.,89.2710285354474));
#13458=CARTESIAN_POINT('',(-0.766343857929312,1.84166898597821,96.7230113585667));
#13459=CARTESIAN_POINT('Ctrl Pts',(-0.766343857929312,1.84166898597821,
96.7230113585667));
#13460=CARTESIAN_POINT('Ctrl Pts',(-0.689464277964599,1.87365963921433,
96.7173743733537));
#13461=CARTESIAN_POINT('Ctrl Pts',(-0.610651735565635,1.90080711524305,
96.7115687222733));
#13462=CARTESIAN_POINT('Ctrl Pts',(-0.448970235501531,1.94540048021294,
96.6998596526854));
#13463=CARTESIAN_POINT('Ctrl Pts',(-0.366223654018037,1.96266124007479,
96.6939689168249));
#13464=CARTESIAN_POINT('Ctrl Pts',(-0.234099561889875,1.9815721640297,96.6848374860735));
#13465=CARTESIAN_POINT('Ctrl Pts',(-0.185328462711493,1.9867271620772,96.6815235471886));
#13466=CARTESIAN_POINT('Ctrl Pts',(-0.0967024770106042,1.99280219464184,
96.6756112671446));
#13467=CARTESIAN_POINT('Ctrl Pts',(-0.0569165008103657,1.99433518783667,
96.6729967891622));
#13468=CARTESIAN_POINT('Ctrl Pts',(0.00799370580248113,1.99489193867091,
96.668793257551));
#13469=CARTESIAN_POINT('Ctrl Pts',(0.0330989629791975,1.99463337479979,
96.6671824926306));
#13470=CARTESIAN_POINT('Ctrl Pts',(0.0822279360528475,1.99319950556032,
96.6640576343969));
#13471=CARTESIAN_POINT('Ctrl Pts',(0.106248385720628,1.99206351897154,96.662542591882));
#13472=CARTESIAN_POINT('Ctrl Pts',(0.165381681276155,1.9881942698625,96.6588408983002));
#13473=CARTESIAN_POINT('Ctrl Pts',(0.200454519605292,1.98496492944509,96.6566698667405));
#13474=CARTESIAN_POINT('Ctrl Pts',(0.377037944035307,1.96397744647056,96.6458320796582));
#13475=CARTESIAN_POINT('Ctrl Pts',(0.516437588427071,1.93200954830316,96.6376152951654));
#13476=CARTESIAN_POINT('Ctrl Pts',(0.73321504568797,1.85713327765633,96.6242415475676));
#13477=CARTESIAN_POINT('Ctrl Pts',(0.813244187714863,1.82350742849959,96.6191518491671));
#13478=CARTESIAN_POINT('Ctrl Pts',(0.913286062133564,1.7735744696473,96.6122934593206));
#13479=CARTESIAN_POINT('Ctrl Pts',(0.935533847184037,1.76194044124667,96.6107347866518));
#13480=CARTESIAN_POINT('Ctrl Pts',(0.970385576848291,1.74286927630774,96.6082302127771));
#13481=CARTESIAN_POINT('Ctrl Pts',(0.983138112306051,1.73570760857862,96.607300141527));
#13482=CARTESIAN_POINT('Ctrl Pts',(1.0083046757042,1.72120805631167,96.6054351165978));
#13483=CARTESIAN_POINT('Ctrl Pts',(1.02072003279402,1.7138745770352,96.6045003893618));
#13484=CARTESIAN_POINT('Ctrl Pts',(1.05402456718766,1.69371210776809,96.6019553523719));
#13485=CARTESIAN_POINT('Ctrl Pts',(1.0747580272508,1.68063188882308,96.600330465321));
#13486=CARTESIAN_POINT('Ctrl Pts',(1.20926713361166,1.5922665914891,96.589546171725));
#13487=CARTESIAN_POINT('Ctrl Pts',(1.31529856772277,1.50586404027768,96.5799136498756));
#13488=CARTESIAN_POINT('Ctrl Pts',(1.47343045748685,1.34746785145387,96.5643818630868));
#13489=CARTESIAN_POINT('Ctrl Pts',(1.53105586631441,1.28161534654556,96.5583944213804));
#13490=CARTESIAN_POINT('Ctrl Pts',(1.60907128548697,1.17965878703582,96.5498377271338));
#13491=CARTESIAN_POINT('Ctrl Pts',(1.6329555797574,1.14636893495378,96.5471439367675));
#13492=CARTESIAN_POINT('Ctrl Pts',(1.66986986589846,1.09142056370508,96.5428534537705));
#13493=CARTESIAN_POINT('Ctrl Pts',(1.68354223555702,1.07021019138013,96.5412330625295));
#13494=CARTESIAN_POINT('Ctrl Pts',(1.70930821101557,1.02852233776606,96.5381148717711));
#13495=CARTESIAN_POINT('Ctrl Pts',(1.72144527078454,1.00807689089324,96.5366156556503));
#13496=CARTESIAN_POINT('Ctrl Pts',(1.75006562929069,0.957839620176097,96.5330010766669));
#13497=CARTESIAN_POINT('Ctrl Pts',(1.76615765463162,0.927832849446242,96.5308998959989));
#13498=CARTESIAN_POINT('Ctrl Pts',(1.85220642307039,0.757018273381394,96.5192293313663));
#13499=CARTESIAN_POINT('Ctrl Pts',(1.90609084977174,0.608742003608438,96.5102409505371));
#13500=CARTESIAN_POINT('Ctrl Pts',(1.96227363326658,0.369297195931189,96.4959201478483));
#13501=CARTESIAN_POINT('Ctrl Pts',(1.97675274988674,0.281679466556155,96.4907039538973));
#13502=CARTESIAN_POINT('Ctrl Pts',(1.98740272489393,0.172351968173701,96.4839186172782));
#13503=CARTESIAN_POINT('Ctrl Pts',(1.98911815303444,0.151273526339116,96.4825976539646));
#13504=CARTESIAN_POINT('Ctrl Pts',(1.99139253939414,0.116495439187971,96.4803913378564));
#13505=CARTESIAN_POINT('Ctrl Pts',(1.99214598592943,0.102809500557032,96.4795162487026));
#13506=CARTESIAN_POINT('Ctrl Pts',(1.99343313839598,0.0740272878003802,
96.4776596416079));
#13507=CARTESIAN_POINT('Ctrl Pts',(1.99393651315791,0.0589309994243547,
96.4766766780363));
#13508=CARTESIAN_POINT('Ctrl Pts',(1.99489655819254,0.0152499198006821,
96.4738087792047));
#13509=CARTESIAN_POINT('Ctrl Pts',(1.99491019654391,-0.0133397280134689,
96.4719024017577));
#13510=CARTESIAN_POINT('Ctrl Pts',(1.99140676794874,-0.18002043663416,96.4606540561745));
#13511=CARTESIAN_POINT('Ctrl Pts',(1.97416743805883,-0.31744240407428,96.4508742304591));
#13512=CARTESIAN_POINT('Ctrl Pts',(1.92798282304451,-0.515971591201918,
96.4367486009863));
#13513=CARTESIAN_POINT('Ctrl Pts',(1.90994196548938,-0.579195480206896,
96.4322449262548));
#13514=CARTESIAN_POINT('Ctrl Pts',(1.87323154609103,-0.687298229869412,
96.4245699100349));
#13515=CARTESIAN_POINT('Ctrl Pts',(1.85598376796744,-0.732598253819112,
96.4213613473285));
#13516=CARTESIAN_POINT('Ctrl Pts',(1.82681215960695,-0.801549939826431,
96.4164883691608));
#13517=CARTESIAN_POINT('Ctrl Pts',(1.81604006013559,-0.82566554055961,96.4147860418146));
#13518=CARTESIAN_POINT('Ctrl Pts',(1.79487217493784,-0.870634200771682,
96.4116134678188));
#13519=CARTESIAN_POINT('Ctrl Pts',(1.78458390273124,-0.891532616084326,
96.4101397996846));
#13520=CARTESIAN_POINT('Ctrl Pts',(1.76032033520567,-0.938714923774441,
96.4068117771997));
#13521=CARTESIAN_POINT('Ctrl Pts',(1.74611786655083,-0.96487612385816,96.4049658502308));
#13522=CARTESIAN_POINT('Ctrl Pts',(1.69773577140828,-1.04942712988325,96.3989870068363));
#13523=CARTESIAN_POINT('Ctrl Pts',(1.66116982482082,-1.10639964075085,96.3949393610025));
#13524=CARTESIAN_POINT('Ctrl Pts',(1.55070492502598,-1.26065148707727,96.3837628430489));
#13525=CARTESIAN_POINT('Ctrl Pts',(1.47067649678868,-1.35315842930146,96.376810080906));
#13526=CARTESIAN_POINT('Ctrl Pts',(1.34916027595902,-1.4700200272377,96.3669234589614));
#13527=CARTESIAN_POINT('Ctrl Pts',(1.31450841706711,-1.50108609112926,96.3641660440778));
#13528=CARTESIAN_POINT('Ctrl Pts',(1.25412309290372,-1.55152732915222,96.3594009189411));
#13529=CARTESIAN_POINT('Ctrl Pts',(1.22894836457798,-1.5715430117683,96.3574252358099));
#13530=CARTESIAN_POINT('Ctrl Pts',(1.1907449895152,-1.60043801301575,96.3544244187224));
#13531=CARTESIAN_POINT('Ctrl Pts',(1.17807593254765,-1.60978648323745,96.3534288589006));
#13532=CARTESIAN_POINT('Ctrl Pts',(1.15440921280275,-1.62682111020908,96.3515655652517));
#13533=CARTESIAN_POINT('Ctrl Pts',(1.14344248094401,-1.63454789009593,96.3507005555775));
#13534=CARTESIAN_POINT('Ctrl Pts',(1.11632363912303,-1.65324843789287,96.3485586958054));
#13535=CARTESIAN_POINT('Ctrl Pts',(1.10008703827698,-1.66409654238385,96.3472740572605));
#13536=CARTESIAN_POINT('Ctrl Pts',(1.03592154766309,-1.70561778602405,96.3421965783959));
#13537=CARTESIAN_POINT('Ctrl Pts',(0.986851562851305,-1.73447062612848,
96.3383127157537));
#13538=CARTESIAN_POINT('Ctrl Pts',(0.820819803416576,-1.82276843839361,
96.3253207793254));
#13539=CARTESIAN_POINT('Ctrl Pts',(0.699216713288035,-1.87278665220588,
96.3160649716041));
#13540=CARTESIAN_POINT('Ctrl Pts',(0.526777346696431,-1.92455748394022,
96.3037483530531));
#13541=CARTESIAN_POINT('Ctrl Pts',(0.479467565956697,-1.93688599022259,
96.3004448014942));
#13542=CARTESIAN_POINT('Ctrl Pts',(0.393081229214581,-1.9560376889607,96.2945558587287));
#13543=CARTESIAN_POINT('Ctrl Pts',(0.354164067314343,-1.96345727645721,
96.2919542562003));
#13544=CARTESIAN_POINT('Ctrl Pts',(0.290449775420704,-1.9736481732425,96.2877758430453));
#13545=CARTESIAN_POINT('Ctrl Pts',(0.265777757992345,-1.97712176171708,
96.2861773117081));
#13546=CARTESIAN_POINT('Ctrl Pts',(0.217426056269668,-1.98300772827609,
96.2830805014674));
#13547=CARTESIAN_POINT('Ctrl Pts',(0.193755595513476,-1.98546029641551,
96.2815811974058));
#13548=CARTESIAN_POINT('Ctrl Pts',(0.135517884639675,-1.99044301291466,
96.2779301255032));
#13549=CARTESIAN_POINT('Ctrl Pts',(0.100917114017489,-1.99249703752709,
96.2757935327702));
#13550=CARTESIAN_POINT('Ctrl Pts',(-0.0846046827132184,-1.99866469573425,
96.2644813767062));
#13551=CARTESIAN_POINT('Ctrl Pts',(-0.235568569189636,-1.98653714948399,
96.2558312891832));
#13552=CARTESIAN_POINT('Ctrl Pts',(-0.467079258888884,-1.94115401048026,
96.2421054116408));
#13553=CARTESIAN_POINT('Ctrl Pts',(-0.549293759465421,-1.91950917588281,
96.2371240076736));
#13554=CARTESIAN_POINT('Ctrl Pts',(-0.653413530598432,-1.88485914959843,
96.2303960326469));
#13555=CARTESIAN_POINT('Ctrl Pts',(-0.676807714353878,-1.87658584734124,
96.2288558973588));
#13556=CARTESIAN_POINT('Ctrl Pts',(-0.713541301420632,-1.86281890031191,
96.2263832292885));
#13557=CARTESIAN_POINT('Ctrl Pts',(-0.726986618235207,-1.85761294951859,
96.225466487555));
#13558=CARTESIAN_POINT('Ctrl Pts',(-0.751967370117653,-1.84762780939674,
96.2237392152045));
#13559=CARTESIAN_POINT('Ctrl Pts',(-0.763516697964149,-1.84288514972356,
96.2229309182148));
#13560=CARTESIAN_POINT('Ctrl Pts',(-0.795276188659995,-1.82949353569359,
96.2206827353197));
#13561=CARTESIAN_POINT('Ctrl Pts',(-0.815388517297554,-1.82061865370054,
96.2192303483533));
#13562=CARTESIAN_POINT('Ctrl Pts',(-0.956745625039975,-1.75543060473539,
96.2088385436923));
#13563=CARTESIAN_POINT('Ctrl Pts',(-1.07219876689463,-1.68738985317196,
96.1994087122163));
#13564=CARTESIAN_POINT('Ctrl Pts',(-1.26346208142889,-1.54706616769951,
96.1829077469186));
#13565=CARTESIAN_POINT('Ctrl Pts',(-1.34206499216761,-1.47939747836251,
96.1758034296733));
#13566=CARTESIAN_POINT('Ctrl Pts',(-1.44099180885904,-1.37982725631339,
96.1664962900924));
#13567=CARTESIAN_POINT('Ctrl Pts',(-1.46619237951386,-1.35301916270848,
96.1640873235063));
#13568=CARTESIAN_POINT('Ctrl Pts',(-1.50684058254147,-1.30730773003644,
96.1601342248655));
#13569=CARTESIAN_POINT('Ctrl Pts',(-1.52270773663096,-1.28879140229587,
96.1585726966644));
#13570=CARTESIAN_POINT('Ctrl Pts',(-1.55380657808148,-1.25112393637244,
96.1554724719422));
#13571=CARTESIAN_POINT('Ctrl Pts',(-1.5690333268361,-1.231974225023,96.1539341361716));
#13572=CARTESIAN_POINT('Ctrl Pts',(-1.60653891622527,-1.18298214739122,
96.1500886299297));
#13573=CARTESIAN_POINT('Ctrl Pts',(-1.62834201737531,-1.15278644941296,
96.1478002225663));
#13574=CARTESIAN_POINT('Ctrl Pts',(-1.71421037312574,-1.02656354170838,
96.1385323570381));
#13575=CARTESIAN_POINT('Ctrl Pts',(-1.77072946969356,-0.925672963410182,
96.1318246763964));
#13576=CARTESIAN_POINT('Ctrl Pts',(-1.86640446829326,-0.713647014422534,
96.1183375458198));
#13577=CARTESIAN_POINT('Ctrl Pts',(-1.90508938296819,-0.602814909970399,
96.1115802835439));
#13578=CARTESIAN_POINT('Ctrl Pts',(-1.9397143958746,-0.465953653239696,
96.1029131731467));
#13579=CARTESIAN_POINT('Ctrl Pts',(-1.94518526216124,-0.442559509934663,
96.1014202871065));
#13580=CARTESIAN_POINT('Ctrl Pts',(-1.95322299243668,-0.405154524452922,
96.0990069539862));
#13581=CARTESIAN_POINT('Ctrl Pts',(-1.95606475888599,-0.39120439357898,
96.0981011149668));
#13582=CARTESIAN_POINT('Ctrl Pts',(-1.96146590392185,-0.363158757678868,
96.0962662248706));
#13583=CARTESIAN_POINT('Ctrl Pts',(-1.96402323233897,-0.349063730070345,
96.0953371344684));
#13584=CARTESIAN_POINT('Ctrl Pts',(-1.97054084618067,-0.31079923640034,
96.0927984235288));
#13585=CARTESIAN_POINT('Ctrl Pts',(-1.97420803448063,-0.286583143919461,
96.0911740591993));
#13586=CARTESIAN_POINT('Ctrl Pts',(-1.99452407220678,-0.133428627739084,
96.0808146554361));
#13587=CARTESIAN_POINT('Ctrl Pts',(-1.99897871200208,-0.00319550967821111,
96.0716448358197));
#13588=CARTESIAN_POINT('Ctrl Pts',(-1.98421493596182,0.229074219302177,
96.0554570290005));
#13589=CARTESIAN_POINT('Ctrl Pts',(-1.96978438357673,0.330965986839788,
96.0484102559658));
#13590=CARTESIAN_POINT('Ctrl Pts',(-1.93963649974095,0.467099545926854,
96.039165756633));
#13591=CARTESIAN_POINT('Ctrl Pts',(-1.93072348538949,0.502671717293794,
96.0367650005118));
#13592=CARTESIAN_POINT('Ctrl Pts',(-1.914269959775,0.561418319614208,96.0328227809592));
#13593=CARTESIAN_POINT('Ctrl Pts',(-1.9072767805266,0.584735306129012,96.0312640555449));
#13594=CARTESIAN_POINT('Ctrl Pts',(-1.89240786699519,0.631203360254122,
96.0281677232443));
#13595=CARTESIAN_POINT('Ctrl Pts',(-1.88452975338433,0.654349227233851,
96.0266305062904));
#13596=CARTESIAN_POINT('Ctrl Pts',(-1.86357558941499,0.712391686724026,
96.0227847801006));
#13597=CARTESIAN_POINT('Ctrl Pts',(-1.84994329691474,0.747078285606989,
96.0204951135324));
#13598=CARTESIAN_POINT('Ctrl Pts',(-1.78872331079815,0.890877884406888,
96.0110082968231));
#13599=CARTESIAN_POINT('Ctrl Pts',(-1.73239109612273,0.99600141503258,96.0041036401483));
#13600=CARTESIAN_POINT('Ctrl Pts',(-1.66701720851842,1.09548217192407,95.9972028497351));
#13601=CARTESIAN_POINT('',(1.47651116554364,1.34124656216706,96.7230113585667));
#13602=CARTESIAN_POINT('Origin',(0.,0.,96.7230113585667));
#13603=CARTESIAN_POINT('Ctrl Pts',(1.47651116554364,1.34124656216706,96.7230113585667));
#13604=CARTESIAN_POINT('Ctrl Pts',(1.48726169713084,1.32941184037036,96.7219908152654));
#13605=CARTESIAN_POINT('Ctrl Pts',(1.49786990397611,1.31744790463115,96.7209789610056));
#13606=CARTESIAN_POINT('Ctrl Pts',(1.52331794848029,1.2880428242571,96.718536457963));
#13607=CARTESIAN_POINT('Ctrl Pts',(1.5380037652555,1.27047093129895,96.7171139473732));
#13608=CARTESIAN_POINT('Ctrl Pts',(1.60871875273944,1.18283520797476,96.7101797591838));
#13609=CARTESIAN_POINT('Ctrl Pts',(1.66028370281715,1.10929505025935,96.7048517184499));
#13610=CARTESIAN_POINT('Ctrl Pts',(1.76294204385633,0.939605223750329,96.6930911735225));
#13611=CARTESIAN_POINT('Ctrl Pts',(1.81147260227835,0.842251572081398,96.686676330969));
#13612=CARTESIAN_POINT('Ctrl Pts',(1.86702105917168,0.703511697215043,96.6775510758976));
#13613=CARTESIAN_POINT('Ctrl Pts',(1.88103569161036,0.665132139708097,96.6750297349017));
#13614=CARTESIAN_POINT('Ctrl Pts',(1.90232366891468,0.600764912572967,96.6707877605653));
#13615=CARTESIAN_POINT('Ctrl Pts',(1.91026601907129,0.575010830388535,96.6690870885901));
#13616=CARTESIAN_POINT('Ctrl Pts',(1.92433456728577,0.525878065994459,96.6658316618409));
#13617=CARTESIAN_POINT('Ctrl Pts',(1.930562447417,0.502533406960201,96.6642802941438));
#13618=CARTESIAN_POINT('Ctrl Pts',(1.94594191713059,0.44037233471568,96.6601338503895));
#13619=CARTESIAN_POINT('Ctrl Pts',(1.95435573480055,0.401386397567637,96.6575172367624));
#13620=CARTESIAN_POINT('Ctrl Pts',(1.9886706534013,0.215532385394707,96.6449523428374));
#13621=CARTESIAN_POINT('Ctrl Pts',(1.99921245983725,0.0663371280025059,
96.6345518089626));
#13622=CARTESIAN_POINT('Ctrl Pts',(1.98863755630319,-0.188790145534754,
96.6166142496946));
#13623=CARTESIAN_POINT('Ctrl Pts',(1.9757579620226,-0.294458167270419,96.6091551022331));
#13624=CARTESIAN_POINT('Ctrl Pts',(1.94975550955884,-0.421958669233819,
96.6004206196238));
#13625=CARTESIAN_POINT('Ctrl Pts',(1.94457419235579,-0.445226907383012,
96.5988381285844));
#13626=CARTESIAN_POINT('Ctrl Pts',(1.93562003260773,-0.482293486178245,
96.5963411776188));
#13627=CARTESIAN_POINT('Ctrl Pts',(1.93211387872579,-0.496153109306232,
96.5954129548742));
#13628=CARTESIAN_POINT('Ctrl Pts',(1.9248929878971,-0.523458778721541,96.5935964454786));
#13629=CARTESIAN_POINT('Ctrl Pts',(1.92118574119671,-0.536905453278055,
96.5927080254385));
#13630=CARTESIAN_POINT('Ctrl Pts',(1.91080081783194,-0.573087452185706,
96.5903315248574));
#13631=CARTESIAN_POINT('Ctrl Pts',(1.90385832913146,-0.59574539536457,96.5888582421786));
#13632=CARTESIAN_POINT('Ctrl Pts',(1.86271299958318,-0.721955597954185,
96.5807066634816));
#13633=CARTESIAN_POINT('Ctrl Pts',(1.82046326714329,-0.822702048367741,
96.5744013530623));
#13634=CARTESIAN_POINT('Ctrl Pts',(1.73035776614839,-0.996169730937496,
96.5630869894992));
#13635=CARTESIAN_POINT('Ctrl Pts',(1.68559403952925,-1.0701700091139,96.5580938729166));
#13636=CARTESIAN_POINT('Ctrl Pts',(1.61333241706799,-1.17378913762508,96.5505983245961));
#13637=CARTESIAN_POINT('Ctrl Pts',(1.58951103883648,-1.20585106812816,96.5482030087696));
#13638=CARTESIAN_POINT('Ctrl Pts',(1.54372809506867,-1.263756054616,96.5437108452052));
#13639=CARTESIAN_POINT('Ctrl Pts',(1.52203888790065,-1.28979579967673,96.5416245376087));
#13640=CARTESIAN_POINT('Ctrl Pts',(1.4844503667446,-1.33265502744519,96.5380675941928));
#13641=CARTESIAN_POINT('Ctrl Pts',(1.46890214621545,-1.34977358214357,96.5366121129104));
#13642=CARTESIAN_POINT('Ctrl Pts',(1.43687143752207,-1.38383033701437,96.5336424222148));
#13643=CARTESIAN_POINT('Ctrl Pts',(1.42037855837579,-1.40075358192053,96.5321278654982));
#13644=CARTESIAN_POINT('Ctrl Pts',(1.37756178549356,-1.44315378970357,96.5282299285628));
#13645=CARTESIAN_POINT('Ctrl Pts',(1.35083063330466,-1.46820489863795,96.5258277130424));
#13646=CARTESIAN_POINT('Ctrl Pts',(1.21956194370333,-1.5846028400713,96.5141696541504));
#13647=CARTESIAN_POINT('Ctrl Pts',(1.10638410154848,-1.66559276343198,96.504484858548));
#13648=CARTESIAN_POINT('Ctrl Pts',(0.892026206343974,-1.78743864716637,
96.4871524225396));
#13649=CARTESIAN_POINT('Ctrl Pts',(0.794138538157914,-1.8330292029446,96.479572559738));
#13650=CARTESIAN_POINT('Ctrl Pts',(0.672939327064835,-1.87793493801065,
96.4709230621138));
#13651=CARTESIAN_POINT('Ctrl Pts',(0.652720963819422,-1.88505766728064,
96.4695040321753));
#13652=CARTESIAN_POINT('Ctrl Pts',(0.619719990977928,-1.89608891691162,
96.4672309521282));
#13653=CARTESIAN_POINT('Ctrl Pts',(0.607006781943613,-1.90019705703338,
96.4663656519168));
#13654=CARTESIAN_POINT('Ctrl Pts',(0.580432425716176,-1.90849033138692,
96.464579083985));
#13655=CARTESIAN_POINT('Ctrl Pts',(0.566565708973241,-1.91265273235321,
96.4636590088358));
#13656=CARTESIAN_POINT('Ctrl Pts',(0.528322261747202,-1.92367991789518,
96.4611516998533));
#13657=CARTESIAN_POINT('Ctrl Pts',(0.503857404482164,-1.93023229019666,
96.4595812290862));
#13658=CARTESIAN_POINT('Ctrl Pts',(0.384145561165289,-1.95986310821064,
96.4520290391205));
#13659=CARTESIAN_POINT('Ctrl Pts',(0.28740181941165,-1.97636924839291,96.4463268218417));
#13660=CARTESIAN_POINT('Ctrl Pts',(0.0630431245642312,-1.99781742069559,
96.4332564475615));
#13661=CARTESIAN_POINT('Ctrl Pts',(-0.0646002763201175,-1.9977668818009,
96.4259170424308));
#13662=CARTESIAN_POINT('Ctrl Pts',(-0.231716905980416,-1.98166050821652,
96.4157668921247));
#13663=CARTESIAN_POINT('Ctrl Pts',(-0.271940152437178,-1.97654225967292,
96.4132842225398));
#13664=CARTESIAN_POINT('Ctrl Pts',(-0.336911341745153,-1.96625420323763,
96.4091938575476));
#13665=CARTESIAN_POINT('Ctrl Pts',(-0.361766956812591,-1.96183317846301,
96.4076098452906));
#13666=CARTESIAN_POINT('Ctrl Pts',(-0.410048241273102,-1.95229675879365,
96.4044922284262));
#13667=CARTESIAN_POINT('Ctrl Pts',(-0.433478843753377,-1.94722833904459,
96.40296036696));
#13668=CARTESIAN_POINT('Ctrl Pts',(-0.490610404977529,-1.9337876246722,
96.3991764045732));
#13669=CARTESIAN_POINT('Ctrl Pts',(-0.524193957378882,-1.9249554785014,
96.3969100223697));
#13670=CARTESIAN_POINT('Ctrl Pts',(-0.698209252987034,-1.8742997663812,
96.3849392493386));
#13671=CARTESIAN_POINT('Ctrl Pts',(-0.833929832856933,-1.81797789754973,
96.3747738640782));
#13672=CARTESIAN_POINT('Ctrl Pts',(-1.03617142861542,-1.70660495689043,
96.3587224166777));
#13673=CARTESIAN_POINT('Ctrl Pts',(-1.10745364032079,-1.66123458087673,
96.3528756342778));
#13674=CARTESIAN_POINT('Ctrl Pts',(-1.19572665299308,-1.59683526152002,
96.3455568179254));
#13675=CARTESIAN_POINT('Ctrl Pts',(-1.21552760319727,-1.58181473590332,
96.3439099297203));
#13676=CARTESIAN_POINT('Ctrl Pts',(-1.24649016775975,-1.55740241902504,
96.341332984309));
#13677=CARTESIAN_POINT('Ctrl Pts',(-1.25783779212775,-1.54825196703071,
96.3403881729019));
#13678=CARTESIAN_POINT('Ctrl Pts',(-1.28025092259099,-1.52976946516374,
96.338523025581));
#13679=CARTESIAN_POINT('Ctrl Pts',(-1.29131708864611,-1.52043981820306,
96.3376027058249));
#13680=CARTESIAN_POINT('Ctrl Pts',(-1.32104886500062,-1.49481481667599,
96.3351285670159));
#13681=CARTESIAN_POINT('Ctrl Pts',(-1.33951469228894,-1.47829021465366,
96.3335902885473));
#13682=CARTESIAN_POINT('Ctrl Pts',(-1.41922980598246,-1.40423460265592,
96.3269174663282));
#13683=CARTESIAN_POINT('Ctrl Pts',(-1.47712190333099,-1.34320574358376,
96.321983496009));
#13684=CARTESIAN_POINT('Ctrl Pts',(-1.58056471606123,-1.21935311586967,
96.3125878147594));
#13685=CARTESIAN_POINT('Ctrl Pts',(-1.62663977922037,-1.15717317869301,
96.3081275335765));
#13686=CARTESIAN_POINT('Ctrl Pts',(-1.69996102432062,-1.04515941785083,
96.3002865052771));
#13687=CARTESIAN_POINT('Ctrl Pts',(-1.72890541181889,-0.996549626455694,
96.2969419619351));
#13688=CARTESIAN_POINT('Ctrl Pts',(-1.77657077531404,-0.908157024875483,
96.2908914474464));
#13689=CARTESIAN_POINT('Ctrl Pts',(-1.79611587033651,-0.868861472125715,
96.2882122117647));
#13690=CARTESIAN_POINT('Ctrl Pts',(-1.82505986117596,-0.805511285070732,
96.2838886781993));
#13691=CARTESIAN_POINT('Ctrl Pts',(-1.83531542692243,-0.781862591873717,
96.2822738842904));
#13692=CARTESIAN_POINT('Ctrl Pts',(-1.85415856548235,-0.735996345457414,
96.2791368626487));
#13693=CARTESIAN_POINT('Ctrl Pts',(-1.86281211673392,-0.713810579413262,
96.2776172036745));
#13694=CARTESIAN_POINT('Ctrl Pts',(-1.8823925376729,-0.660827882326651,
96.2739802633288));
#13695=CARTESIAN_POINT('Ctrl Pts',(-1.89296360185917,-0.629907730075994,
96.2718515853403));
#13696=CARTESIAN_POINT('Ctrl Pts',(-1.93273573648114,-0.50351430244711,
96.2631197231556));
#13697=CARTESIAN_POINT('Ctrl Pts',(-1.95550613988504,-0.406183281122493,
96.256316390069));
#13698=CARTESIAN_POINT('Ctrl Pts',(-1.99167629779247,-0.174405883924532,
96.2400499008643));
#13699=CARTESIAN_POINT('Ctrl Pts',(-1.99890847523624,-0.039478339302607,
96.2305196935086));
#13700=CARTESIAN_POINT('Ctrl Pts',(-1.99108799705584,0.124285972589346,
96.2194529986591));
#13701=CARTESIAN_POINT('Ctrl Pts',(-1.98905760295722,0.153389942001873,
96.2175068260181));
#13702=CARTESIAN_POINT('Ctrl Pts',(-1.98499114611209,0.197664993924626,
96.2145876994767));
#13703=CARTESIAN_POINT('Ctrl Pts',(-1.9834178195782,0.212873411585156,96.2135924894865));
#13704=CARTESIAN_POINT('Ctrl Pts',(-1.98013094169274,0.241433553360454,
96.211739576329));
#13705=CARTESIAN_POINT('Ctrl Pts',(-1.97845688517373,0.254788282443513,
96.2108799786789));
#13706=CARTESIAN_POINT('Ctrl Pts',(-1.9738684505878,0.288614683802531,96.2087182066313));
#13707=CARTESIAN_POINT('Ctrl Pts',(-1.97077061517926,0.309060445906826,
96.2074258689083));
#13708=CARTESIAN_POINT('Ctrl Pts',(-1.9550372623991,0.403012782224272,96.2015379735637));
#13709=CARTESIAN_POINT('Ctrl Pts',(-1.9386022338701,0.475829441113306,96.1971168997327));
#13710=CARTESIAN_POINT('Ctrl Pts',(-1.89445362025812,0.63048358710917,96.1877132891303));
#13711=CARTESIAN_POINT('Ctrl Pts',(-1.86542953263183,0.711784439051225,
96.1827588419002));
#13712=CARTESIAN_POINT('Ctrl Pts',(-1.80697813392815,0.847112706339792,
96.1741611377272));
#13713=CARTESIAN_POINT('Ctrl Pts',(-1.78015194144302,0.902124304349809,
96.1705609332047));
#13714=CARTESIAN_POINT('Ctrl Pts',(-1.72869993150253,0.996373144169574,
96.1641141611748));
#13715=CARTESIAN_POINT('Ctrl Pts',(-1.70515664328039,1.03614826425857,96.1613009464872));
#13716=CARTESIAN_POINT('Ctrl Pts',(-1.67588371553814,1.08189977128651,96.1579357444606));
#13717=CARTESIAN_POINT('Ctrl Pts',(-1.67147107660237,1.08870463147012,96.1574317715579));
#13718=CARTESIAN_POINT('Ctrl Pts',(-1.66701720827332,1.09548217229703,96.1569262941178));
#13719=CARTESIAN_POINT('Ctrl Pts',(-0.873522400031092,1.789212756073,90.4848163895282));
#13720=CARTESIAN_POINT('Ctrl Pts',(-1.46965815673703,1.49816970645545,90.5272386010227));
#13721=CARTESIAN_POINT('Ctrl Pts',(-2.33738230715447,0.277481532884632,
90.6120830240118));
#13722=CARTESIAN_POINT('Ctrl Pts',(-1.49668109501954,-1.8199475688586,90.7393496584954));
#13723=CARTESIAN_POINT('Ctrl Pts',(0.721519576667083,-2.24126671624503,
90.866616292979));
#13724=CARTESIAN_POINT('Ctrl Pts',(2.27564354702501,-0.605727798775474,
90.9938829274627));
#13725=CARTESIAN_POINT('Ctrl Pts',(1.73989546947818,1.58726092695295,91.1211495619463));
#13726=CARTESIAN_POINT('Ctrl Pts',(-0.394491289803378,2.32163771660372,
91.2484161964299));
#13727=CARTESIAN_POINT('Ctrl Pts',(-2.16633358048632,0.923512996017912,
91.3756828309135));
#13728=CARTESIAN_POINT('Ctrl Pts',(-1.94817348818047,-1.32310505219048,
91.5029494653973));
#13729=CARTESIAN_POINT('Ctrl Pts',(0.0596887161652472,-2.3542100608739,
91.6302160998808));
#13730=CARTESIAN_POINT('Ctrl Pts',(2.01270081331805,-1.22267742138027,91.7574827343644));
#13731=CARTESIAN_POINT('Ctrl Pts',(2.11677850049902,1.03206715101337,91.8847493688481));
#13732=CARTESIAN_POINT('Ctrl Pts',(0.276299030076897,2.33870880557926,92.0120160033317));
#13733=CARTESIAN_POINT('Ctrl Pts',(-1.81799707544443,1.49692744562467,92.1392826378152));
#13734=CARTESIAN_POINT('Ctrl Pts',(-2.24221328773756,-0.71998981316718,
92.266549272299));
#13735=CARTESIAN_POINT('Ctrl Pts',(-0.606646986926806,-2.27549634805281,
92.3938159067825));
#13736=CARTESIAN_POINT('Ctrl Pts',(1.58620794911894,-1.74064620775171,92.5210825412663));
#13737=CARTESIAN_POINT('Ctrl Pts',(2.32191234227693,0.393227629060235,92.6483491757497));
#13738=CARTESIAN_POINT('Ctrl Pts',(0.924620103765244,2.16586758240207,92.7756158102334));
#13739=CARTESIAN_POINT('Ctrl Pts',(-1.32206313274466,1.94885963628849,92.9028824447171));
#13740=CARTESIAN_POINT('Ctrl Pts',(-2.35424914491832,-0.0584445673734767,
93.0301490792007));
#13741=CARTESIAN_POINT('Ctrl Pts',(-1.22373276785853,-2.01205936745052,
93.1574157136843));
#13742=CARTESIAN_POINT('Ctrl Pts',(1.03095084926626,-2.1173202739826,93.2846823481681));
#13743=CARTESIAN_POINT('Ctrl Pts',(2.33856399250142,-0.277530625282423,
93.4119489826516));
#13744=CARTESIAN_POINT('Ctrl Pts',(1.49788372757163,1.81720916022372,93.5392156171351));
#13745=CARTESIAN_POINT('Ctrl Pts',(-0.718809229756443,2.24259182299006,
93.6664822516189));
#13746=CARTESIAN_POINT('Ctrl Pts',(-2.2751768192432,0.607844746766972,93.7937488861024));
#13747=CARTESIAN_POINT('Ctrl Pts',(-1.74148085787701,-1.58529152456845,
93.9210155205861));
#13748=CARTESIAN_POINT('Ctrl Pts',(0.39200534075291,-2.32211898878962,94.0482821550696));
#13749=CARTESIAN_POINT('Ctrl Pts',(2.16538059562593,-0.925760055246912,
94.1755487895534));
#13750=CARTESIAN_POINT('Ctrl Pts',(1.94955526487718,1.3210371221532,94.3028154240369));
#13751=CARTESIAN_POINT('Ctrl Pts',(-0.0572053256286392,2.35427956528251,
94.4300820585206));
#13752=CARTESIAN_POINT('Ctrl Pts',(-2.01141494837865,1.22479173695497,94.5573486930042));
#13753=CARTESIAN_POINT('Ctrl Pts',(-2.11786263969355,-1.02983625776083,
94.6846153274878));
#13754=CARTESIAN_POINT('Ctrl Pts',(-0.278761581426706,-2.33841745149781,
94.8118819619715));
#13755=CARTESIAN_POINT('Ctrl Pts',(1.81642050034851,-1.49884032661424,94.939148596455));
#13756=CARTESIAN_POINT('Ctrl Pts',(2.2429697838632,0.717629216563515,95.0664152309388));
#13757=CARTESIAN_POINT('Ctrl Pts',(0.609042460650236,2.27485544869131,95.1936818654223));
#13758=CARTESIAN_POINT('Ctrl Pts',(-1.5843750171001,1.7423173159803,95.320948499906));
#13759=CARTESIAN_POINT('Ctrl Pts',(-2.32232421427614,-0.390787518315191,
95.4482151343895));
#13760=CARTESIAN_POINT('Ctrl Pts',(-0.926901358188101,-2.1648837441642,
95.5754817688732));
#13761=CARTESIAN_POINT('Ctrl Pts',(1.32001402965102,-1.95026918160178,95.7027484033568));
#13762=CARTESIAN_POINT('Ctrl Pts',(2.35430264557917,0.0560043638979313,
95.8300150378406));
#13763=CARTESIAN_POINT('Ctrl Pts',(1.22586397590062,2.01069206430939,95.957281672324));
#13764=CARTESIAN_POINT('Ctrl Pts',(-1.02874906980149,2.11856292007691,96.0845483068079));
#13765=CARTESIAN_POINT('Ctrl Pts',(-2.33821394037349,0.279669963294229,
96.2118149412912));
#13766=CARTESIAN_POINT('Ctrl Pts',(-1.49991103301835,-1.81497489952105,
96.3390815757751));
#13767=CARTESIAN_POINT('Ctrl Pts',(0.716678355738466,-2.24469053279049,
96.4663482102585));
#13768=CARTESIAN_POINT('Ctrl Pts',(2.27428213796879,-0.6072203508056,96.5936329237197));
#13769=CARTESIAN_POINT('Ctrl Pts',(1.91968396703937,0.848347233302648,96.678495425686));
#13770=CARTESIAN_POINT('Ctrl Pts',(1.47321010047682,1.33939374792847,96.7209357161579));
#13771=CARTESIAN_POINT('Ctrl Pts',(-0.941185533557266,1.92780535726628,
90.5738598409889));
#13772=CARTESIAN_POINT('Ctrl Pts',(-1.58349802631975,1.61421808356536,90.6162820524834));
#13773=CARTESIAN_POINT('Ctrl Pts',(-2.5184361772614,0.298975280509143,90.7011264754725));
#13774=CARTESIAN_POINT('Ctrl Pts',(-1.61261416413696,-1.96092089176129,
90.8283931099562));
#13775=CARTESIAN_POINT('Ctrl Pts',(0.777408556109435,-2.41487546295108,
90.9556597444397));
#13776=CARTESIAN_POINT('Ctrl Pts',(2.45191512652298,-0.652647535381667,
91.0829263789235));
#13777=CARTESIAN_POINT('Ctrl Pts',(1.87466794865983,1.71021031902061,91.210193013407));
#13778=CARTESIAN_POINT('Ctrl Pts',(-0.425048625042778,2.50147200913288,
91.3374596478906));
#13779=CARTESIAN_POINT('Ctrl Pts',(-2.33413799891161,0.995048406169388,
91.4647262823743));
#13780=CARTESIAN_POINT('Ctrl Pts',(-2.09907920377313,-1.42559290346061,
91.5919929168578));
#13781=CARTESIAN_POINT('Ctrl Pts',(0.0643122101612201,-2.53656741048728,
91.7192595513416));
#13782=CARTESIAN_POINT('Ctrl Pts',(2.16860482204746,-1.31738613820236,91.8465261858251));
#13783=CARTESIAN_POINT('Ctrl Pts',(2.28074437741244,1.11201117699887,91.9737928203088));
#13784=CARTESIAN_POINT('Ctrl Pts',(0.297701180914228,2.51986542638844,92.1010594547923));
#13785=CARTESIAN_POINT('Ctrl Pts',(-1.95881931292982,1.6128795970849,92.228326089276));
#13786=CARTESIAN_POINT('Ctrl Pts',(-2.41589535596724,-0.775760296973985,
92.3555927237596));
#13787=CARTESIAN_POINT('Ctrl Pts',(-0.653637923940244,-2.4517565255035,
92.4828593582433));
#13788=CARTESIAN_POINT('Ctrl Pts',(1.70907577741699,-1.87547683919603,92.6101259927268));
#13789=CARTESIAN_POINT('Ctrl Pts',(2.50176790733853,0.423687081010561,92.7373926272105));
#13790=CARTESIAN_POINT('Ctrl Pts',(0.996241270594892,2.3336359045686,92.8646592616943));
#13791=CARTESIAN_POINT('Ctrl Pts',(-1.42447027682906,2.09981850098307,92.9919258961778));
#13792=CARTESIAN_POINT('Ctrl Pts',(-2.53660952198573,-0.0629716894781019,
93.1191925306614));
#13793=CARTESIAN_POINT('Ctrl Pts',(-1.31852323192565,-2.16791368971812,
93.2464591651451));
#13794=CARTESIAN_POINT('Ctrl Pts',(1.11080840640544,-2.28132811672488,93.3737257996286));
#13795=CARTESIAN_POINT('Ctrl Pts',(2.51970939607493,-0.299028175609036,
93.5009924341123));
#13796=CARTESIAN_POINT('Ctrl Pts',(1.61390995272828,1.95797036571637,93.628259068596));
#13797=CARTESIAN_POINT('Ctrl Pts',(-0.774488265452751,2.41630321259872,
93.7555257030794));
#13798=CARTESIAN_POINT('Ctrl Pts',(-2.45141224595995,0.654928462378868,
93.8827923375632));
#13799=CARTESIAN_POINT('Ctrl Pts',(-1.8763761414045,-1.70808836652804,94.0100589720467));
#13800=CARTESIAN_POINT('Ctrl Pts',(0.422370114127229,-2.50199056071101,
94.1373256065305));
#13801=CARTESIAN_POINT('Ctrl Pts',(2.33311119574748,-0.997469522833716,
94.264592241014));
#13802=CARTESIAN_POINT('Ctrl Pts',(2.10056801303263,1.42336479135333,94.3918588754976));
#13803=CARTESIAN_POINT('Ctrl Pts',(-0.0616364559422705,2.53664229871441,
94.5191255099812));
#13804=CARTESIAN_POINT('Ctrl Pts',(-2.16721935387969,1.3196642288755,94.6463921444649));
#13805=CARTESIAN_POINT('Ctrl Pts',(-2.2819124941387,-1.10960747852916,94.7736587789485));
#13806=CARTESIAN_POINT('Ctrl Pts',(-0.300354481740857,-2.51955150399036,
94.9009254134322));
#13807=CARTESIAN_POINT('Ctrl Pts',(1.9571206161674,-1.61494065002954,95.0281920479158));
#13808=CARTESIAN_POINT('Ctrl Pts',(2.41671045035935,0.773216848318456,95.1554586823994));
#13809=CARTESIAN_POINT('Ctrl Pts',(0.656218951300763,2.45106598201258,95.2827253168831));
#13810=CARTESIAN_POINT('Ctrl Pts',(-1.70710086629843,1.87727739163715,95.4099919513666));
#13811=CARTESIAN_POINT('Ctrl Pts',(-2.5022116829845,-0.421057959040214,
95.5372585858503));
#13812=CARTESIAN_POINT('Ctrl Pts',(-0.998699231216256,-2.33257585812122,
95.6645252203339));
#13813=CARTESIAN_POINT('Ctrl Pts',(1.42226245000237,-2.101337229819,95.7917918548176));
#13814=CARTESIAN_POINT('Ctrl Pts',(2.53666716681318,0.0603424675943402,
95.9190584893012));
#13815=CARTESIAN_POINT('Ctrl Pts',(1.32081952355841,2.16644047513726,96.0463251237848));
#13816=CARTESIAN_POINT('Ctrl Pts',(-1.10843607688045,2.28266701831146,96.1735917582684));
#13817=CARTESIAN_POINT('Ctrl Pts',(-2.51933222887374,0.301333226959783,
96.300858392752));
#13818=CARTESIAN_POINT('Ctrl Pts',(-1.61609429346009,-1.95556303895352,
96.4281250272357));
#13819=CARTESIAN_POINT('Ctrl Pts',(0.77219233371765,-2.41856448867272,96.5553916617193));
#13820=CARTESIAN_POINT('Ctrl Pts',(2.45044826258347,-0.654255700643123,
96.6826763751803));
#13821=CARTESIAN_POINT('Ctrl Pts',(2.06838288144068,0.914060295865755,96.7675388771468));
#13822=CARTESIAN_POINT('Ctrl Pts',(1.58732510398118,1.44314332321926,96.8099791676186));
#13823=CARTESIAN_POINT('Ctrl Pts',(-1.00884866708344,2.06639795845957,90.6629032924495));
#13824=CARTESIAN_POINT('Ctrl Pts',(-1.69733789590249,1.73026646067528,90.7053255039442));
#13825=CARTESIAN_POINT('Ctrl Pts',(-2.69949004736833,0.320469028133655,
90.7901699269332));
#13826=CARTESIAN_POINT('Ctrl Pts',(-1.72854723325438,-2.10189421466399,
90.9174365614169));
#13827=CARTESIAN_POINT('Ctrl Pts',(0.83329753555179,-2.58848420965714,91.0447031959004));
#13828=CARTESIAN_POINT('Ctrl Pts',(2.62818670602095,-0.699567271987858,
91.171969830384));
#13829=CARTESIAN_POINT('Ctrl Pts',(2.00944042784148,1.83315971108825,91.2992364648678));
#13830=CARTESIAN_POINT('Ctrl Pts',(-0.455605960282178,2.68130630166204,
91.4265030993513));
#13831=CARTESIAN_POINT('Ctrl Pts',(-2.50194241733692,1.06658381632086,91.553769733835));
#13832=CARTESIAN_POINT('Ctrl Pts',(-2.24998491936581,-1.52808075473076,
91.6810363683186));
#13833=CARTESIAN_POINT('Ctrl Pts',(0.0689357041571928,-2.71892476010065,
91.8083030028023));
#13834=CARTESIAN_POINT('Ctrl Pts',(2.32450883077687,-1.41209485502446,91.9355696372858));
#13835=CARTESIAN_POINT('Ctrl Pts',(2.44471025432585,1.19195520298437,92.0628362717697));
#13836=CARTESIAN_POINT('Ctrl Pts',(0.319103331751555,2.70102204719762,92.1901029062529));
#13837=CARTESIAN_POINT('Ctrl Pts',(-2.09964155041522,1.72883174854512,92.3173695407368));
#13838=CARTESIAN_POINT('Ctrl Pts',(-2.58957742419693,-0.83153078078079,
92.4446361752204));
#13839=CARTESIAN_POINT('Ctrl Pts',(-0.700628860953678,-2.62801670295417,
92.5719028097039));
#13840=CARTESIAN_POINT('Ctrl Pts',(1.83194360571502,-2.01030747064033,92.6991694441877));
#13841=CARTESIAN_POINT('Ctrl Pts',(2.68162347240014,0.454146532960888,92.8264360786714));
#13842=CARTESIAN_POINT('Ctrl Pts',(1.06786243742454,2.50140422673511,92.9537027131547));
#13843=CARTESIAN_POINT('Ctrl Pts',(-1.52687742091346,2.25077736567763,93.0809693476386));
#13844=CARTESIAN_POINT('Ctrl Pts',(-2.71896989905314,-0.0674988115827291,
93.2082359821221));
#13845=CARTESIAN_POINT('Ctrl Pts',(-1.41331369599278,-2.3237680119857,93.3355026166056));
#13846=CARTESIAN_POINT('Ctrl Pts',(1.19066596354461,-2.44533595946718,93.4627692510895));
#13847=CARTESIAN_POINT('Ctrl Pts',(2.70085479964844,-0.320525725935651,
93.5900358855729));
#13848=CARTESIAN_POINT('Ctrl Pts',(1.72993617788491,2.09873157120903,93.7173025200566));
#13849=CARTESIAN_POINT('Ctrl Pts',(-0.830167301149058,2.59001460220737,
93.8445691545403));
#13850=CARTESIAN_POINT('Ctrl Pts',(-2.6276476726767,0.702012177990762,93.971835789024));
#13851=CARTESIAN_POINT('Ctrl Pts',(-2.01127142493201,-1.83088520848765,
94.0991024235075));
#13852=CARTESIAN_POINT('Ctrl Pts',(0.452734887501548,-2.68186213263241,
94.2263690579912));
#13853=CARTESIAN_POINT('Ctrl Pts',(2.50084179586903,-1.06917899042052,94.3536356924748));
#13854=CARTESIAN_POINT('Ctrl Pts',(2.2515807611881,1.52569246055347,94.4809023269583));
#13855=CARTESIAN_POINT('Ctrl Pts',(-0.0660675862559036,2.71900503214631,
94.6081689614421));
#13856=CARTESIAN_POINT('Ctrl Pts',(-2.32302375938074,1.41453672079602,94.7354355959255));
#13857=CARTESIAN_POINT('Ctrl Pts',(-2.44596234858386,-1.1893786992975,94.8627022304094));
#13858=CARTESIAN_POINT('Ctrl Pts',(-0.321947382055006,-2.70068555648289,
94.9899688648929));
#13859=CARTESIAN_POINT('Ctrl Pts',(2.09782073198627,-1.73104097344485,95.1172354993765));
#13860=CARTESIAN_POINT('Ctrl Pts',(2.5904511168555,0.828804480073396,95.2445021338601));
#13861=CARTESIAN_POINT('Ctrl Pts',(0.703395441951291,2.62727651533385,95.3717687683439));
#13862=CARTESIAN_POINT('Ctrl Pts',(-1.82982671549677,2.01223746729401,95.4990354028273));
#13863=CARTESIAN_POINT('Ctrl Pts',(-2.68209915169286,-0.451328399765236,
95.626302037311));
#13864=CARTESIAN_POINT('Ctrl Pts',(-1.07049710424441,-2.50026797207826,
95.7535686717946));
#13865=CARTESIAN_POINT('Ctrl Pts',(1.52451087035372,-2.25240527803622,95.8808353062783));
#13866=CARTESIAN_POINT('Ctrl Pts',(2.71903168804719,0.0646805712907468,
96.008101940762));
#13867=CARTESIAN_POINT('Ctrl Pts',(1.4157750712162,2.32218888596513,96.1353685752456));
#13868=CARTESIAN_POINT('Ctrl Pts',(-1.1881230839594,2.44677111654599,96.2626352097291));
#13869=CARTESIAN_POINT('Ctrl Pts',(-2.700450517374,0.322996490625344,96.3899018442128));
#13870=CARTESIAN_POINT('Ctrl Pts',(-1.73227755390183,-2.09615117838598,
96.5171684786964));
#13871=CARTESIAN_POINT('Ctrl Pts',(0.827706311696832,-2.59243844455495,
96.64443511318));
#13872=CARTESIAN_POINT('Ctrl Pts',(2.62661438719814,-0.701291050480648,
96.771719826641));
#13873=CARTESIAN_POINT('Ctrl Pts',(2.21708179584199,0.97977335842886,96.8565823286075));
#13874=CARTESIAN_POINT('Ctrl Pts',(1.70144010748552,1.54689289851004,96.8990226190793));
#13875=CARTESIAN_POINT('Ctrl Pts',(-1.07651180060961,2.20499055965285,90.7519467439103));
#13876=CARTESIAN_POINT('Ctrl Pts',(-1.81117776548521,1.84631483778521,90.7943689554048));
#13877=CARTESIAN_POINT('Ctrl Pts',(-2.88054391747525,0.341962775758166,
90.879213378394));
#13878=CARTESIAN_POINT('Ctrl Pts',(-1.84448030237179,-2.24286753756668,
91.0064800128776));
#13879=CARTESIAN_POINT('Ctrl Pts',(0.889186514994142,-2.7620929563632,91.1337466473612));
#13880=CARTESIAN_POINT('Ctrl Pts',(2.80445828551892,-0.746487008594048,
91.2610132818449));
#13881=CARTESIAN_POINT('Ctrl Pts',(2.14421290702314,1.95610910315591,91.3882799163285));
#13882=CARTESIAN_POINT('Ctrl Pts',(-0.486163295521579,2.86114059419121,
91.5155465508121));
#13883=CARTESIAN_POINT('Ctrl Pts',(-2.66974683576221,1.13811922647233,91.6428131852957));
#13884=CARTESIAN_POINT('Ctrl Pts',(-2.40089063495847,-1.63056860600089,
91.7700798197793));
#13885=CARTESIAN_POINT('Ctrl Pts',(0.073559198153165,-2.90128210971402,
91.8973464542631));
#13886=CARTESIAN_POINT('Ctrl Pts',(2.48041283950629,-1.50680357184655,92.0246130887465));
#13887=CARTESIAN_POINT('Ctrl Pts',(2.60867613123927,1.27189922896985,92.1518797232303));
#13888=CARTESIAN_POINT('Ctrl Pts',(0.340505482588885,2.8821786680068,92.2791463577138));
#13889=CARTESIAN_POINT('Ctrl Pts',(-2.24046378790063,1.84478390000535,92.4064129921973));
#13890=CARTESIAN_POINT('Ctrl Pts',(-2.76325949242661,-0.887301264587592,
92.5336796266812));
#13891=CARTESIAN_POINT('Ctrl Pts',(-0.747619797967113,-2.80427688040486,
92.6609462611647));
#13892=CARTESIAN_POINT('Ctrl Pts',(1.95481143401308,-2.14513810208465,92.7882128956484));
#13893=CARTESIAN_POINT('Ctrl Pts',(2.86147903746175,0.484605984911214,92.9154795301319));
#13894=CARTESIAN_POINT('Ctrl Pts',(1.13948360425419,2.66917254890164,93.0427461646156));
#13895=CARTESIAN_POINT('Ctrl Pts',(-1.62928456499786,2.4017362303722,93.1700127990993));
#13896=CARTESIAN_POINT('Ctrl Pts',(-2.90133027612055,-0.0720259336873552,
93.2972794335828));
#13897=CARTESIAN_POINT('Ctrl Pts',(-1.5081041600599,-2.47962233425328,93.4245460680664));
#13898=CARTESIAN_POINT('Ctrl Pts',(1.27052352068378,-2.60934380220947,93.5518127025501));
#13899=CARTESIAN_POINT('Ctrl Pts',(2.88200020322195,-0.342023276262264,
93.6790793370337));
#13900=CARTESIAN_POINT('Ctrl Pts',(1.84596240304155,2.23949277670167,93.8063459715173));
#13901=CARTESIAN_POINT('Ctrl Pts',(-0.885846336845365,2.76372599181604,
93.933612606001));
#13902=CARTESIAN_POINT('Ctrl Pts',(-2.80388309939345,0.749095893602658,
94.0608792404846));
#13903=CARTESIAN_POINT('Ctrl Pts',(-2.14616670845951,-1.95368205044725,
94.1881458749681));
#13904=CARTESIAN_POINT('Ctrl Pts',(0.483099660875866,-2.86173370455381,
94.3154125094519));
#13905=CARTESIAN_POINT('Ctrl Pts',(2.66857239599058,-1.14088845800733,94.4426791439354));
#13906=CARTESIAN_POINT('Ctrl Pts',(2.40259350934356,1.6280201297536,94.5699457784191));
#13907=CARTESIAN_POINT('Ctrl Pts',(-0.0704987165695354,2.9013677655782,
94.6972124129027));
#13908=CARTESIAN_POINT('Ctrl Pts',(-2.47882816488178,1.50940921271655,94.8244790473864));
#13909=CARTESIAN_POINT('Ctrl Pts',(-2.61001220302903,-1.26914992006584,
94.9517456818698));
#13910=CARTESIAN_POINT('Ctrl Pts',(-0.343540282369155,-2.88181960897544,
95.0790123163536));
#13911=CARTESIAN_POINT('Ctrl Pts',(2.23852084780516,-1.84714129686014,95.2062789508372));
#13912=CARTESIAN_POINT('Ctrl Pts',(2.76419178335165,0.884392111828334,95.3335455853208));
#13913=CARTESIAN_POINT('Ctrl Pts',(0.750571932601818,2.80348704865511,95.4608122198045));
#13914=CARTESIAN_POINT('Ctrl Pts',(-1.9525525646951,2.14719754295085,95.5880788542881));
#13915=CARTESIAN_POINT('Ctrl Pts',(-2.86198662040122,-0.481598840490258,
95.7153454887717));
#13916=CARTESIAN_POINT('Ctrl Pts',(-1.14229497727256,-2.66796008603529,
95.8426121232553));
#13917=CARTESIAN_POINT('Ctrl Pts',(1.62675929070508,-2.40347332625343,95.969878757739));
#13918=CARTESIAN_POINT('Ctrl Pts',(2.90139620928121,0.0690186749871554,
96.0971453922227));
#13919=CARTESIAN_POINT('Ctrl Pts',(1.510730618874,2.477937296793,96.2244120267062));
#13920=CARTESIAN_POINT('Ctrl Pts',(-1.26781009103836,2.61087521478053,96.3516786611899));
#13921=CARTESIAN_POINT('Ctrl Pts',(-2.88156880587425,0.344659754290898,
96.4789452956735));
#13922=CARTESIAN_POINT('Ctrl Pts',(-1.84846081434358,-2.23673931781844,
96.6062119301572));
#13923=CARTESIAN_POINT('Ctrl Pts',(0.883220289676016,-2.76631240043719,
96.7334785646408));
#13924=CARTESIAN_POINT('Ctrl Pts',(2.80278051181281,-0.748326400318174,
96.8607632781017));
#13925=CARTESIAN_POINT('Ctrl Pts',(2.3657807102433,1.04548642099196,96.9456257800682));
#13926=CARTESIAN_POINT('Ctrl Pts',(1.81555511098988,1.65064247380082,96.98806607054));
#13927=CARTESIAN_POINT('Ctrl Pts',(0.588712386787453,-2.38292909182934,
96.7230113585668));
#13928=CARTESIAN_POINT('Ctrl Pts',(0.640648769308371,-2.3652933144126,96.7230113585668));
#13929=CARTESIAN_POINT('Ctrl Pts',(0.691875067436002,-2.34581391031218,
96.7230113585668));
#13930=CARTESIAN_POINT('Ctrl Pts',(0.742296016079015,-2.32446461360961,
96.7230113585668));
#13931=CARTESIAN_POINT('Ctrl Pts',(0.820739821153515,-2.2912498464526,96.7230113585668));
#13932=CARTESIAN_POINT('Ctrl Pts',(0.897236129890821,-2.25351082281703,
96.7230113585668));
#13933=CARTESIAN_POINT('Ctrl Pts',(0.971544835524987,-2.21156500778445,
96.7230113585668));
#13934=CARTESIAN_POINT('Ctrl Pts',(1.03217330020216,-2.17734142195619,96.7230113585668));
#13935=CARTESIAN_POINT('Ctrl Pts',(1.09134509111778,-2.14031633100486,96.7230113585668));
#13936=CARTESIAN_POINT('Ctrl Pts',(1.14891121002181,-2.10064528356617,96.7230113585668));
#13937=CARTESIAN_POINT('Ctrl Pts',(1.16159513936322,-2.09190429542607,96.7230113585668));
#13938=CARTESIAN_POINT('Ctrl Pts',(1.17419734893583,-2.08303729003666,96.7230113585668));
#13939=CARTESIAN_POINT('Ctrl Pts',(1.18671008065498,-2.07405069777297,96.7230113585668));
#13940=CARTESIAN_POINT('Ctrl Pts',(1.2556958568937,-2.02450539807606,96.7230113585668));
#13941=CARTESIAN_POINT('Ctrl Pts',(1.32202432452181,-1.97128734189988,96.7230113585668));
#13942=CARTESIAN_POINT('Ctrl Pts',(1.38545426454246,-1.91470942721314,96.7230113585668));
#13943=CARTESIAN_POINT('Ctrl Pts',(1.43441942286438,-1.87103373479946,96.7230113585668));
#13944=CARTESIAN_POINT('Ctrl Pts',(1.48165667196868,-1.82535488812884,96.7230113585668));
#13945=CARTESIAN_POINT('Ctrl Pts',(1.52703736438344,-1.7778050599483,96.7230113585668));
#13946=CARTESIAN_POINT('Ctrl Pts',(1.54858651511599,-1.75522588893425,96.7230113585668));
#13947=CARTESIAN_POINT('Ctrl Pts',(1.56971679742231,-1.73222471822232,96.7230113585668));
#13948=CARTESIAN_POINT('Ctrl Pts',(1.59041304366888,-1.70881516364333,96.7230113585668));
#13949=CARTESIAN_POINT('Ctrl Pts',(1.60045213541326,-1.69745993220119,96.7230113585668));
#13950=CARTESIAN_POINT('Ctrl Pts',(1.61039045013747,-1.68600700476021,96.7230113585668));
#13951=CARTESIAN_POINT('Ctrl Pts',(1.62022185084907,-1.67446300273117,96.7230113585668));
#13952=CARTESIAN_POINT('Ctrl Pts',(1.67412442902213,-1.61117075271984,96.7230113585668));
#13953=CARTESIAN_POINT('Ctrl Pts',(1.72466397502101,-1.54532438173906,96.7230113585668));
#13954=CARTESIAN_POINT('Ctrl Pts',(1.77161894887438,-1.47721544158816,96.7230113585668));
#13955=CARTESIAN_POINT('Ctrl Pts',(1.81810231493719,-1.40979057607613,96.7230113585668));
#13956=CARTESIAN_POINT('Ctrl Pts',(1.86107318675472,-1.34014747392538,96.7230113585667));
#13957=CARTESIAN_POINT('Ctrl Pts',(1.90027066793302,-1.26854810370225,96.7230113585667));
#13958=CARTESIAN_POINT('Ctrl Pts',(1.93827854866182,-1.19912169562974,96.7230113585667));
#13959=CARTESIAN_POINT('Ctrl Pts',(1.97273879647841,-1.1278551884302,96.7230113585667));
#13960=CARTESIAN_POINT('Ctrl Pts',(2.00336580355094,-1.05497981877367,96.7230113585667));
#13961=CARTESIAN_POINT('Ctrl Pts',(2.02129404247609,-1.01232050714498,96.7230113585667));
#13962=CARTESIAN_POINT('Ctrl Pts',(2.03790785886586,-0.969109813993785,
96.7230113585668));
#13963=CARTESIAN_POINT('Ctrl Pts',(2.05314159279707,-0.925394393548234,
96.7230113585668));
#13964=CARTESIAN_POINT('Ctrl Pts',(2.05752593699301,-0.912812878683333,
96.7230113585668));
#13965=CARTESIAN_POINT('Ctrl Pts',(2.06179609056006,-0.90018878324672,96.7230113585667));
#13966=CARTESIAN_POINT('Ctrl Pts',(2.06594555589405,-0.887538783166725,
96.7230113585667));
#13967=CARTESIAN_POINT('Ctrl Pts',(2.09030106369674,-0.813288933884062,
96.7230113585667));
#13968=CARTESIAN_POINT('Ctrl Pts',(2.11054754703649,-0.738021766380488,
96.7230113585668));
#13969=CARTESIAN_POINT('Ctrl Pts',(2.1264523557256,-0.661972017543704,96.7230113585668));
#13970=CARTESIAN_POINT('Ctrl Pts',(2.13251522995639,-0.632982039009962,
96.7230113585668));
#13971=CARTESIAN_POINT('Ctrl Pts',(2.13794668381121,-0.603878262914742,
96.7230113585667));
#13972=CARTESIAN_POINT('Ctrl Pts',(2.14273181896565,-0.574673529019169,
96.7230113585667));
#13973=CARTESIAN_POINT('Ctrl Pts',(2.15558851779652,-0.496206264038638,
96.7230113585667));
#13974=CARTESIAN_POINT('Ctrl Pts',(2.16378320115503,-0.417009388046162,
96.7230113585668));
#13975=CARTESIAN_POINT('Ctrl Pts',(2.16743223057129,-0.33743940379413,96.7230113585668));
#13976=CARTESIAN_POINT('Ctrl Pts',(2.17098140797991,-0.260046771864714,
96.7230113585668));
#13977=CARTESIAN_POINT('Ctrl Pts',(2.17022968718329,-0.182300337705529,
96.7230113585668));
#13978=CARTESIAN_POINT('Ctrl Pts',(2.16523998757234,-0.104545110509807,
96.7230113585668));
#13979=CARTESIAN_POINT('Ctrl Pts',(2.16444474155328,-0.0921526741489186,
96.7230113585668));
#13980=CARTESIAN_POINT('Ctrl Pts',(2.16354155389744,-0.0797575534964672,
96.7230113585668));
#13981=CARTESIAN_POINT('Ctrl Pts',(2.1625312776458,-0.0673695075572312,
96.7230113585668));
#13982=CARTESIAN_POINT('Ctrl Pts',(2.1562180590047,0.0100434202668876,96.7230113585668));
#13983=CARTESIAN_POINT('Ctrl Pts',(2.14574427085824,0.0869961031253285,
96.7230113585668));
#13984=CARTESIAN_POINT('Ctrl Pts',(2.13125086339959,0.163162923078114,96.7230113585668));
#13985=CARTESIAN_POINT('Ctrl Pts',(2.11677422416584,0.239241621423175,96.7230113585668));
#13986=CARTESIAN_POINT('Ctrl Pts',(2.09828678062113,0.314537217629474,96.7230113585668));
#13987=CARTESIAN_POINT('Ctrl Pts',(2.07588093305262,0.388707135189438,96.7230113585668));
#13988=CARTESIAN_POINT('Ctrl Pts',(2.05365575074666,0.462278997818072,96.7230113585668));
#13989=CARTESIAN_POINT('Ctrl Pts',(2.02757460817981,0.534744112225099,96.7230113585668));
#13990=CARTESIAN_POINT('Ctrl Pts',(1.99768768671817,0.605737007823448,96.7230113585668));
#13991=CARTESIAN_POINT('Ctrl Pts',(1.98597215240563,0.633565892956258,96.7230113585668));
#13992=CARTESIAN_POINT('Ctrl Pts',(1.97367142411387,0.661168148916436,96.7230113585668));
#13993=CARTESIAN_POINT('Ctrl Pts',(1.96078707526267,0.688520011253182,96.7230113585668));
#13994=CARTESIAN_POINT('Ctrl Pts',(1.95276721707462,0.705545167871723,96.7230113585668));
#13995=CARTESIAN_POINT('Ctrl Pts',(1.94451794942827,0.722479472898389,96.7230113585668));
#13996=CARTESIAN_POINT('Ctrl Pts',(1.93605669336428,0.739283797803819,96.7230113585668));
#13997=CARTESIAN_POINT('Ctrl Pts',(1.90242108599403,0.806085188798996,96.7230113585668));
#13998=CARTESIAN_POINT('Ctrl Pts',(1.86540482271834,0.870913728227497,96.7230113585667));
#13999=CARTESIAN_POINT('Ctrl Pts',(1.8250950839614,0.933459813271843,96.7230113585667));
#14000=CARTESIAN_POINT('Ctrl Pts',(1.78524429298128,0.995293777931269,96.7230113585667));
#14001=CARTESIAN_POINT('Ctrl Pts',(1.74217409759157,1.05489768041583,96.7230113585667));
#14002=CARTESIAN_POINT('Ctrl Pts',(1.69593353228868,1.11193673353134,96.7230113585667));
#14003=CARTESIAN_POINT('Ctrl Pts',(1.65129120780821,1.16700431111312,96.7230113585667));
#14004=CARTESIAN_POINT('Ctrl Pts',(1.60369337036815,1.21968169051598,96.7230113585667));
#14005=CARTESIAN_POINT('Ctrl Pts',(1.55315866977046,1.26962629746061,96.7230113585667));
#14006=CARTESIAN_POINT('Ctrl Pts',(1.52831927675166,1.29417564090965,96.7230113585667));
#14007=CARTESIAN_POINT('Ctrl Pts',(1.50276997933335,1.31806405778729,96.7230113585667));
#14008=CARTESIAN_POINT('Ctrl Pts',(1.47651116554366,1.34124656216704,96.7230113585667));
#14009=CARTESIAN_POINT('Ctrl Pts',(-1.1629311539782,-1.62480320830708,90.7500736540522));
#14010=CARTESIAN_POINT('Ctrl Pts',(-1.20248717512367,-1.60291707496938,
90.7500736540522));
#14011=CARTESIAN_POINT('Ctrl Pts',(-1.24117742673991,-1.5796333799921,90.7500736540522));
#14012=CARTESIAN_POINT('Ctrl Pts',(-1.27891854248392,-1.5549680498462,90.7500736540522));
#14013=CARTESIAN_POINT('Ctrl Pts',(-1.3391412895418,-1.51561007355979,90.7500736540522));
#14014=CARTESIAN_POINT('Ctrl Pts',(-1.39694873666562,-1.47273701788695,
90.7500736540522));
#14015=CARTESIAN_POINT('Ctrl Pts',(-1.45225791381737,-1.42669773153816,
90.7500736540522));
#14016=CARTESIAN_POINT('Ctrl Pts',(-1.48252910851924,-1.40150002886441,
90.7500736540522));
#14017=CARTESIAN_POINT('Ctrl Pts',(-1.51205165542062,-1.37535297886323,
90.7500736540522));
#14018=CARTESIAN_POINT('Ctrl Pts',(-1.5408093008143,-1.34830778980114,90.7500736540522));
#14019=CARTESIAN_POINT('Ctrl Pts',(-1.55479063378575,-1.33515901533173,
90.7500736540522));
#14020=CARTESIAN_POINT('Ctrl Pts',(-1.56859113601269,-1.32179788964324,
90.7500736540522));
#14021=CARTESIAN_POINT('Ctrl Pts',(-1.58220874619757,-1.30822998007715,
90.7500736540522));
#14022=CARTESIAN_POINT('Ctrl Pts',(-1.59343008164899,-1.29704959948551,
90.7500736540522));
#14023=CARTESIAN_POINT('Ctrl Pts',(-1.60452061623741,-1.2857353417468,90.7500736540522));
#14024=CARTESIAN_POINT('Ctrl Pts',(-1.61547660352134,-1.27429395107632,
90.7500736540522));
#14025=CARTESIAN_POINT('Ctrl Pts',(-1.66744198904932,-1.22002624687413,
90.7500736540522));
#14026=CARTESIAN_POINT('Ctrl Pts',(-1.71640398877985,-1.16288084511768,
90.7500736540522));
#14027=CARTESIAN_POINT('Ctrl Pts',(-1.76226853571781,-1.10322863632069,
90.7500736540522));
#14028=CARTESIAN_POINT('Ctrl Pts',(-1.79953220669005,-1.05476287289812,
90.7500736540522));
#14029=CARTESIAN_POINT('Ctrl Pts',(-1.83475096252,-1.00464114381801,90.7500736540523));
#14030=CARTESIAN_POINT('Ctrl Pts',(-1.86786104451265,-0.953040921544573,
90.7500736540523));
#14031=CARTESIAN_POINT('Ctrl Pts',(-1.88146828181041,-0.931834798610553,
90.7500736540523));
#14032=CARTESIAN_POINT('Ctrl Pts',(-1.89471921467165,-0.910378765130967,
90.7500736540522));
#14033=CARTESIAN_POINT('Ctrl Pts',(-1.90760870916851,-0.888684374343241,
90.7500736540522));
#14034=CARTESIAN_POINT('Ctrl Pts',(-1.91577328640956,-0.87494252206757,
90.7500736540522));
#14035=CARTESIAN_POINT('Ctrl Pts',(-1.92379338532837,-0.86110380603922,
90.7500736540523));
#14036=CARTESIAN_POINT('Ctrl Pts',(-1.93165776304693,-0.847189230573697,
90.7500736540523));
#14037=CARTESIAN_POINT('Ctrl Pts',(-1.97012662979234,-0.779125619114782,
90.7500736540523));
#14038=CARTESIAN_POINT('Ctrl Pts',(-2.00493023271791,-0.709154461979746,
90.7500736540523));
#14039=CARTESIAN_POINT('Ctrl Pts',(-2.03597045608216,-0.637659028599459,
90.7500736540523));
#14040=CARTESIAN_POINT('Ctrl Pts',(-2.06739142995637,-0.565286606597039,
90.7500736540523));
#14041=CARTESIAN_POINT('Ctrl Pts',(-2.0949567808205,-0.491351478981031,
90.7500736540523));
#14042=CARTESIAN_POINT('Ctrl Pts',(-2.11852959809477,-0.416210774009595,
90.7500736540523));
#14043=CARTESIAN_POINT('Ctrl Pts',(-2.14196667005475,-0.341502770759492,
90.7500736540523));
#14044=CARTESIAN_POINT('Ctrl Pts',(-2.16145761271948,-0.265602104107118,
90.7500736540523));
#14045=CARTESIAN_POINT('Ctrl Pts',(-2.17682448455395,-0.18883326108786,
90.7500736540523));
#14046=CARTESIAN_POINT('Ctrl Pts',(-2.18114611784962,-0.16724351975103,
90.7500736540523));
#14047=CARTESIAN_POINT('Ctrl Pts',(-2.1851412830939,-0.145584999209621,
90.7500736540523));
#14048=CARTESIAN_POINT('Ctrl Pts',(-2.18880530501091,-0.123864692850796,
90.7500736540523));
#14049=CARTESIAN_POINT('Ctrl Pts',(-2.19098529876454,-0.110941699140181,
90.7500736540523));
#14050=CARTESIAN_POINT('Ctrl Pts',(-2.19304836677221,-0.0979947967337072,
90.7500736540523));
#14051=CARTESIAN_POINT('Ctrl Pts',(-2.19499250099196,-0.085031936846214,
90.7500736540523));
#14052=CARTESIAN_POINT('Ctrl Pts',(-2.20701790455726,-0.00485042472448606,
90.7500736540523));
#14053=CARTESIAN_POINT('Ctrl Pts',(-2.2144573386233,0.0756695034371889,
90.7500736540523));
#14054=CARTESIAN_POINT('Ctrl Pts',(-2.21718406235607,0.156150190113027,
90.7500736540523));
#14055=CARTESIAN_POINT('Ctrl Pts',(-2.21836944509456,0.191137385779644,
90.7500736540523));
#14056=CARTESIAN_POINT('Ctrl Pts',(-2.21866364274063,0.226117562255175,
90.7500736540523));
#14057=CARTESIAN_POINT('Ctrl Pts',(-2.21805357014175,0.261061209453445,
90.7500736540523));
#14058=CARTESIAN_POINT('Ctrl Pts',(-2.21668480419082,0.339461181152025,
90.7500736540523));
#14059=CARTESIAN_POINT('Ctrl Pts',(-2.21076796745135,0.417676800779223,
90.7500736540523));
#14060=CARTESIAN_POINT('Ctrl Pts',(-2.20054345997488,0.49544826966194,90.7500736540523));
#14061=CARTESIAN_POINT('Ctrl Pts',(-2.19031895249841,0.573219738544656,
90.7500736540523));
#14062=CARTESIAN_POINT('Ctrl Pts',(-2.17578648103929,0.650547822033016,
90.7500736540523));
#14063=CARTESIAN_POINT('Ctrl Pts',(-2.15713417814691,0.727175031660327,
90.7500736540523));
#14064=CARTESIAN_POINT('Ctrl Pts',(-2.1539803082068,0.740131729523996,90.7500736540523));
#14065=CARTESIAN_POINT('Ctrl Pts',(-2.15070853499987,0.753068378664176,
90.7500736540523));
#14066=CARTESIAN_POINT('Ctrl Pts',(-2.14731962968966,0.765983716177013,
90.7500736540523));
#14067=CARTESIAN_POINT('Ctrl Pts',(-2.14412530405667,0.778157497944161,
90.7500736540523));
#14068=CARTESIAN_POINT('Ctrl Pts',(-2.14082936994079,0.790302951605743,
90.7500736540523));
#14069=CARTESIAN_POINT('Ctrl Pts',(-2.13743320332618,0.802418155946092,
90.7500736540523));
#14070=CARTESIAN_POINT('Ctrl Pts',(-2.11559292525712,0.88032936045494,90.7500736540523));
#14071=CARTESIAN_POINT('Ctrl Pts',(-2.08960869205439,0.957000970977793,
90.7500736540522));
#14072=CARTESIAN_POINT('Ctrl Pts',(-2.05975308903368,1.0321622444044,90.7500736540522));
#14073=CARTESIAN_POINT('Ctrl Pts',(-2.02936458120719,1.10866510198154,90.7500736540522));
#14074=CARTESIAN_POINT('Ctrl Pts',(-1.99496506341364,1.18360404711025,90.7500736540523));
#14075=CARTESIAN_POINT('Ctrl Pts',(-1.9567873698184,1.25669491216257,90.7500736540523));
#14076=CARTESIAN_POINT('Ctrl Pts',(-1.91822311031008,1.33052585432081,90.7500736540523));
#14077=CARTESIAN_POINT('Ctrl Pts',(-1.87580347456082,1.40247202242494,90.7500736540523));
#14078=CARTESIAN_POINT('Ctrl Pts',(-1.82971715604818,1.47222861375008,90.7500736540523));
#14079=CARTESIAN_POINT('Ctrl Pts',(-1.81119809279695,1.50025920435988,90.7500736540523));
#14080=CARTESIAN_POINT('Ctrl Pts',(-1.79208641832787,1.52793603129552,90.7500736540522));
#14081=CARTESIAN_POINT('Ctrl Pts',(-1.77239225197708,1.55523825579694,90.7500736540522));
#14082=CARTESIAN_POINT('Ctrl Pts',(-1.76263940974474,1.56875872086315,90.7500736540522));
#14083=CARTESIAN_POINT('Ctrl Pts',(-1.75274156406399,1.58218996914953,90.7500736540522));
#14084=CARTESIAN_POINT('Ctrl Pts',(-1.74271568305835,1.59550888248852,90.7500736540522));
#14085=CARTESIAN_POINT('Ctrl Pts',(-1.69105993064107,1.66413113020107,90.7500736540522));
#14086=CARTESIAN_POINT('Ctrl Pts',(-1.63593306559914,1.72988154427594,90.7500736540522));
#14087=CARTESIAN_POINT('Ctrl Pts',(-1.5775910963695,1.79246237937079,90.7500736540522));
#14088=CARTESIAN_POINT('Ctrl Pts',(-1.51916579161454,1.85513260477654,90.7500736540522));
#14089=CARTESIAN_POINT('Ctrl Pts',(-1.45751575777673,1.91462512805355,90.7500736540522));
#14090=CARTESIAN_POINT('Ctrl Pts',(-1.39284891655045,1.9706235418493,90.7500736540522));
#14091=CARTESIAN_POINT('Ctrl Pts',(-1.3295666745946,2.02542295842457,90.7500736540522));
#14092=CARTESIAN_POINT('Ctrl Pts',(-1.2633948711054,2.07687707547168,90.7500736540522));
#14093=CARTESIAN_POINT('Ctrl Pts',(-1.19448888753409,2.12466016003287,90.7500736540522));
#14094=CARTESIAN_POINT('Ctrl Pts',(-1.15555458977215,2.15165927891728,90.7500736540522));
#14095=CARTESIAN_POINT('Ctrl Pts',(-1.11574669177119,2.17748577160815,90.7500736540522));
#14096=CARTESIAN_POINT('Ctrl Pts',(-1.07508846035166,2.2020751695659,90.7500736540522));
#14097=CARTESIAN_POINT('Origin',(-5.69858952725515E-16,8.58067791224701E-17,
90.7500736540522));
#14098=CARTESIAN_POINT('',(-2.4505,-3.00099698131059E-16,90.7500736540522));
#14099=CARTESIAN_POINT('Origin',(0.,0.,90.7500736540522));
#14100=CARTESIAN_POINT('',(1.11860366144128,2.18029266352253,90.7500736540522));
#14101=CARTESIAN_POINT('Origin',(0.,0.,90.7500736540522));
#14102=CARTESIAN_POINT('Ctrl Pts',(1.11860366144127,2.18029266352252,90.7500736540522));
#14103=CARTESIAN_POINT('Ctrl Pts',(1.15162264457275,2.15955585985248,90.7500736540522));
#14104=CARTESIAN_POINT('Ctrl Pts',(1.18407930231287,2.13798223312585,90.7500736540523));
#14105=CARTESIAN_POINT('Ctrl Pts',(1.2159377932849,2.11556938451728,90.7500736540523));
#14106=CARTESIAN_POINT('Ctrl Pts',(1.28560972406618,2.06655430598646,90.7500736540523));
#14107=CARTESIAN_POINT('Ctrl Pts',(1.35242359596798,2.01352759821736,90.7500736540523));
#14108=CARTESIAN_POINT('Ctrl Pts',(1.41621167348851,1.95685023476083,90.7500736540523));
#14109=CARTESIAN_POINT('Ctrl Pts',(1.4485350295639,1.92813009344868,90.7500736540523));
#14110=CARTESIAN_POINT('Ctrl Pts',(1.48008078664681,1.89847201623414,90.7500736540522));
#14111=CARTESIAN_POINT('Ctrl Pts',(1.51082285430447,1.8679203368343,90.7500736540522));
#14112=CARTESIAN_POINT('Ctrl Pts',(1.52957938642694,1.84927996552161,90.7500736540522));
#14113=CARTESIAN_POINT('Ctrl Pts',(1.54803668440887,1.83030691799242,90.7500736540522));
#14114=CARTESIAN_POINT('Ctrl Pts',(1.56618825539262,1.81101104547671,90.7500736540522));
#14115=CARTESIAN_POINT('Ctrl Pts',(1.57674283195666,1.79979109299882,90.7500736540522));
#14116=CARTESIAN_POINT('Ctrl Pts',(1.58719094483532,1.78846519805228,90.7500736540522));
#14117=CARTESIAN_POINT('Ctrl Pts',(1.59752636698703,1.7770412829028,90.7500736540522));
#14118=CARTESIAN_POINT('Ctrl Pts',(1.65450684340916,1.71405980829358,90.7500736540522));
#14119=CARTESIAN_POINT('Ctrl Pts',(1.70811520307835,1.64804892541984,90.7500736540522));
#14120=CARTESIAN_POINT('Ctrl Pts',(1.7581816725158,1.57936535303345,90.7500736540522));
#14121=CARTESIAN_POINT('Ctrl Pts',(1.79683292035112,1.52634172647561,90.7500736540522));
#14122=CARTESIAN_POINT('Ctrl Pts',(1.83337245026146,1.47172442149015,90.7500736540522));
#14123=CARTESIAN_POINT('Ctrl Pts',(1.86770238229061,1.41566979012823,90.7500736540522));
#14124=CARTESIAN_POINT('Ctrl Pts',(1.88400353449563,1.38905292771059,90.7500736540522));
#14125=CARTESIAN_POINT('Ctrl Pts',(1.89980622399855,1.36211192267649,90.7500736540522));
#14126=CARTESIAN_POINT('Ctrl Pts',(1.91509849671254,1.33486328413342,90.7500736540522));
#14127=CARTESIAN_POINT('Ctrl Pts',(1.9225163087319,1.32164580611193,90.7500736540522));
#14128=CARTESIAN_POINT('Ctrl Pts',(1.92981500217531,1.30835408931338,90.7500736540522));
#14129=CARTESIAN_POINT('Ctrl Pts',(1.93698997498754,1.29499590064715,90.7500736540522));
#14130=CARTESIAN_POINT('Ctrl Pts',(1.97632810621595,1.22175713131972,90.7500736540522));
#14131=CARTESIAN_POINT('Ctrl Pts',(2.011840092034,1.14673115001634,90.7500736540522));
#14132=CARTESIAN_POINT('Ctrl Pts',(2.04337087962439,1.0702496833273,90.7500736540522));
#14133=CARTESIAN_POINT('Ctrl Pts',(2.07458497279001,0.994536394535134,90.7500736540522));
#14134=CARTESIAN_POINT('Ctrl Pts',(2.1018976767583,0.917395750779118,90.7500736540522));
#14135=CARTESIAN_POINT('Ctrl Pts',(2.12510922745775,0.839138863226887,90.7500736540522));
#14136=CARTESIAN_POINT('Ctrl Pts',(2.14761632748849,0.763257005136517,90.7500736540522));
#14137=CARTESIAN_POINT('Ctrl Pts',(2.16626745954812,0.686324834641116,90.7500736540522));
#14138=CARTESIAN_POINT('Ctrl Pts',(2.18083222156942,0.608628635176532,90.7500736540522));
#14139=CARTESIAN_POINT('Ctrl Pts',(2.1893580477943,0.563147336271684,90.7500736540522));
#14140=CARTESIAN_POINT('Ctrl Pts',(2.19648271621353,0.517404343444855,90.7500736540522));
#14141=CARTESIAN_POINT('Ctrl Pts',(2.20215188602963,0.471459112307776,90.7500736540522));
#14142=CARTESIAN_POINT('Ctrl Pts',(2.20378351406345,0.458235742824217,90.7500736540522));
#14143=CARTESIAN_POINT('Ctrl Pts',(2.20529453685117,0.444994839301754,90.7500736540522));
#14144=CARTESIAN_POINT('Ctrl Pts',(2.20668212071864,0.431754073468555,90.7500736540522));
#14145=CARTESIAN_POINT('Ctrl Pts',(2.21482655469238,0.354037298563444,90.7500736540522));
#14146=CARTESIAN_POINT('Ctrl Pts',(2.21873982537425,0.276192904866269,90.7500736540522));
#14147=CARTESIAN_POINT('Ctrl Pts',(2.21824403489587,0.198499425861476,90.7500736540522));
#14148=CARTESIAN_POINT('Ctrl Pts',(2.21805504044083,0.168882808833148,90.7500736540522));
#14149=CARTESIAN_POINT('Ctrl Pts',(2.2172248263468,0.139288154592789,90.7500736540522));
#14150=CARTESIAN_POINT('Ctrl Pts',(2.2157415379887,0.109731156930863,90.7500736540522));
#14151=CARTESIAN_POINT('Ctrl Pts',(2.21175624551703,0.0303175488993252,
90.7500736540522));
#14152=CARTESIAN_POINT('Ctrl Pts',(2.20305993064706,-0.0488257888431539,
90.7500736540522));
#14153=CARTESIAN_POINT('Ctrl Pts',(2.18984154198201,-0.127374924856007,
90.7500736540522));
#14154=CARTESIAN_POINT('Ctrl Pts',(2.17698486180796,-0.20377463931855,90.7500736540522));
#14155=CARTESIAN_POINT('Ctrl Pts',(2.15984942904707,-0.279612912181562,
90.7500736540522));
#14156=CARTESIAN_POINT('Ctrl Pts',(2.13856952809271,-0.354565773154105,
90.7500736540522));
#14157=CARTESIAN_POINT('Ctrl Pts',(2.13517799014349,-0.3665115746377,90.7500736540522));
#14158=CARTESIAN_POINT('Ctrl Pts',(2.1316803732889,-0.378437229566964,90.7500736540522));
#14159=CARTESIAN_POINT('Ctrl Pts',(2.12807957002442,-0.390333378570073,
90.7500736540522));
#14160=CARTESIAN_POINT('Ctrl Pts',(2.10555064548884,-0.464763283085853,
90.7500736540522));
#14161=CARTESIAN_POINT('Ctrl Pts',(2.07904216588284,-0.537862381076858,
90.7500736540522));
#14162=CARTESIAN_POINT('Ctrl Pts',(2.04876132870682,-0.609341044688673,
90.7500736540522));
#14163=CARTESIAN_POINT('Ctrl Pts',(2.01842212874393,-0.680957475099535,
90.7500736540522));
#14164=CARTESIAN_POINT('Ctrl Pts',(1.98429535798103,-0.750948067942242,
90.7500736540522));
#14165=CARTESIAN_POINT('Ctrl Pts',(1.94654558957243,-0.818993232114188,
90.7500736540522));
#14166=CARTESIAN_POINT('Ctrl Pts',(1.9095059907965,-0.88575829282372,90.7500736540522));
#14167=CARTESIAN_POINT('Ctrl Pts',(1.86897771992724,-0.950651078774011,
90.7500736540522));
#14168=CARTESIAN_POINT('Ctrl Pts',(1.8250843907989,-1.01333162280846,90.7500736540522));
#14169=CARTESIAN_POINT('Ctrl Pts',(1.80772089155411,-1.03812704390362,90.7500736540522));
#14170=CARTESIAN_POINT('Ctrl Pts',(1.78983050709486,-1.06257580205391,90.7500736540522));
#14171=CARTESIAN_POINT('Ctrl Pts',(1.77141983903051,-1.08665482731573,90.7500736540522));
#14172=CARTESIAN_POINT('Ctrl Pts',(1.75998908115404,-1.10160493704056,90.7500736540522));
#14173=CARTESIAN_POINT('Ctrl Pts',(1.74835324490105,-1.11641784806647,90.7500736540522));
#14174=CARTESIAN_POINT('Ctrl Pts',(1.73653761305467,-1.13105898801412,90.7500736540522));
#14175=CARTESIAN_POINT('Ctrl Pts',(1.6894484845429,-1.18940868352909,90.7500736540522));
#14176=CARTESIAN_POINT('Ctrl Pts',(1.63945635267561,-1.24510343119323,90.7500736540522));
#14177=CARTESIAN_POINT('Ctrl Pts',(1.58671285136659,-1.29785677787551,90.7500736540522));
#14178=CARTESIAN_POINT('Ctrl Pts',(1.5348340863669,-1.34974522683233,90.7500736540522));
#14179=CARTESIAN_POINT('Ctrl Pts',(1.48029277358304,-1.39878848761766,90.7500736540522));
#14180=CARTESIAN_POINT('Ctrl Pts',(1.4232065330979,-1.44467201634083,90.7500736540522));
#14181=CARTESIAN_POINT('Ctrl Pts',(1.36795223109561,-1.48908310965255,90.7500736540522));
#14182=CARTESIAN_POINT('Ctrl Pts',(1.31031313664948,-1.53053432787586,90.7500736540522));
#14183=CARTESIAN_POINT('Ctrl Pts',(1.2503797473084,-1.56869474102025,90.7500736540522));
#14184=CARTESIAN_POINT('Ctrl Pts',(1.22092070607232,-1.58745171766992,90.7500736540522));
#14185=CARTESIAN_POINT('Ctrl Pts',(1.19090716214411,-1.60541289253108,90.7500736540522));
#14186=CARTESIAN_POINT('Ctrl Pts',(1.16034898466942,-1.62253437445148,90.7500736540522));
#14187=CARTESIAN_POINT('Ctrl Pts',(1.42641864629319,-1.99638045030102,90.4850961099509));
#14188=CARTESIAN_POINT('Ctrl Pts',(2.09188384541137,-1.52093832304627,90.5275363992458));
#14189=CARTESIAN_POINT('Ctrl Pts',(2.89741194200073,0.140230266537244,90.6123989000352));
#14190=CARTESIAN_POINT('Ctrl Pts',(1.44681938588662,2.51760976119924,90.7396836123194));
#14191=CARTESIAN_POINT('Ctrl Pts',(-1.3349513413323,2.57619747619588,90.8669502468028));
#14192=CARTESIAN_POINT('Ctrl Pts',(-2.88927286053599,0.270948746763703,
90.9942168812865));
#14193=CARTESIAN_POINT('Ctrl Pts',(-1.78994692638796,-2.28455322460687,
91.12148351577));
#14194=CARTESIAN_POINT('Ctrl Pts',(0.953961383261563,-2.74071497093679,
91.2487501502538));
#14195=CARTESIAN_POINT('Ctrl Pts',(2.82139223301607,-0.679478173895668,
91.3760167847374));
#14196=CARTESIAN_POINT('Ctrl Pts',(2.09705047335778,2.00611323769679,91.5032834192211));
#14197=CARTESIAN_POINT('Ctrl Pts',(-0.553753233031221,2.84873431719668,
91.6305500537047));
#14198=CARTESIAN_POINT('Ctrl Pts',(-2.69584252699719,1.07443894056368,91.7578166881883));
#14199=CARTESIAN_POINT('Ctrl Pts',(-2.36143656052974,-1.68689575431721,
91.885083322672));
#14200=CARTESIAN_POINT('Ctrl Pts',(0.142278221441695,-2.89857479605069,
92.0123499571555));
#14201=CARTESIAN_POINT('Ctrl Pts',(2.51528897469708,-1.44751790783786,92.1396165916392));
#14202=CARTESIAN_POINT('Ctrl Pts',(2.57766098092973,1.33328598602465,92.2668832261228));
#14203=CARTESIAN_POINT('Ctrl Pts',(0.272095583979841,2.88928179142881,92.3941498606065));
#14204=CARTESIAN_POINT('Ctrl Pts',(-2.28342689430216,1.79107451910037,92.52141649509));
#14205=CARTESIAN_POINT('Ctrl Pts',(-2.74130709999466,-0.952481874254109,
92.6486831295738));
#14206=CARTESIAN_POINT('Ctrl Pts',(-0.680918780824363,-2.82105223071625,
92.7759497640573));
#14207=CARTESIAN_POINT('Ctrl Pts',(2.00498727946868,-2.09809728512521,92.9032163985409));
#14208=CARTESIAN_POINT('Ctrl Pts',(2.8490361412242,0.552249279642321,93.0304830330245));
#14209=CARTESIAN_POINT('Ctrl Pts',(1.0758525501431,2.6952787356818,93.1577496675082));
#14210=CARTESIAN_POINT('Ctrl Pts',(-1.68564991556116,2.36232312597231,93.2850163019919));
#14211=CARTESIAN_POINT('Ctrl Pts',(-2.89865056198864,-0.140751934076159,
93.4122829364753));
#14212=CARTESIAN_POINT('Ctrl Pts',(-1.4488410761114,-2.51452693783455,93.5395495709592));
#14213=CARTESIAN_POINT('Ctrl Pts',(1.33192866603113,-2.57836231230752,93.6668162054426));
#14214=CARTESIAN_POINT('Ctrl Pts',(2.88913831737708,-0.27361646611042,93.7940828399263));
#14215=CARTESIAN_POINT('Ctrl Pts',(1.7922761444701,2.28248382498065,93.9213494744098));
#14216=CARTESIAN_POINT('Ctrl Pts',(-0.951038737978436,2.74180806978394,
94.0486161088936));
#14217=CARTESIAN_POINT('Ctrl Pts',(-2.82069343799303,0.682403641351875,
94.1758827433772));
#14218=CARTESIAN_POINT('Ctrl Pts',(-2.09915236596629,-2.00388261960105,
94.3031493778608));
#14219=CARTESIAN_POINT('Ctrl Pts',(0.550749519047719,-2.84932641895892,
94.4304160123444));
#14220=CARTESIAN_POINT('Ctrl Pts',(2.69471207121477,-1.07727117779746,94.5576826468281));
#14221=CARTESIAN_POINT('Ctrl Pts',(2.36321006187575,1.68440628057551,94.6849492813116));
#14222=CARTESIAN_POINT('Ctrl Pts',(-0.13922607033149,2.89872409491546,94.8122159157953));
#14223=CARTESIAN_POINT('Ctrl Pts',(-2.51376406076365,1.45016478372299,94.9394825502789));
#14224=CARTESIAN_POINT('Ctrl Pts',(-2.57906282911108,-1.33057192336286,
95.0667491847626));
#14225=CARTESIAN_POINT('Ctrl Pts',(-0.275137668947571,-2.88899259322745,
95.1940158192461));
#14226=CARTESIAN_POINT('Ctrl Pts',(2.28154102460352,-1.79347998828841,95.3212824537299));
#14227=CARTESIAN_POINT('Ctrl Pts',(2.74230639971675,0.949600746334372,95.4485490882135));
#14228=CARTESIAN_POINT('Ctrl Pts',(0.683892160422594,2.82032291874159,95.5758157226971));
#14229=CARTESIAN_POINT('Ctrl Pts',(-2.00278524276074,2.100229102182,95.7030823571806));
#14230=CARTESIAN_POINT('Ctrl Pts',(-2.84959995676592,-0.549294827686968,
95.8303489916643));
#14231=CARTESIAN_POINT('Ctrl Pts',(-1.07872195676699,-2.69405267444053,
95.9576156261479));
#14232=CARTESIAN_POINT('Ctrl Pts',(1.68322819081122,-2.36428346291339,96.0848822606317));
#14233=CARTESIAN_POINT('Ctrl Pts',(2.89866254755287,0.138080851014796,96.2121488951151));
#14234=CARTESIAN_POINT('Ctrl Pts',(1.4517612276782,2.51222567813746,96.3394155295989));
#14235=CARTESIAN_POINT('Ctrl Pts',(-1.32976764136635,2.58134911723269,96.4666821640825));
#14236=CARTESIAN_POINT('Ctrl Pts',(-2.88770364074214,0.273366351750177,
96.593948798566));
#14237=CARTESIAN_POINT('Ctrl Pts',(-2.15978309563236,-1.42262140700734,
96.6787932215551));
#14238=CARTESIAN_POINT('Ctrl Pts',(-1.51734708719904,-1.92817607117051,
96.7212154330496));
#14239=CARTESIAN_POINT('Ctrl Pts',(1.33678351078741,-1.87092931949251,90.5741137937452));
#14240=CARTESIAN_POINT('Ctrl Pts',(1.96043134902606,-1.42536363812717,90.6165540830401));
#14241=CARTESIAN_POINT('Ctrl Pts',(2.71534063165141,0.131418296099438,90.7014165838296));
#14242=CARTESIAN_POINT('Ctrl Pts',(1.35590228238173,2.35940495037305,90.8287012961136));
#14243=CARTESIAN_POINT('Ctrl Pts',(-1.25106394636245,2.4143110549348,90.9559679305972));
#14244=CARTESIAN_POINT('Ctrl Pts',(-2.70771300429019,0.253922519790013,
91.083234565081));
#14245=CARTESIAN_POINT('Ctrl Pts',(-1.67746793173104,-2.14099352115659,
91.2105011995644));
#14246=CARTESIAN_POINT('Ctrl Pts',(0.894015126895566,-2.56849038705249,
91.3377678340482));
#14247=CARTESIAN_POINT('Ctrl Pts',(2.64409794723359,-0.636780247625117,
91.4650344685317));
#14248=CARTESIAN_POINT('Ctrl Pts',(1.9652733097387,1.880050505435,91.5923011030154));
#14249=CARTESIAN_POINT('Ctrl Pts',(-0.518955772826602,2.66972187424701,
91.7195677374989));
#14250=CARTESIAN_POINT('Ctrl Pts',(-2.5264376956473,1.00692195999112,91.8468343719827));
#14251=CARTESIAN_POINT('Ctrl Pts',(-2.21304556280866,-1.58089242218517,
91.9741010064663));
#14252=CARTESIAN_POINT('Ctrl Pts',(0.133337558970979,-2.71643041277807,
92.1013676409498));
#14253=CARTESIAN_POINT('Ctrl Pts',(2.35723000044779,-1.35655690970924,92.2286342754335));
#14254=CARTESIAN_POINT('Ctrl Pts',(2.41568259406972,1.24950324080055,92.3559009099171));
#14255=CARTESIAN_POINT('Ctrl Pts',(0.254997290569318,2.70772137397204,92.4831675444008));
#14256=CARTESIAN_POINT('Ctrl Pts',(-2.13993796864894,1.67852466731756,92.6104341788844));
#14257=CARTESIAN_POINT('Ctrl Pts',(-2.56904530714055,-0.892628589184238,
92.737700813368));
#14258=CARTESIAN_POINT('Ctrl Pts',(-0.638130327836708,-2.64377931043703,
92.8649674478516));
#14259=CARTESIAN_POINT('Ctrl Pts',(1.87899530162292,-1.96625434059751,92.9922340823353));
#14260=CARTESIAN_POINT('Ctrl Pts',(2.67000473186684,0.517546326801413,93.1195007168189));
#14261=CARTESIAN_POINT('Ctrl Pts',(1.00824673934771,2.52590933257809,93.2467673513025));
#14262=CARTESIAN_POINT('Ctrl Pts',(-1.57972487105247,2.21387641710795,93.3740339857862));
#14263=CARTESIAN_POINT('Ctrl Pts',(-2.71650141763824,-0.131907182420398,
93.5013006202697));
#14264=CARTESIAN_POINT('Ctrl Pts',(-1.35779693102744,-2.35651584944093,
93.6285672547535));
#14265=CARTESIAN_POINT('Ctrl Pts',(1.24823121383224,-2.41633985428142,93.7558338892369));
#14266=CARTESIAN_POINT('Ctrl Pts',(2.7075869157279,-0.256422601546072,93.8831005237207));
#14267=CARTESIAN_POINT('Ctrl Pts',(1.67965078340178,2.13905416113437,94.0103671582042));
#14268=CARTESIAN_POINT('Ctrl Pts',(-0.891276138568037,2.56951479634378,
94.1376337926878));
#14269=CARTESIAN_POINT('Ctrl Pts',(-2.64344306399391,0.63952188078237,94.2649004271716));
#14270=CARTESIAN_POINT('Ctrl Pts',(-1.96724312090724,-1.87796005779748,
94.3921670616551));
#14271=CARTESIAN_POINT('Ctrl Pts',(0.516140810098302,-2.67027676875468,
94.5194336961388));
#14272=CARTESIAN_POINT('Ctrl Pts',(2.52537827690404,-1.00957622144696,94.6467003306223));
#14273=CARTESIAN_POINT('Ctrl Pts',(2.21470761858861,1.5785593852068,94.7739669651061));
#14274=CARTESIAN_POINT('Ctrl Pts',(-0.130477202870647,2.71657032980812,
94.9012335995896));
#14275=CARTESIAN_POINT('Ctrl Pts',(-2.35580091102381,1.35903745779204,95.0285002340733));
#14276=CARTESIAN_POINT('Ctrl Pts',(-2.41699635110614,-1.24695972791046,
95.1557668685569));
#14277=CARTESIAN_POINT('Ctrl Pts',(-0.257848213076424,-2.70745034878043,
95.2830335030406));
#14278=CARTESIAN_POINT('Ctrl Pts',(2.13817060566391,-1.68077897852883,95.4103001375242));
#14279=CARTESIAN_POINT('Ctrl Pts',(2.56998181157724,0.889928509298448,95.5375667720078));
#14280=CARTESIAN_POINT('Ctrl Pts',(0.640916862370981,2.6430958279093,95.6648334064913));
#14281=CARTESIAN_POINT('Ctrl Pts',(-1.87693163933909,1.96825219578325,95.7921000409751));
#14282=CARTESIAN_POINT('Ctrl Pts',(-2.67053311764,-0.51477753051037,95.9193666754586));
#14283=CARTESIAN_POINT('Ctrl Pts',(-1.01093583449556,-2.52476031615517,
96.0466333099423));
#14284=CARTESIAN_POINT('Ctrl Pts',(1.5774553257673,-2.21571356786677,96.173899944426));
#14285=CARTESIAN_POINT('Ctrl Pts',(2.71651265003811,0.129403948323132,96.3011665789095));
#14286=CARTESIAN_POINT('Ctrl Pts',(1.360533582342,2.35435919927017,96.4284332133931));
#14287=CARTESIAN_POINT('Ctrl Pts',(-1.24620598642386,2.41913897050462,96.5556998478769));
#14288=CARTESIAN_POINT('Ctrl Pts',(-2.70624239315462,0.256188204194738,
96.6829664823604));
#14289=CARTESIAN_POINT('Ctrl Pts',(-2.02406385854639,-1.33322488732366,
96.7678109053495));
#14290=CARTESIAN_POINT('Ctrl Pts',(-1.42199807299214,-1.80701085514679,
96.810233116844));
#14291=CARTESIAN_POINT('Ctrl Pts',(1.24714837528162,-1.74547818868399,90.6631314775395));
#14292=CARTESIAN_POINT('Ctrl Pts',(1.82897885264073,-1.32978895320807,90.7055717668344));
#14293=CARTESIAN_POINT('Ctrl Pts',(2.53326932130208,0.122606325661629,90.7904342676238));
#14294=CARTESIAN_POINT('Ctrl Pts',(1.26498517887684,2.20120013954685,90.9177189799079));
#14295=CARTESIAN_POINT('Ctrl Pts',(-1.16717655139261,2.25242463367372,91.0449856143915));
#14296=CARTESIAN_POINT('Ctrl Pts',(-2.52615314804439,0.236896292816323,
91.1722522488752));
#14297=CARTESIAN_POINT('Ctrl Pts',(-1.56498893707412,-1.9974338177063,91.2995188833588));
#14298=CARTESIAN_POINT('Ctrl Pts',(0.83406887052957,-2.39626580316819,91.4267855178424));
#14299=CARTESIAN_POINT('Ctrl Pts',(2.46680366145111,-0.594082321354566,
91.554052152326));
#14300=CARTESIAN_POINT('Ctrl Pts',(1.83349614611961,1.75398777317319,91.6813187868096));
#14301=CARTESIAN_POINT('Ctrl Pts',(-0.484158312621983,2.49070943129734,
91.8085854212933));
#14302=CARTESIAN_POINT('Ctrl Pts',(-2.3570328642974,0.939404979418549,91.9358520557769));
#14303=CARTESIAN_POINT('Ctrl Pts',(-2.06465456508757,-1.47488909005313,
92.0631186902605));
#14304=CARTESIAN_POINT('Ctrl Pts',(0.124396896500263,-2.53428602950544,
92.1903853247442));
#14305=CARTESIAN_POINT('Ctrl Pts',(2.19917102619849,-1.26559591158063,92.3176519592278));
#14306=CARTESIAN_POINT('Ctrl Pts',(2.25370420720971,1.16572049557646,92.4449185937114));
#14307=CARTESIAN_POINT('Ctrl Pts',(0.237898997158793,2.52616095651527,92.572185228195));
#14308=CARTESIAN_POINT('Ctrl Pts',(-1.99644904299573,1.56597481553477,92.6994518626787));
#14309=CARTESIAN_POINT('Ctrl Pts',(-2.39678351428644,-0.832775304114368,
92.8267184971623));
#14310=CARTESIAN_POINT('Ctrl Pts',(-0.595341874849054,-2.4665063901578,
92.9539851316459));
#14311=CARTESIAN_POINT('Ctrl Pts',(1.75300332377717,-1.8344113960698,93.0812517661295));
#14312=CARTESIAN_POINT('Ctrl Pts',(2.49097332250947,0.482843373960504,93.2085184006132));
#14313=CARTESIAN_POINT('Ctrl Pts',(0.940640928552308,2.35653992947437,93.3357850350967));
#14314=CARTESIAN_POINT('Ctrl Pts',(-1.47379982654378,2.0654297082436,93.4630516695805));
#14315=CARTESIAN_POINT('Ctrl Pts',(-2.53435227328783,-0.123062430764635,
93.590318304064));
#14316=CARTESIAN_POINT('Ctrl Pts',(-1.26675278594347,-2.19850476104731,
93.7175849385477));
#14317=CARTESIAN_POINT('Ctrl Pts',(1.16453376163335,-2.25431739625531,93.8448515730313));
#14318=CARTESIAN_POINT('Ctrl Pts',(2.52603551407873,-0.239228736981724,
93.9721182075149));
#14319=CARTESIAN_POINT('Ctrl Pts',(1.56702542233345,1.99562449728809,94.0993848419986));
#14320=CARTESIAN_POINT('Ctrl Pts',(-0.831513539157641,2.39722152290362,
94.2266514764821));
#14321=CARTESIAN_POINT('Ctrl Pts',(-2.4661926899948,0.596640120212867,94.3539181109658));
#14322=CARTESIAN_POINT('Ctrl Pts',(-1.8353338758482,-1.75203749599391,94.4811847454494));
#14323=CARTESIAN_POINT('Ctrl Pts',(0.481532101148887,-2.49122711855045,
94.6084513799331));
#14324=CARTESIAN_POINT('Ctrl Pts',(2.3560444825933,-0.94188126509646,94.7357180144167));
#14325=CARTESIAN_POINT('Ctrl Pts',(2.06620517530148,1.47271248983809,94.8629846489003));
#14326=CARTESIAN_POINT('Ctrl Pts',(-0.121728335409802,2.53441656470078,
94.9902512833839));
#14327=CARTESIAN_POINT('Ctrl Pts',(-2.19783776128397,1.26791013186111,95.1175179178676));
#14328=CARTESIAN_POINT('Ctrl Pts',(-2.25492987310121,-1.16334753245806,
95.2447845523511));
#14329=CARTESIAN_POINT('Ctrl Pts',(-0.240558757205277,-2.52590810433341,
95.3720511868348));
#14330=CARTESIAN_POINT('Ctrl Pts',(1.99480018672429,-1.56807796876924,95.4993178213184));
#14331=CARTESIAN_POINT('Ctrl Pts',(2.39765722343773,0.830256272262522,95.6265844558021));
#14332=CARTESIAN_POINT('Ctrl Pts',(0.597941564319369,2.46586873707703,95.7538510902856));
#14333=CARTESIAN_POINT('Ctrl Pts',(-1.75107803591743,1.83627528938449,95.8811177247694));
#14334=CARTESIAN_POINT('Ctrl Pts',(-2.49146627851409,-0.480260233333773,
96.0083843592529));
#14335=CARTESIAN_POINT('Ctrl Pts',(-0.943149712224129,-2.3554679578698,
96.1356509937365));
#14336=CARTESIAN_POINT('Ctrl Pts',(1.47168246072336,-2.06714367282014,96.2629176282202));
#14337=CARTESIAN_POINT('Ctrl Pts',(2.53436275252335,0.120727045631471,96.3901842627038));
#14338=CARTESIAN_POINT('Ctrl Pts',(1.2693059370058,2.19649272040287,96.5174508971874));
#14339=CARTESIAN_POINT('Ctrl Pts',(-1.16264433148138,2.25692882377654,96.6447175316711));
#14340=CARTESIAN_POINT('Ctrl Pts',(-2.52478114556709,0.239010056639298,
96.7719841661547));
#14341=CARTESIAN_POINT('Ctrl Pts',(-1.88834462146043,-1.24382836763997,
96.8568285891438));
#14342=CARTESIAN_POINT('Ctrl Pts',(-1.32664905878525,-1.68584563912308,
96.8992508006383));
#14343=CARTESIAN_POINT('Ctrl Pts',(1.15751323977584,-1.62002705787548,90.7521491613338));
#14344=CARTESIAN_POINT('Ctrl Pts',(1.69752635625542,-1.23421426828898,90.7945894506287));
#14345=CARTESIAN_POINT('Ctrl Pts',(2.35119801095275,0.113794355223823,90.8794519514181));
#14346=CARTESIAN_POINT('Ctrl Pts',(1.17406807537195,2.04299532872065,91.0067366637022));
#14347=CARTESIAN_POINT('Ctrl Pts',(-1.08328915642277,2.09053821241265,91.1340032981858));
#14348=CARTESIAN_POINT('Ctrl Pts',(-2.34459329179859,0.219870065842631,
91.2612699326695));
#14349=CARTESIAN_POINT('Ctrl Pts',(-1.45250994241719,-1.85387411425601,
91.3885365671531));
#14350=CARTESIAN_POINT('Ctrl Pts',(0.774122614163573,-2.2240412192839,91.5158032016367));
#14351=CARTESIAN_POINT('Ctrl Pts',(2.28950937566864,-0.551384395084015,
91.6430698361204));
#14352=CARTESIAN_POINT('Ctrl Pts',(1.70171898250053,1.6279250409114,91.7703364706039));
#14353=CARTESIAN_POINT('Ctrl Pts',(-0.449360852417364,2.31169698834768,
91.8976031050876));
#14354=CARTESIAN_POINT('Ctrl Pts',(-2.18762803294751,0.871887998845985,
92.0248697395712));
#14355=CARTESIAN_POINT('Ctrl Pts',(-1.9162635673665,-1.3688857579211,92.1521363740549));
#14356=CARTESIAN_POINT('Ctrl Pts',(0.115456234029549,-2.3521416462328,92.2794030085384));
#14357=CARTESIAN_POINT('Ctrl Pts',(2.04111205194919,-1.17463491345201,92.4066696430221));
#14358=CARTESIAN_POINT('Ctrl Pts',(2.0917258203497,1.08193775035237,92.5339362775058));
#14359=CARTESIAN_POINT('Ctrl Pts',(0.220800703748267,2.3446005390585,92.6612029119892));
#14360=CARTESIAN_POINT('Ctrl Pts',(-1.85296011734251,1.45342496375197,92.7884695464731));
#14361=CARTESIAN_POINT('Ctrl Pts',(-2.22452172143234,-0.772922019044498,
92.9157361809566));
#14362=CARTESIAN_POINT('Ctrl Pts',(-0.552553421861399,-2.28923346987856,
93.0430028154402));
#14363=CARTESIAN_POINT('Ctrl Pts',(1.62701134593142,-1.7025684515421,93.1702694499238));
#14364=CARTESIAN_POINT('Ctrl Pts',(2.31194191315208,0.448140421119597,93.2975360844075));
#14365=CARTESIAN_POINT('Ctrl Pts',(0.873035117756911,2.18717052637064,93.4248027188911));
#14366=CARTESIAN_POINT('Ctrl Pts',(-1.36787478203509,1.91698299937924,93.5520693533747));
#14367=CARTESIAN_POINT('Ctrl Pts',(-2.35220312893742,-0.114217679108873,
93.6793359878583));
#14368=CARTESIAN_POINT('Ctrl Pts',(-1.1757086408595,-2.04049367265369,93.806602622342));
#14369=CARTESIAN_POINT('Ctrl Pts',(1.08083630943445,-2.0922949382292,93.9338692568256));
#14370=CARTESIAN_POINT('Ctrl Pts',(2.34448411242956,-0.222034872417374,
94.0611358913091));
#14371=CARTESIAN_POINT('Ctrl Pts',(1.45440006126512,1.85219483344182,94.188402525793));
#14372=CARTESIAN_POINT('Ctrl Pts',(-0.771750939747243,2.22492824946345,
94.3156691602764));
#14373=CARTESIAN_POINT('Ctrl Pts',(-2.28894231599568,0.553758359643362,
94.4429357947601));
#14374=CARTESIAN_POINT('Ctrl Pts',(-1.70342463078915,-1.62611493419034,
94.5702024292437));
#14375=CARTESIAN_POINT('Ctrl Pts',(0.446923392199468,-2.31217746834622,
94.6974690637273));
#14376=CARTESIAN_POINT('Ctrl Pts',(2.18671068828257,-0.87418630874596,94.824735698211));
#14377=CARTESIAN_POINT('Ctrl Pts',(1.91770273201434,1.36686559446937,94.9520023326946));
#14378=CARTESIAN_POINT('Ctrl Pts',(-0.112979467948959,2.35226279959343,
95.0792689671782));
#14379=CARTESIAN_POINT('Ctrl Pts',(-2.03987461154412,1.17678280593016,95.2065356016618));
#14380=CARTESIAN_POINT('Ctrl Pts',(-2.09286339509628,-1.07973533700565,
95.3338022361456));
#14381=CARTESIAN_POINT('Ctrl Pts',(-0.223269301334131,-2.34436585988639,
95.4610688706291));
#14382=CARTESIAN_POINT('Ctrl Pts',(1.85142976778467,-1.45537695900965,95.5883355051127));
#14383=CARTESIAN_POINT('Ctrl Pts',(2.22533263529822,0.770584035226599,95.7156021395964));
#14384=CARTESIAN_POINT('Ctrl Pts',(0.554966266267755,2.28864164624474,95.84286877408));
#14385=CARTESIAN_POINT('Ctrl Pts',(-1.62522443249577,1.70429838298573,95.9701354085636));
#14386=CARTESIAN_POINT('Ctrl Pts',(-2.31239943938818,-0.445742936157174,
96.0974020430472));
#14387=CARTESIAN_POINT('Ctrl Pts',(-0.875363589952698,-2.18617559958444,
96.2246686775309));
#14388=CARTESIAN_POINT('Ctrl Pts',(1.36590959567943,-1.91857377777351,96.3519353120145));
#14389=CARTESIAN_POINT('Ctrl Pts',(2.3522128550086,0.112050142939805,96.4792019464981));
#14390=CARTESIAN_POINT('Ctrl Pts',(1.17807829166959,2.03862624153558,96.6064685809818));
#14391=CARTESIAN_POINT('Ctrl Pts',(-1.0790826765389,2.09471867704846,96.7337352154654));
#14392=CARTESIAN_POINT('Ctrl Pts',(-2.34331989797958,0.221831909083859,
96.861001849949));
#14393=CARTESIAN_POINT('Ctrl Pts',(-1.75262538437446,-1.15443184795629,
96.9458462729381));
#14394=CARTESIAN_POINT('Ctrl Pts',(-1.23130004457835,-1.56468042309936,
96.9882684844326));
#14395=CARTESIAN_POINT('',(-0.793252505200376,1.83204963892414,96.723977388184));
#14396=CARTESIAN_POINT('Ctrl Pts',(-0.794009102248012,1.83356035954796,
96.7230113585668));
#14397=CARTESIAN_POINT('Ctrl Pts',(-0.837291874002563,1.82051106939911,
96.7230113585668));
#14398=CARTESIAN_POINT('Ctrl Pts',(-0.880023176065944,1.8059130308115,96.7230113585668));
#14399=CARTESIAN_POINT('Ctrl Pts',(-0.922118158570995,1.7897642254726,96.7230113585668));
#14400=CARTESIAN_POINT('Ctrl Pts',(-0.989542432506282,1.76389839990142,
96.7230113585668));
#14401=CARTESIAN_POINT('Ctrl Pts',(-1.05533499621115,1.73405720162925,96.7230113585668));
#14402=CARTESIAN_POINT('Ctrl Pts',(-1.11933937792182,1.70056771355782,96.7230113585668));
#14403=CARTESIAN_POINT('Ctrl Pts',(-1.17096240512104,1.67355661357696,96.7230113585668));
#14404=CARTESIAN_POINT('Ctrl Pts',(-1.2214222453498,1.64417097646139,96.7230113585668));
#14405=CARTESIAN_POINT('Ctrl Pts',(-1.27063140042659,1.612558416562,96.7230113585668));
#14406=CARTESIAN_POINT('Ctrl Pts',(-1.28395910376886,1.60399653779023,96.7230113585668));
#14407=CARTESIAN_POINT('Ctrl Pts',(-1.29718718705757,1.59527619216679,96.7230113585668));
#14408=CARTESIAN_POINT('Ctrl Pts',(-1.31031056320797,1.58640318349424,96.7230113585668));
#14409=CARTESIAN_POINT('Ctrl Pts',(-1.37255435913609,1.54431875836207,96.7230113585668));
#14410=CARTESIAN_POINT('Ctrl Pts',(-1.43246940936956,1.4987878264592,96.7230113585668));
#14411=CARTESIAN_POINT('Ctrl Pts',(-1.48988552335752,1.45015309019523,96.7230113585668));
#14412=CARTESIAN_POINT('Ctrl Pts',(-1.53653455176071,1.41063869195792,96.7230113585668));
#14413=CARTESIAN_POINT('Ctrl Pts',(-1.58153400798001,1.36907421455917,96.7230113585668));
#14414=CARTESIAN_POINT('Ctrl Pts',(-1.62478412958448,1.32561968798594,96.7230113585668));
#14415=CARTESIAN_POINT('Ctrl Pts',(-1.64255840351002,1.30776141083055,96.7230113585668));
#14416=CARTESIAN_POINT('Ctrl Pts',(-1.66003711651052,1.28958369174573,96.7230113585668));
#14417=CARTESIAN_POINT('Ctrl Pts',(-1.67721281325249,1.27109674069572,96.7230113585668));
#14418=CARTESIAN_POINT('Ctrl Pts',(-1.68809273408154,1.25938620767827,96.7230113585668));
#14419=CARTESIAN_POINT('Ctrl Pts',(-1.69885185685385,1.24755050758685,96.7230113585668));
#14420=CARTESIAN_POINT('Ctrl Pts',(-1.70947475987798,1.23560780147555,96.7230113585668));
#14421=CARTESIAN_POINT('Ctrl Pts',(-1.76143601470801,1.1771908137463,96.7230113585668));
#14422=CARTESIAN_POINT('Ctrl Pts',(-1.81021688338235,1.11613601970109,96.7230113585668));
#14423=CARTESIAN_POINT('Ctrl Pts',(-1.85564060628833,1.05279736816488,96.7230113585668));
#14424=CARTESIAN_POINT('Ctrl Pts',(-1.90162151964286,0.988681772569438,
96.7230113585668));
#14425=CARTESIAN_POINT('Ctrl Pts',(-1.94416322520855,0.922225295514363,
96.7230113585668));
#14426=CARTESIAN_POINT('Ctrl Pts',(-1.98305655594857,0.853748149314053,
96.7230113585668));
#14427=CARTESIAN_POINT('Ctrl Pts',(-2.02172591850317,0.785665330415768,
96.7230113585668));
#14428=CARTESIAN_POINT('Ctrl Pts',(-2.05678954190754,0.715584254543018,
96.7230113585668));
#14429=CARTESIAN_POINT('Ctrl Pts',(-2.08800503716774,0.643784571834216,
96.7230113585668));
#14430=CARTESIAN_POINT('Ctrl Pts',(-2.09678381022876,0.623592256604256,
96.7230113585668));
#14431=CARTESIAN_POINT('Ctrl Pts',(-2.10525796886676,0.603263841203811,
96.7230113585668));
#14432=CARTESIAN_POINT('Ctrl Pts',(-2.1134214676846,0.582805175485435,96.7230113585668));
#14433=CARTESIAN_POINT('Ctrl Pts',(-2.11827851823285,0.570632848917964,
96.7230113585668));
#14434=CARTESIAN_POINT('Ctrl Pts',(-2.12302631749701,0.558412486391,96.7230113585668));
#14435=CARTESIAN_POINT('Ctrl Pts',(-2.12766122540615,0.546151436333585,
96.7230113585668));
#14436=CARTESIAN_POINT('Ctrl Pts',(-2.15633033981201,0.470310998136579,
96.7230113585668));
#14437=CARTESIAN_POINT('Ctrl Pts',(-2.1805880672175,0.393172356210161,96.7230113585668));
#14438=CARTESIAN_POINT('Ctrl Pts',(-2.20023085075779,0.315077935502425,
96.7230113585668));
#14439=CARTESIAN_POINT('Ctrl Pts',(-2.20877013194232,0.281128051770403,
96.7230113585668));
#14440=CARTESIAN_POINT('Ctrl Pts',(-2.21643679729787,0.246997034801529,
96.7230113585668));
#14441=CARTESIAN_POINT('Ctrl Pts',(-2.2232118307638,0.212710970602204,96.7230113585668));
#14442=CARTESIAN_POINT('Ctrl Pts',(-2.2384123422071,0.135786522357324,96.7230113585668));
#14443=CARTESIAN_POINT('Ctrl Pts',(-2.24912823491718,0.0580828721013101,
96.7230113585667));
#14444=CARTESIAN_POINT('Ctrl Pts',(-2.25553969589224,-0.0200953176490006,
96.7230113585667));
#14445=CARTESIAN_POINT('Ctrl Pts',(-2.2619511568673,-0.0982735073993113,
96.7230113585667));
#14446=CARTESIAN_POINT('Ctrl Pts',(-2.26405806090902,-0.176927046626794,
96.7230113585667));
#14447=CARTESIAN_POINT('Ctrl Pts',(-2.26198999100256,-0.255764556751951,
96.7230113585667));
#14448=CARTESIAN_POINT('Ctrl Pts',(-2.26164030555424,-0.26909502009201,
96.7230113585667));
#14449=CARTESIAN_POINT('Ctrl Pts',(-2.26117114012459,-0.28243075742817,
96.7230113585667));
#14450=CARTESIAN_POINT('Ctrl Pts',(-2.26058298212319,-0.295770371599199,
96.7230113585667));
#14451=CARTESIAN_POINT('Ctrl Pts',(-2.26002859528514,-0.308344044835706,
96.7230113585667));
#14452=CARTESIAN_POINT('Ctrl Pts',(-2.25936891052518,-0.320911461615806,
96.7230113585667));
#14453=CARTESIAN_POINT('Ctrl Pts',(-2.25860486758928,-0.333470453701026,
96.7230113585667));
#14454=CARTESIAN_POINT('Ctrl Pts',(-2.25370545505801,-0.414004780126182,
96.7230113585667));
#14455=CARTESIAN_POINT('Ctrl Pts',(-2.2445184297719,-0.494203504147783,
96.7230113585667));
#14456=CARTESIAN_POINT('Ctrl Pts',(-2.23125141378542,-0.573747205190449,
96.7230113585667));
#14457=CARTESIAN_POINT('Ctrl Pts',(-2.21758819715782,-0.65566636619959,
96.7230113585667));
#14458=CARTESIAN_POINT('Ctrl Pts',(-2.199597743887,-0.736891642756019,96.7230113585667));
#14459=CARTESIAN_POINT('Ctrl Pts',(-2.17745214020847,-0.817087333965471,
96.7230113585667));
#14460=CARTESIAN_POINT('Ctrl Pts',(-2.15530653652994,-0.897283025174922,
96.7230113585667));
#14461=CARTESIAN_POINT('Ctrl Pts',(-2.1290055920952,-0.976450102162561,
96.7230113585667));
#14462=CARTESIAN_POINT('Ctrl Pts',(-2.09866874566655,-1.05425199061378,
96.7230113585667));
#14463=CARTESIAN_POINT('Ctrl Pts',(-2.08661076762519,-1.08517588590817,
96.7230113585667));
#14464=CARTESIAN_POINT('Ctrl Pts',(-2.07391462100506,-1.11588401593709,
96.7230113585667));
#14465=CARTESIAN_POINT('Ctrl Pts',(-2.06058559778188,-1.14635467735089,
96.7230113585667));
#14466=CARTESIAN_POINT('Ctrl Pts',(-2.05390436829635,-1.16162822576271,
96.7230113585667));
#14467=CARTESIAN_POINT('Ctrl Pts',(-2.04706257850103,-1.17684515372061,
96.7230113585667));
#14468=CARTESIAN_POINT('Ctrl Pts',(-2.04007193789771,-1.19197928395999,
96.7230113585667));
#14469=CARTESIAN_POINT('Ctrl Pts',(-2.00405444114075,-1.26995403874251,
96.7230113585667));
#14470=CARTESIAN_POINT('Ctrl Pts',(-1.96403813188458,-1.34585382007019,
96.7230113585667));
#14471=CARTESIAN_POINT('Ctrl Pts',(-1.92021044960232,-1.41933358024217,
96.7230113585667));
#14472=CARTESIAN_POINT('Ctrl Pts',(-1.87632015444256,-1.49291831469027,
96.7230113585667));
#14473=CARTESIAN_POINT('Ctrl Pts',(-1.82860736272488,-1.56407711696169,
96.7230113585667));
#14474=CARTESIAN_POINT('Ctrl Pts',(-1.77720857262822,-1.632456840965,96.7230113585667));
#14475=CARTESIAN_POINT('Ctrl Pts',(-1.72691027409469,-1.6993724972497,96.7230113585667));
#14476=CARTESIAN_POINT('Ctrl Pts',(-1.67308174783659,-1.7636276913924,96.7230113585667));
#14477=CARTESIAN_POINT('Ctrl Pts',(-1.61580616688792,-1.82487124435851,
96.7230113585667));
#14478=CARTESIAN_POINT('Ctrl Pts',(-1.58344350848759,-1.85947594239974,
96.7230113585667));
#14479=CARTESIAN_POINT('Ctrl Pts',(-1.54997954742544,-1.89311869319316,
96.7230113585666));
#14480=CARTESIAN_POINT('Ctrl Pts',(-1.51542342753583,-1.92573157144902,
96.7230113585666));
#14481=CARTESIAN_POINT('Ctrl Pts',(-0.766343857929314,1.84166898597821,
96.7230113585667));
#14482=CARTESIAN_POINT('Ctrl Pts',(-0.775119863224321,1.83801716917172,
96.7233333684391));
#14483=CARTESIAN_POINT('Ctrl Pts',(-0.783869765361946,1.83430262156666,
96.7236553783116));
#14484=CARTESIAN_POINT('Ctrl Pts',(-0.792592670269147,1.83052572271892,
96.723977388184));
#14485=CARTESIAN_POINT('Ctrl Pts',(1.11860366144128,2.18029266352253,90.7500736540522));
#14486=CARTESIAN_POINT('Ctrl Pts',(1.10424245208046,2.18748324778742,90.7500736540522));
#14487=CARTESIAN_POINT('Ctrl Pts',(1.08988124271963,2.19467383205231,90.7500736540522));
#14488=CARTESIAN_POINT('Ctrl Pts',(1.07552003335881,2.2018644163172,90.7500736540522));
#14489=CARTESIAN_POINT('Origin',(0.,0.,88.2780718176998));
#14490=CARTESIAN_POINT('',(-1.77103530981268,-2.16889272333904E-16,88.2780718176998));
#14491=CARTESIAN_POINT('Origin',(-6.60753780880871,-8.0919000278027E-16,
88.2780718176998));
#14492=CARTESIAN_POINT('Origin',(0.,0.,88.2780718176998));
#14493=CARTESIAN_POINT('Origin',(3.86373699625103,0.,96.7230113585667));
#14494=CARTESIAN_POINT('',(-3.86373699625103,-4.73171314520603E-16,96.7230113585667));
#14495=CARTESIAN_POINT('Origin',(0.,0.,96.7230113585667));
#14496=CARTESIAN_POINT('Origin',(0.,0.,98.1470603273161));
#14497=CARTESIAN_POINT('',(-3.86373699625103,-4.73171314520603E-16,99.5711092960655));
#14498=CARTESIAN_POINT('Origin',(0.,0.,99.5711092960655));
#14499=CARTESIAN_POINT('',(-3.86373699625103,-4.73171314520603E-16,98.1470603273161));
#14500=CARTESIAN_POINT('Origin',(0.,0.,99.6988479078803));
#14501=CARTESIAN_POINT('',(-3.53729387716894,-4.33193562431847E-16,99.826586519695));
#14502=CARTESIAN_POINT('',(-3.70051543670999,4.53182438476226E-16,99.6988479078803));
#14503=CARTESIAN_POINT('Origin',(0.,0.,99.826586519695));
#14504=CARTESIAN_POINT('Origin',(0.684464879973279,0.,99.826586519695));
#14505=CARTESIAN_POINT('',(-0.684464879973279,-8.38227724388054E-17,99.826586519695));
#14506=CARTESIAN_POINT('Origin',(0.,0.,99.826586519695));
#14507=CARTESIAN_POINT('Origin',(0.,0.,98.9134919982045));
#14508=CARTESIAN_POINT('',(-0.684464879973279,-8.38227724388054E-17,98.000397476714));
#14509=CARTESIAN_POINT('Origin',(0.,0.,98.000397476714));
#14510=CARTESIAN_POINT('',(-0.684464879973279,-8.38227724388053E-17,98.9134919982045));
#14511=CARTESIAN_POINT('Origin',(0.,0.,98.000397476714));
#14512=CARTESIAN_POINT('Origin',(1.77103530981268,0.,87.0039956821063));
#14513=CARTESIAN_POINT('',(-1.77103530981268,-2.16889272333904E-16,87.0039956821063));
#14514=CARTESIAN_POINT('Origin',(0.,0.,87.0039956821063));
#14515=CARTESIAN_POINT('Origin',(0.,0.,87.6410337499031));
#14516=CARTESIAN_POINT('',(-1.77103530981268,-2.16889272333904E-16,87.6410337499031));
#14533=UNCERTAINTY_MEASURE_WITH_UNIT(LENGTH_MEASURE(0.01),#14545,
'DISTANCE_ACCURACY_VALUE',
'Maximum model space distance between geometric entities at asserted c
onnectivities');
#14534=UNCERTAINTY_MEASURE_WITH_UNIT(LENGTH_MEASURE(0.01),#14545,
'DISTANCE_ACCURACY_VALUE',
'Maximum model space distance between geometric entities at asserted c
onnectivities');
#14543=(
GEOMETRIC_REPRESENTATION_CONTEXT(3)
GLOBAL_UNCERTAINTY_ASSIGNED_CONTEXT((#14533))
GLOBAL_UNIT_ASSIGNED_CONTEXT((#14545,#14547,#14548))
REPRESENTATION_CONTEXT('','3D')
);
#14544=(
GEOMETRIC_REPRESENTATION_CONTEXT(3)
GLOBAL_UNCERTAINTY_ASSIGNED_CONTEXT((#14534))
GLOBAL_UNIT_ASSIGNED_CONTEXT((#14545,#14547,#14548))
REPRESENTATION_CONTEXT('','3D')
);
#14545=(
LENGTH_UNIT()
NAMED_UNIT(*)
SI_UNIT(.MILLI.,.METRE.)
);
#14547=(
NAMED_UNIT(*)
PLANE_ANGLE_UNIT()
SI_UNIT($,.RADIAN.)
);
#14548=(
NAMED_UNIT(*)
SI_UNIT($,.STERADIAN.)
SOLID_ANGLE_UNIT()
);
#14557=SHAPE_DEFINITION_REPRESENTATION(#14566,#14583);
#14566=PRODUCT_DEFINITION_SHAPE('',$,#14593);
#14583=SHAPE_REPRESENTATION('',(#2086),#14543);
#14584=PRODUCT_DEFINITION_CONTEXT('part definition',#14613,'design');
#14593=PRODUCT_DEFINITION('Screw_02','Screw_02',#14602,#14584);
#14602=PRODUCT_DEFINITION_FORMATION('',$,#14623);
#14613=APPLICATION_CONTEXT(
'Core Data for Automotive Mechanical Design Process');
#14614=PRODUCT_CONTEXT('part definition',#14613,'mechanical');
#14623=PRODUCT('Screw_02','Screw_02',$,(#14614));
#14627=PRESENTATION_STYLE_ASSIGNMENT((#14631));
#14631=SURFACE_STYLE_USAGE(.BOTH.,#14635);
#14635=SURFACE_SIDE_STYLE('',(#14639));
#14639=SURFACE_STYLE_FILL_AREA(#14643);
#14643=FILL_AREA_STYLE('Opaque(203,203,203)',(#14647));
#14647=FILL_AREA_STYLE_COLOUR('Opaque(203,203,203)',#14651);
#14651=COLOUR_RGB('Opaque(203,203,203)', 0.31764706, 0.68627451, 0.89019608);
ENDSEC;
END-ISO-10303-21;
